ISO-10303-21;
HEADER;
FILE_DESCRIPTION (('STEP AP214'),
    '1' );
FILE_NAME ('6. Lower Jaw.step',
    '2026-10-09T08:13:37',
    ( '' ),
    ( '' ),
    'SwSTEP 2.0',
    'SolidWorks 2021',
    '' );
FILE_SCHEMA (( 'AUTOMOTIVE_DESIGN' ));
ENDSEC;

DATA;
#6=DIRECTION ( 'NONE',  ( 1.000000000000000000, -0.000000000000000000, 0.000000000000000000 ) ) ;
#18=DIRECTION ( 'NONE',  ( 1.000000000000000000, 0.000000000000000000, 0.000000000000000000 ) ) ;
#21=FACE_OUTER_BOUND ( 'NONE', #40498, .T. ) ;
#33=DIRECTION ( 'NONE',  ( 0.000000000000000000, -0.000000000000000000, -1.000000000000000000 ) ) ;
#41=CARTESIAN_POINT ( 'NONE',  ( 39.74999999999999289, 18.74999999999997868, -3.750000000000000000 ) ) ;
#63=ORIENTED_EDGE ( 'NONE', *, *, #14885, .F. ) ;
#64=DIRECTION ( 'NONE',  ( 0.000000000000000000, 0.000000000000000000, -1.000000000000000000 ) ) ;
#68=EDGE_LOOP ( 'NONE', ( #29117, #12517, #42805, #36614 ) ) ;
#72=ADVANCED_FACE ( 'NONE', ( #68858 ), #63563, .T. ) ;
#91=EDGE_LOOP ( 'NONE', ( #34667, #18919, #19506, #38504 ) ) ;
#125=TOROIDAL_SURFACE ( 'NONE', #45179, 0.5000000000000000000, 0.2500000000000000000 ) ;
#138=CYLINDRICAL_SURFACE ( 'NONE', #6916, 0.2500000000000002220 ) ;
#142=DIRECTION ( 'NONE',  ( 0.000000000000000000, -1.000000000000000000, 0.000000000000000000 ) ) ;
#147=VECTOR ( 'NONE', #29815, 1000.000000000000000 ) ;
#161=ORIENTED_EDGE ( 'NONE', *, *, #21267, .T. ) ;
#164=SPHERICAL_SURFACE ( 'NONE', #64743, 0.2500000000000000000 ) ;
#173=EDGE_CURVE ( 'NONE', #4422, #21622, #52492, .T. ) ;
#178=ORIENTED_EDGE ( 'NONE', *, *, #22736, .F. ) ;
#181=DIRECTION ( 'NONE',  ( -1.000000000000000000, 0.000000000000000000, 0.000000000000000000 ) ) ;
#187=DIRECTION ( 'NONE',  ( -1.445602896647337931E-16, 1.000000000000000000, 0.000000000000000000 ) ) ;
#192=ORIENTED_EDGE ( 'NONE', *, *, #68046, .T. ) ;
#200=CARTESIAN_POINT ( 'NONE',  ( 52.99999999999999289, 27.99999999999998579, 3.750000000000000000 ) ) ;
#240=ORIENTED_EDGE ( 'NONE', *, *, #61435, .F. ) ;
#248=AXIS2_PLACEMENT_3D ( 'NONE', #65963, #7915, #18135 ) ;
#253=ORIENTED_EDGE ( 'NONE', *, *, #40055, .T. ) ;
#259=FACE_OUTER_BOUND ( 'NONE', #25224, .T. ) ;
#268=ORIENTED_EDGE ( 'NONE', *, *, #5778, .F. ) ;
#288=ORIENTED_EDGE ( 'NONE', *, *, #20970, .T. ) ;
#291=CARTESIAN_POINT ( 'NONE',  ( 0.000000000000000000, 21.74999999999998224, 3.750000000000000000 ) ) ;
#292=DIRECTION ( 'NONE',  ( 0.000000000000000000, 0.000000000000000000, 1.000000000000000000 ) ) ;
#295=AXIS2_PLACEMENT_3D ( 'NONE', #291, #21821, #59418 ) ;
#305=AXIS2_PLACEMENT_3D ( 'NONE', #48367, #58534, #16691 ) ;
#306=CIRCLE ( 'NONE', #39710, 0.2500000000000002220 ) ;
#329=LINE ( 'NONE', #43015, #27426 ) ;
#334=EDGE_CURVE ( 'NONE', #46687, #29083, #34195, .T. ) ;
#349=ORIENTED_EDGE ( 'NONE', *, *, #57912, .F. ) ;
#364=DIRECTION ( 'NONE',  ( 1.000000000000000000, 0.000000000000000000, 0.000000000000000000 ) ) ;
#377=ORIENTED_EDGE ( 'NONE', *, *, #6524, .T. ) ;
#385=AXIS2_PLACEMENT_3D ( 'NONE', #51419, #38910, #35597 ) ;
#412=DIRECTION ( 'NONE',  ( 0.000000000000000000, -0.000000000000000000, 1.000000000000000000 ) ) ;
#420=AXIS2_PLACEMENT_3D ( 'NONE', #64761, #28836, #27779 ) ;
#434=ORIENTED_EDGE ( 'NONE', *, *, #4204, .F. ) ;
#436=EDGE_CURVE ( 'NONE', #66069, #10730, #32165, .T. ) ;
#439=CARTESIAN_POINT ( 'NONE',  ( 61.74999999999998579, 30.74999999999999289, -4.000000000000000000 ) ) ;
#452=DIRECTION ( 'NONE',  ( -1.000000000000000000, 0.000000000000000000, 0.000000000000000000 ) ) ;
#455=EDGE_CURVE ( 'NONE', #58809, #68764, #43475, .T. ) ;
#459=AXIS2_PLACEMENT_3D ( 'NONE', #49067, #22282, #38157 ) ;
#460=CIRCLE ( 'NONE', #48869, 0.2500000000000002220 ) ;
#466=EDGE_LOOP ( 'NONE', ( #50263, #33098, #39209, #1885 ) ) ;
#506=ORIENTED_EDGE ( 'NONE', *, *, #15438, .F. ) ;
#509=CARTESIAN_POINT ( 'NONE',  ( 0.000000000000000000, 1.000000000000000222, 3.000000000000000000 ) ) ;
#521=CYLINDRICAL_SURFACE ( 'NONE', #54220, 0.2500000000000002220 ) ;
#567=AXIS2_PLACEMENT_3D ( 'NONE', #40858, #31645, #58735 ) ;
#568=EDGE_CURVE ( 'NONE', #2804, #25571, #6450, .T. ) ;
#578=EDGE_CURVE ( 'NONE', #68782, #823, #306, .T. ) ;
#589=DIRECTION ( 'NONE',  ( -2.312964634635740689E-15, 1.000000000000000000, -0.000000000000000000 ) ) ;
#590=ORIENTED_EDGE ( 'NONE', *, *, #62902, .T. ) ;
#597=LINE ( 'NONE', #54114, #32415 ) ;
#598=FACE_OUTER_BOUND ( 'NONE', #29023, .T. ) ;
#603=DIRECTION ( 'NONE',  ( -1.000000000000000000, 0.000000000000000000, 0.000000000000000000 ) ) ;
#640=SPHERICAL_SURFACE ( 'NONE', #63217, 0.2500000000000000000 ) ;
#643=CARTESIAN_POINT ( 'NONE',  ( 26.25000000000001066, 18.74999999999997868, -3.750000000000000000 ) ) ;
#666=LINE ( 'NONE', #54539, #66260 ) ;
#668=CYLINDRICAL_SURFACE ( 'NONE', #49557, 1.000000000000000000 ) ;
#692=DIRECTION ( 'NONE',  ( -0.000000000000000000, 0.000000000000000000, -1.000000000000000000 ) ) ;
#720=ADVANCED_FACE ( 'NONE', ( #53122 ), #26361, .T. ) ;
#741=ADVANCED_FACE ( 'NONE', ( #50258 ), #13012, .T. ) ;
#775=DIRECTION ( 'NONE',  ( 0.000000000000000000, 0.000000000000000000, 1.000000000000000000 ) ) ;
#815=DIRECTION ( 'NONE',  ( 1.000000000000000000, 0.000000000000000000, 0.000000000000000000 ) ) ;
#818=DIRECTION ( 'NONE',  ( 0.000000000000000000, 0.000000000000000000, -1.000000000000000000 ) ) ;
#821=DIRECTION ( 'NONE',  ( 0.000000000000000000, 1.000000000000000000, -0.000000000000000000 ) ) ;
#823=VERTEX_POINT ( 'NONE', #49569 ) ;
#825=DIRECTION ( 'NONE',  ( -1.000000000000000000, 0.000000000000000000, 0.000000000000000000 ) ) ;
#835=VERTEX_POINT ( 'NONE', #28774 ) ;
#845=DIRECTION ( 'NONE',  ( 1.000000000000000000, 0.000000000000000000, -0.000000000000000000 ) ) ;
#869=ORIENTED_EDGE ( 'NONE', *, *, #37055, .F. ) ;
#893=ORIENTED_EDGE ( 'NONE', *, *, #58691, .T. ) ;
#894=CARTESIAN_POINT ( 'NONE',  ( 14.09999999999999609, 11.99999999999999289, 3.500000000000004885 ) ) ;
#906=DIRECTION ( 'NONE',  ( 0.000000000000000000, -1.000000000000000000, 0.000000000000000000 ) ) ;
#912=CARTESIAN_POINT ( 'NONE',  ( 1.000000000000000000, 1.000000000000000222, 3.000000000000000000 ) ) ;
#945=ORIENTED_EDGE ( 'NONE', *, *, #68006, .F. ) ;
#957=AXIS2_PLACEMENT_3D ( 'NONE', #20614, #36831, #10071 ) ;
#963=ORIENTED_EDGE ( 'NONE', *, *, #66472, .F. ) ;
#970=CYLINDRICAL_SURFACE ( 'NONE', #33737, 0.2500000000000002220 ) ;
#976=DIRECTION ( 'NONE',  ( 0.000000000000000000, 0.000000000000000000, -1.000000000000000000 ) ) ;
#986=CIRCLE ( 'NONE', #40403, 0.2500000000000002220 ) ;
#989=ORIENTED_EDGE ( 'NONE', *, *, #32331, .T. ) ;
#1003=ORIENTED_EDGE ( 'NONE', *, *, #1274, .T. ) ;
#1008=TOROIDAL_SURFACE ( 'NONE', #8984, 0.7500000000000000000, 0.2500000000000000000 ) ;
#1010=CIRCLE ( 'NONE', #35957, 1.000000000000000000 ) ;
#1034=VERTEX_POINT ( 'NONE', #15419 ) ;
#1035=CARTESIAN_POINT ( 'NONE',  ( 62.24999999999998579, 33.99999999999999289, -3.750000000000000000 ) ) ;
#1057=EDGE_CURVE ( 'NONE', #33883, #50178, #6563, .T. ) ;
#1065=AXIS2_PLACEMENT_3D ( 'NONE', #36610, #68921, #58024 ) ;
#1073=CARTESIAN_POINT ( 'NONE',  ( 39.74999999999999289, 18.99999999999997868, 4.000000000000000000 ) ) ;
#1089=CARTESIAN_POINT ( 'NONE',  ( 39.74999999999999289, 18.74999999999997868, 3.750000000000000000 ) ) ;
#1092=ORIENTED_EDGE ( 'NONE', *, *, #60276, .T. ) ;
#1116=DIRECTION ( 'NONE',  ( -0.000000000000000000, -0.000000000000000000, 1.000000000000000000 ) ) ;
#1167=DIRECTION ( 'NONE',  ( -0.000000000000000000, 0.000000000000000000, -1.000000000000000000 ) ) ;
#1185=CARTESIAN_POINT ( 'NONE',  ( 1.000000000000000000, 1.000000000000000222, 3.000000000000000000 ) ) ;
#1186=ORIENTED_EDGE ( 'NONE', *, *, #33909, .F. ) ;
#1213=CARTESIAN_POINT ( 'NONE',  ( 17.25000000000000711, 25.24999999999998224, 3.750000000000000000 ) ) ;
#1224=DIRECTION ( 'NONE',  ( -1.000000000000000000, 0.000000000000000000, 0.000000000000000000 ) ) ;
#1232=ORIENTED_EDGE ( 'NONE', *, *, #57235, .T. ) ;
#1241=DIRECTION ( 'NONE',  ( -0.000000000000000000, -1.000000000000000000, -0.000000000000000000 ) ) ;
#1253=MECHANICAL_DESIGN_GEOMETRIC_PRESENTATION_REPRESENTATION('',(#11456),#65392);
#1271=DIRECTION ( 'NONE',  ( 1.000000000000000000, -0.000000000000000000, -0.000000000000000000 ) ) ;
#1274=EDGE_CURVE ( 'NONE', #33237, #54480, #4739, .T. ) ;
#1277=LINE ( 'NONE', #49203, #61033 ) ;
#1281=EDGE_CURVE ( 'NONE', #34416, #38988, #39322, .T. ) ;
#1284=DIRECTION ( 'NONE',  ( 1.000000000000000000, 0.000000000000000000, 0.000000000000000000 ) ) ;
#1287=AXIS2_PLACEMENT_3D ( 'NONE', #47917, #10571, #69642 ) ;
#1316=DIRECTION ( 'NONE',  ( 1.000000000000000000, -0.000000000000000000, 0.000000000000000000 ) ) ;
#1319=DIRECTION ( 'NONE',  ( -1.000000000000000000, 0.000000000000000000, 0.000000000000000000 ) ) ;
#1323=STYLED_ITEM ( 'NONE', ( #8302 ), #23504 ) ;
#1347=DIRECTION ( 'NONE',  ( -1.000000000000000000, 7.709882115452469292E-16, 0.000000000000000000 ) ) ;
#1393=ADVANCED_FACE ( 'NONE', ( #12430 ), #49750, .T. ) ;
#1395=CARTESIAN_POINT ( 'NONE',  ( 66.49999999999998579, 33.99999999999999289, 4.000000000000000000 ) ) ;
#1398=CARTESIAN_POINT ( 'NONE',  ( 3.249999999999998668, 36.74999999999999289, -3.750000000000000000 ) ) ;
#1399=CARTESIAN_POINT ( 'NONE',  ( 1.000000000000000000, 36.74999999999999289, -3.750000000000000000 ) ) ;
#1401=ADVANCED_FACE ( 'NONE', ( #54310 ), #49085, .T. ) ;
#1456=VECTOR ( 'NONE', #66838, 1000.000000000000000 ) ;
#1464=EDGE_CURVE ( 'NONE', #31245, #59005, #62374, .T. ) ;
#1478=DIRECTION ( 'NONE',  ( 0.000000000000000000, -1.000000000000000000, 0.000000000000000000 ) ) ;
#1497=DIRECTION ( 'NONE',  ( 0.000000000000000000, 0.000000000000000000, 1.000000000000000000 ) ) ;
#1504=EDGE_CURVE ( 'NONE', #34547, #21325, #2896, .T. ) ;
#1511=CARTESIAN_POINT ( 'NONE',  ( 0.2500000000000000000, 36.74999999999999289, 3.000000000000000000 ) ) ;
#1513=DIRECTION ( 'NONE',  ( 0.000000000000000000, 0.000000000000000000, -1.000000000000000000 ) ) ;
#1522=DIRECTION ( 'NONE',  ( 1.156482317317870344E-15, -1.000000000000000000, -0.000000000000000000 ) ) ;
#1538=ADVANCED_FACE ( 'NONE', ( #20505 ), #57449, .T. ) ;
#1544=SPHERICAL_SURFACE ( 'NONE', #65316, 0.2500000000000000000 ) ;
#1579=CARTESIAN_POINT ( 'NONE',  ( 10.99999999999999645, 11.99999999999999289, 3.500000000000004885 ) ) ;
#1580=CARTESIAN_POINT ( 'NONE',  ( -1.908195823574483386E-14, 24.74999999999996803, 4.000000000000000000 ) ) ;
#1589=CARTESIAN_POINT ( 'NONE',  ( 39.24999999999999289, 16.24999999999997513, -4.000000000000000000 ) ) ;
#1601=ORIENTED_EDGE ( 'NONE', *, *, #20283, .F. ) ;
#1602=AXIS2_PLACEMENT_3D ( 'NONE', #64294, #16145, #53733 ) ;
#1610=AXIS2_PLACEMENT_3D ( 'NONE', #32355, #32704, #38392 ) ;
#1621=DIRECTION ( 'NONE',  ( -1.000000000000000000, 0.000000000000000000, 0.000000000000000000 ) ) ;
#1642=DIRECTION ( 'NONE',  ( 0.000000000000000000, 0.000000000000000000, -1.000000000000000000 ) ) ;
#1650=DIRECTION ( 'NONE',  ( -1.000000000000000000, -7.709882115452468306E-16, 0.000000000000000000 ) ) ;
#1651=LINE ( 'NONE', #60764, #28776 ) ;
#1652=VERTEX_POINT ( 'NONE', #54585 ) ;
#1669=DIRECTION ( 'NONE',  ( 1.000000000000000000, 0.000000000000000000, 0.000000000000000000 ) ) ;
#1681=DIRECTION ( 'NONE',  ( -1.000000000000000000, 0.000000000000000000, 0.000000000000000000 ) ) ;
#1682=DIRECTION ( 'NONE',  ( -0.000000000000000000, 0.000000000000000000, -1.000000000000000000 ) ) ;
#1750=DIRECTION ( 'NONE',  ( 1.000000000000000000, -0.000000000000000000, 0.000000000000000000 ) ) ;
#1756=ORIENTED_EDGE ( 'NONE', *, *, #7312, .F. ) ;
#1773=EDGE_CURVE ( 'NONE', #32850, #4180, #8147, .T. ) ;
#1799=CARTESIAN_POINT ( 'NONE',  ( 3.249999999999999112, 34.24999999999998579, -4.000000000000000000 ) ) ;
#1805=ORIENTED_EDGE ( 'NONE', *, *, #57852, .F. ) ;
#1810=ORIENTED_EDGE ( 'NONE', *, *, #45487, .T. ) ;
#1811=DIRECTION ( 'NONE',  ( 0.000000000000000000, 0.000000000000000000, -1.000000000000000000 ) ) ;
#1833=EDGE_LOOP ( 'NONE', ( #2523, #16517, #30246, #42888 ) ) ;
#1857=VECTOR ( 'NONE', #11669, 1000.000000000000000 ) ;
#1860=EDGE_CURVE ( 'NONE', #23940, #51066, #49036, .T. ) ;
#1864=DIRECTION ( 'NONE',  ( 0.7071067811865447972, 0.000000000000000000, 0.7071067811865502373 ) ) ;
#1880=DIRECTION ( 'NONE',  ( 0.000000000000000000, -0.000000000000000000, -1.000000000000000000 ) ) ;
#1885=ORIENTED_EDGE ( 'NONE', *, *, #17807, .F. ) ;
#1891=VECTOR ( 'NONE', #60717, 1000.000000000000000 ) ;
#1897=( NAMED_UNIT ( * ) PLANE_ANGLE_UNIT ( ) SI_UNIT ( $, .RADIAN. ) );
#1909=ORIENTED_EDGE ( 'NONE', *, *, #66811, .F. ) ;
#1943=CARTESIAN_POINT ( 'NONE',  ( 0.2500000000000000000, 36.74999999999999289, -3.000000000000000000 ) ) ;
#1951=ORIENTED_EDGE ( 'NONE', *, *, #22847, .T. ) ;
#1970=CARTESIAN_POINT ( 'NONE',  ( 12.75000000000000533, 27.99999999999998224, 4.000000000000000000 ) ) ;
#1979=CIRCLE ( 'NONE', #8851, 1.000000000000000000 ) ;
#2003=ORIENTED_EDGE ( 'NONE', *, *, #7167, .T. ) ;
#2010=ORIENTED_EDGE ( 'NONE', *, *, #18790, .F. ) ;
#2012=ADVANCED_FACE ( 'NONE', ( #59088 ), #33132, .T. ) ;
#2020=CARTESIAN_POINT ( 'NONE',  ( 17.25000000000000711, 24.74999999999997868, -4.000000000000000000 ) ) ;
#2026=ORIENTED_EDGE ( 'NONE', *, *, #15373, .T. ) ;
#2036=ORIENTED_EDGE ( 'NONE', *, *, #45415, .F. ) ;
#2053=LINE ( 'NONE', #55942, #12463 ) ;
#2103=DIRECTION ( 'NONE',  ( 1.000000000000000000, 7.709882115452468306E-16, -0.000000000000000000 ) ) ;
#2175=DIRECTION ( 'NONE',  ( 0.000000000000000000, 0.000000000000000000, 1.000000000000000000 ) ) ;
#2205=CARTESIAN_POINT ( 'NONE',  ( 21.25000000000001066, 24.74999999999998224, -4.000000000000000000 ) ) ;
#2209=PLANE ( 'NONE',  #33470 ) ;
#2214=ORIENTED_EDGE ( 'NONE', *, *, #4094, .F. ) ;
#2215=CARTESIAN_POINT ( 'NONE',  ( 66.24999999999998579, 33.74999999999999289, -3.750000000000000000 ) ) ;
#2216=EDGE_CURVE ( 'NONE', #34249, #13744, #2256, .T. ) ;
#2220=ORIENTED_EDGE ( 'NONE', *, *, #11023, .T. ) ;
#2221=CARTESIAN_POINT ( 'NONE',  ( 44.25000000000000000, 21.74999999999998579, 3.750000000000000000 ) ) ;
#2238=VECTOR ( 'NONE', #40361, 1000.000000000000000 ) ;
#2256=LINE ( 'NONE', #24459, #37639 ) ;
#2278=CARTESIAN_POINT ( 'NONE',  ( 53.24999999999999289, 27.99999999999998579, -3.750000000000000000 ) ) ;
#2280=DIRECTION ( 'NONE',  ( 0.000000000000000000, 0.000000000000000000, -1.000000000000000000 ) ) ;
#2281=LINE ( 'NONE', #29788, #48310 ) ;
#2297=ORIENTED_EDGE ( 'NONE', *, *, #15659, .F. ) ;
#2303=DIRECTION ( 'NONE',  ( 0.000000000000000000, 0.000000000000000000, -1.000000000000000000 ) ) ;
#2339=ORIENTED_EDGE ( 'NONE', *, *, #33147, .T. ) ;
#2384=VECTOR ( 'NONE', #67549, 1000.000000000000000 ) ;
#2386=LINE ( 'NONE', #45418, #1456 ) ;
#2406=LINE ( 'NONE', #13716, #62136 ) ;
#2415=EDGE_CURVE ( 'NONE', #57518, #35469, #19497, .T. ) ;
#2428=CARTESIAN_POINT ( 'NONE',  ( 57.24999999999999289, 28.24999999999998934, 4.000000000000000000 ) ) ;
#2445=AXIS2_PLACEMENT_3D ( 'NONE', #17055, #1478, #38537 ) ;
#2446=ORIENTED_EDGE ( 'NONE', *, *, #61390, .T. ) ;
#2453=ORIENTED_EDGE ( 'NONE', *, *, #10095, .F. ) ;
#2455=FACE_OUTER_BOUND ( 'NONE', #46483, .T. ) ;
#2459=VERTEX_POINT ( 'NONE', #61629 ) ;
#2463=ADVANCED_FACE ( 'NONE', ( #66948 ), #50763, .F. ) ;
#2469=DIRECTION ( 'NONE',  ( -1.000000000000000000, 0.000000000000000000, 0.000000000000000000 ) ) ;
#2473=CIRCLE ( 'NONE', #20515, 0.7499999999999997780 ) ;
#2480=ADVANCED_FACE ( 'NONE', ( #62351, #45849, #55687 ), #8553, .T. ) ;
#2495=FACE_OUTER_BOUND ( 'NONE', #39996, .T. ) ;
#2496=CARTESIAN_POINT ( 'NONE',  ( 16.75000000000000711, 25.24999999999998224, -4.000000000000000000 ) ) ;
#2503=ORIENTED_EDGE ( 'NONE', *, *, #21511, .F. ) ;
#2523=ORIENTED_EDGE ( 'NONE', *, *, #33273, .T. ) ;
#2524=CIRCLE ( 'NONE', #20554, 0.5000000000000004441 ) ;
#2555=AXIS2_PLACEMENT_3D ( 'NONE', #35981, #4640, #57426 ) ;
#2570=DIRECTION ( 'NONE',  ( 0.000000000000000000, -0.000000000000000000, -1.000000000000000000 ) ) ;
#2574=DIRECTION ( 'NONE',  ( 0.000000000000000000, 1.000000000000000000, 0.000000000000000000 ) ) ;
#2575=AXIS2_PLACEMENT_3D ( 'NONE', #67750, #9367, #62795 ) ;
#2576=CIRCLE ( 'NONE', #42002, 0.2500000000000002220 ) ;
#2592=ORIENTED_EDGE ( 'NONE', *, *, #12382, .T. ) ;
#2603=ORIENTED_EDGE ( 'NONE', *, *, #64246, .F. ) ;
#2659=AXIS2_PLACEMENT_3D ( 'NONE', #51438, #18396, #39884 ) ;
#2663=LINE ( 'NONE', #6943, #5056 ) ;
#2673=DIRECTION ( 'NONE',  ( -1.000000000000000000, -1.156482317317870344E-15, 0.000000000000000000 ) ) ;
#2676=EDGE_LOOP ( 'NONE', ( #9878, #47349, #46477, #2010 ) ) ;
#2678=CIRCLE ( 'NONE', #42109, 0.2500000000000002220 ) ;
#2681=CARTESIAN_POINT ( 'NONE',  ( 1.000000000000000000, 36.99999999999999289, 3.750000000000000000 ) ) ;
#2721=CARTESIAN_POINT ( 'NONE',  ( 57.74999999999998579, 30.99999999999999289, 3.750000000000000000 ) ) ;
#2722=DIRECTION ( 'NONE',  ( -1.000000000000000000, 0.000000000000000000, 0.000000000000000000 ) ) ;
#2738=EDGE_LOOP ( 'NONE', ( #13558, #7318, #46143, #48998 ) ) ;
#2745=FACE_OUTER_BOUND ( 'NONE', #54559, .T. ) ;
#2753=FACE_OUTER_BOUND ( 'NONE', #8256, .T. ) ;
#2770=VERTEX_POINT ( 'NONE', #66144 ) ;
#2780=DIRECTION ( 'NONE',  ( 0.000000000000000000, 0.000000000000000000, -1.000000000000000000 ) ) ;
#2790=VERTEX_POINT ( 'NONE', #55246 ) ;
#2799=AXIS2_PLACEMENT_3D ( 'NONE', #29274, #54960, #56013 ) ;
#2804=VERTEX_POINT ( 'NONE', #23586 ) ;
#2817=CARTESIAN_POINT ( 'NONE',  ( 25.75000000000001066, 21.99999999999998224, 4.000000000000000000 ) ) ;
#2823=CARTESIAN_POINT ( 'NONE',  ( 53.24999999999999289, 27.74999999999998579, -3.750000000000000000 ) ) ;
#2824=EDGE_CURVE ( 'NONE', #8197, #4422, #36457, .T. ) ;
#2837=CARTESIAN_POINT ( 'NONE',  ( 61.74999999999998579, 31.24999999999999289, 4.000000000000000000 ) ) ;
#2861=EDGE_CURVE ( 'NONE', #64044, #34249, #64483, .T. ) ;
#2865=DIRECTION ( 'NONE',  ( 0.000000000000000000, 0.000000000000000000, 1.000000000000000000 ) ) ;
#2869=ORIENTED_EDGE ( 'NONE', *, *, #33273, .F. ) ;
#2889=AXIS2_PLACEMENT_3D ( 'NONE', #18890, #29088, #40063 ) ;
#2896=CIRCLE ( 'NONE', #11931, 0.2500000000000002220 ) ;
#2912=DIRECTION ( 'NONE',  ( 0.000000000000000000, 1.000000000000000000, 0.000000000000000000 ) ) ;
#2947=DIRECTION ( 'NONE',  ( 0.000000000000000000, 1.000000000000000000, 0.000000000000000000 ) ) ;
#2957=ORIENTED_EDGE ( 'NONE', *, *, #45632, .F. ) ;
#2964=ADVANCED_FACE ( 'NONE', ( #58725 ), #37882, .F. ) ;
#2965=DIRECTION ( 'NONE',  ( -1.000000000000000000, 0.000000000000000000, 0.000000000000000000 ) ) ;
#3016=ORIENTED_EDGE ( 'NONE', *, *, #4801, .T. ) ;
#3026=FACE_OUTER_BOUND ( 'NONE', #44690, .T. ) ;
#3034=EDGE_CURVE ( 'NONE', #50390, #3561, #49916, .T. ) ;
#3037=LINE ( 'NONE', #56559, #58847 ) ;
#3039=DIRECTION ( 'NONE',  ( -1.000000000000000000, 0.000000000000000000, 0.000000000000000000 ) ) ;
#3048=DIRECTION ( 'NONE',  ( -1.000000000000000000, 0.000000000000000000, 0.000000000000000000 ) ) ;
#3071=LINE ( 'NONE', #8427, #25917 ) ;
#3084=FILL_AREA_STYLE ('',( #8444 ) ) ;
#3102=EDGE_LOOP ( 'NONE', ( #3375, #31173, #49907, #49228 ) ) ;
#3103=CYLINDRICAL_SURFACE ( 'NONE', #46626, 0.2500000000000002220 ) ;
#3107=LINE ( 'NONE', #13366, #44515 ) ;
#3121=VECTOR ( 'NONE', #54835, 1000.000000000000000 ) ;
#3144=ORIENTED_EDGE ( 'NONE', *, *, #32812, .F. ) ;
#3147=EDGE_CURVE ( 'NONE', #33883, #8197, #15072, .T. ) ;
#3193=VECTOR ( 'NONE', #52078, 1000.000000000000000 ) ;
#3200=CARTESIAN_POINT ( 'NONE',  ( 0.000000000000000000, 0.000000000000000000, -4.000000000000000000 ) ) ;
#3201=DIRECTION ( 'NONE',  ( 0.000000000000000000, 0.000000000000000000, -1.000000000000000000 ) ) ;
#3210=CIRCLE ( 'NONE', #50420, 1.000000000000000000 ) ;
#3213=EDGE_CURVE ( 'NONE', #3825, #17887, #14332, .T. ) ;
#3220=ORIENTED_EDGE ( 'NONE', *, *, #5520, .T. ) ;
#3224=LINE ( 'NONE', #66967, #11706 ) ;
#3225=ADVANCED_FACE ( 'NONE', ( #3026 ), #57241, .F. ) ;
#3229=ORIENTED_EDGE ( 'NONE', *, *, #40628, .F. ) ;
#3230=AXIS2_PLACEMENT_3D ( 'NONE', #36907, #63930, #48154 ) ;
#3233=ORIENTED_EDGE ( 'NONE', *, *, #19785, .T. ) ;
#3243=DIRECTION ( 'NONE',  ( 0.000000000000000000, -0.000000000000000000, 1.000000000000000000 ) ) ;
#3267=ORIENTED_EDGE ( 'NONE', *, *, #52310, .T. ) ;
#3278=ADVANCED_FACE ( 'NONE', ( #21696 ), #164, .T. ) ;
#3280=LINE ( 'NONE', #13892, #24124 ) ;
#3294=VECTOR ( 'NONE', #12988, 1000.000000000000000 ) ;
#3296=DIRECTION ( 'NONE',  ( 1.000000000000000000, 0.000000000000000000, 0.000000000000000000 ) ) ;
#3329=DIRECTION ( 'NONE',  ( -1.000000000000000000, 0.000000000000000000, 0.000000000000000000 ) ) ;
#3330=DIRECTION ( 'NONE',  ( -0.000000000000000000, 0.000000000000000000, -1.000000000000000000 ) ) ;
#3363=EDGE_LOOP ( 'NONE', ( #20386, #63079, #68936, #44805 ) ) ;
#3375=ORIENTED_EDGE ( 'NONE', *, *, #21255, .T. ) ;
#3394=CIRCLE ( 'NONE', #18120, 0.2500000000000002220 ) ;
#3413=CARTESIAN_POINT ( 'NONE',  ( 57.74999999999999289, 28.24999999999998934, 4.000000000000000000 ) ) ;
#3415=ORIENTED_EDGE ( 'NONE', *, *, #68452, .F. ) ;
#3425=DIRECTION ( 'NONE',  ( -0.000000000000000000, -1.000000000000000000, -0.000000000000000000 ) ) ;
#3440=AXIS2_PLACEMENT_3D ( 'NONE', #26046, #42302, #31677 ) ;
#3453=DIRECTION ( 'NONE',  ( 7.709882115452441682E-16, -1.000000000000000000, 0.000000000000000000 ) ) ;
#3460=EDGE_CURVE ( 'NONE', #60522, #59058, #20124, .T. ) ;
#3467=CARTESIAN_POINT ( 'NONE',  ( 3.249999999999998668, 36.74999999999999289, 4.000000000000000000 ) ) ;
#3484=CARTESIAN_POINT ( 'NONE',  ( 16.75000000000000711, 27.74999999999998224, 3.750000000000000000 ) ) ;
#3490=FACE_OUTER_BOUND ( 'NONE', #40124, .T. ) ;
#3501=EDGE_LOOP ( 'NONE', ( #25914, #64832, #14198, #5261 ) ) ;
#3535=ORIENTED_EDGE ( 'NONE', *, *, #15302, .T. ) ;
#3541=EDGE_CURVE ( 'NONE', #61482, #20333, #6045, .T. ) ;
#3548=ADVANCED_FACE ( 'NONE', ( #64451 ), #38794, .T. ) ;
#3561=VERTEX_POINT ( 'NONE', #27481 ) ;
#3591=FACE_BOUND ( 'NONE', #53019, .T. ) ;
#3644=STYLED_ITEM ( 'NONE', ( #62191 ), #47581 ) ;
#3647=FACE_OUTER_BOUND ( 'NONE', #25622, .T. ) ;
#3663=DIRECTION ( 'NONE',  ( 0.000000000000000000, 1.000000000000000000, -0.000000000000000000 ) ) ;
#3671=AXIS2_PLACEMENT_3D ( 'NONE', #44926, #845, #22387 ) ;
#3673=CARTESIAN_POINT ( 'NONE',  ( 66.49999999999998579, 33.99999999999999289, 3.750000000000000000 ) ) ;
#3676=DIRECTION ( 'NONE',  ( -1.000000000000000000, 0.000000000000000000, 0.000000000000000000 ) ) ;
#3687=CARTESIAN_POINT ( 'NONE',  ( 43.75000000000000000, 19.24999999999998224, -3.750000000000000000 ) ) ;
#3691=EDGE_CURVE ( 'NONE', #20333, #57903, #8135, .T. ) ;
#3700=CIRCLE ( 'NONE', #8273, 0.2500000000000002220 ) ;
#3712=AXIS2_PLACEMENT_3D ( 'NONE', #28784, #39732, #34750 ) ;
#3716=VECTOR ( 'NONE', #7673, 1000.000000000000000 ) ;
#3721=DIRECTION ( 'NONE',  ( -1.000000000000000000, 0.000000000000000000, 0.000000000000000000 ) ) ;
#3744=DIRECTION ( 'NONE',  ( 1.000000000000000000, -0.000000000000000000, -0.000000000000000000 ) ) ;
#3765=CYLINDRICAL_SURFACE ( 'NONE', #65496, 3.100000000000000533 ) ;
#3775=CIRCLE ( 'NONE', #30709, 0.2500000000000002220 ) ;
#3777=ORIENTED_EDGE ( 'NONE', *, *, #46272, .F. ) ;
#3786=DIRECTION ( 'NONE',  ( 0.000000000000000000, -0.000000000000000000, 1.000000000000000000 ) ) ;
#3788=TOROIDAL_SURFACE ( 'NONE', #52158, 0.5000000000000000000, 0.2500000000000000000 ) ;
#3812=AXIS2_PLACEMENT_3D ( 'NONE', #54191, #27442, #38424 ) ;
#3814=CYLINDRICAL_SURFACE ( 'NONE', #4865, 0.2500000000000002220 ) ;
#3822=DIRECTION ( 'NONE',  ( -1.000000000000000000, 0.000000000000000000, 0.000000000000000000 ) ) ;
#3825=VERTEX_POINT ( 'NONE', #41912 ) ;
#3833=CARTESIAN_POINT ( 'NONE',  ( 44.00000000000000000, 19.24999999999998224, 4.000000000000000000 ) ) ;
#3843=ORIENTED_EDGE ( 'NONE', *, *, #38614, .T. ) ;
#3851=DIRECTION ( 'NONE',  ( 0.000000000000000000, 1.000000000000000000, 0.000000000000000000 ) ) ;
#3871=ORIENTED_EDGE ( 'NONE', *, *, #47980, .F. ) ;
#3878=EDGE_CURVE ( 'NONE', #50390, #47709, #49141, .T. ) ;
#3882=CYLINDRICAL_SURFACE ( 'NONE', #24065, 0.2500000000000002220 ) ;
#3884=EDGE_LOOP ( 'NONE', ( #893, #39481, #3871 ) ) ;
#3888=DIRECTION ( 'NONE',  ( 0.000000000000000000, -0.000000000000000000, 1.000000000000000000 ) ) ;
#3907=PLANE ( 'NONE',  #4905 ) ;
#3913=AXIS2_PLACEMENT_3D ( 'NONE', #15060, #48459, #21682 ) ;
#3926=VERTEX_POINT ( 'NONE', #21440 ) ;
#3956=DIRECTION ( 'NONE',  ( -2.312964634635740689E-15, 1.000000000000000000, -0.000000000000000000 ) ) ;
#3965=DIRECTION ( 'NONE',  ( 1.000000000000000000, 2.312964634635707951E-15, 0.000000000000000000 ) ) ;
#3975=DIRECTION ( 'NONE',  ( 1.000000000000000000, 0.000000000000000000, 0.000000000000000000 ) ) ;
#3985=CARTESIAN_POINT ( 'NONE',  ( 26.00000000000001066, 18.99999999999997868, 4.000000000000000000 ) ) ;
#3993=DIRECTION ( 'NONE',  ( 1.000000000000000000, 7.709882115452468306E-16, 0.000000000000000000 ) ) ;
#4035=DIRECTION ( 'NONE',  ( 1.000000000000000000, 0.000000000000000000, 0.000000000000000000 ) ) ;
#4043=CARTESIAN_POINT ( 'NONE',  ( 10.99999999999999645, 11.99999999999999289, 4.000000000000000000 ) ) ;
#4045=ADVANCED_FACE ( 'NONE', ( #56562 ), #46048, .T. ) ;
#4050=PRODUCT ( '6. Lower Jaw', '6. Lower Jaw', '', ( #11796 ) ) ;
#4076=DIRECTION ( 'NONE',  ( -1.000000000000000000, 0.000000000000000000, 0.000000000000000000 ) ) ;
#4094=EDGE_CURVE ( 'NONE', #51729, #67943, #55979, .T. ) ;
#4102=VERTEX_POINT ( 'NONE', #15084 ) ;
#4120=SPHERICAL_SURFACE ( 'NONE', #61997, 0.2500000000000000000 ) ;
#4122=LINE ( 'NONE', #2817, #51501 ) ;
#4180=VERTEX_POINT ( 'NONE', #35472 ) ;
#4195=CARTESIAN_POINT ( 'NONE',  ( 30.50000000000001066, 16.24999999999997513, -4.000000000000000000 ) ) ;
#4202=EDGE_LOOP ( 'NONE', ( #51029, #434, #506, #41564 ) ) ;
#4204=EDGE_CURVE ( 'NONE', #61310, #19333, #54052, .T. ) ;
#4218=CARTESIAN_POINT ( 'NONE',  ( 48.50000000000000000, 21.74999999999998579, -3.750000000000000000 ) ) ;
#4222=DIRECTION ( 'NONE',  ( -0.000000000000000000, -0.000000000000000000, -1.000000000000000000 ) ) ;
#4226=LINE ( 'NONE', #68997, #27380 ) ;
#4252=EDGE_CURVE ( 'NONE', #60522, #19333, #31250, .T. ) ;
#4257=VERTEX_POINT ( 'NONE', #54400 ) ;
#4261=VERTEX_POINT ( 'NONE', #6221 ) ;
#4280=EDGE_LOOP ( 'NONE', ( #14354, #20010, #7496, #18611 ) ) ;
#4286=ORIENTED_EDGE ( 'NONE', *, *, #30059, .F. ) ;
#4293=FACE_OUTER_BOUND ( 'NONE', #37995, .T. ) ;
#4307=DIRECTION ( 'NONE',  ( 0.000000000000000000, 0.000000000000000000, -1.000000000000000000 ) ) ;
#4321=CARTESIAN_POINT ( 'NONE',  ( 44.25000000000000000, 21.74999999999998579, 3.750000000000000000 ) ) ;
#4337=CARTESIAN_POINT ( 'NONE',  ( 68.99999999999998579, 1.000000000000008438, 3.000000000000000000 ) ) ;
#4338=FACE_OUTER_BOUND ( 'NONE', #61733, .T. ) ;
#4361=DIRECTION ( 'NONE',  ( 0.000000000000000000, 1.000000000000000000, 0.000000000000000000 ) ) ;
#4362=CARTESIAN_POINT ( 'NONE',  ( 0.000000000000000000, 15.74999999999997513, 4.000000000000000000 ) ) ;
#4373=ORIENTED_EDGE ( 'NONE', *, *, #41261, .F. ) ;
#4386=ORIENTED_EDGE ( 'NONE', *, *, #54151, .F. ) ;
#4417=EDGE_CURVE ( 'NONE', #33237, #51630, #31314, .T. ) ;
#4422=VERTEX_POINT ( 'NONE', #55081 ) ;
#4424=ORIENTED_EDGE ( 'NONE', *, *, #21022, .T. ) ;
#4426=AXIS2_PLACEMENT_3D ( 'NONE', #42749, #43455, #64142 ) ;
#4431=DIRECTION ( 'NONE',  ( 0.000000000000000000, 1.000000000000000000, 0.000000000000000000 ) ) ;
#4482=AXIS2_PLACEMENT_3D ( 'NONE', #44211, #17463, #51513 ) ;
#4502=CARTESIAN_POINT ( 'NONE',  ( 43.75000000000000000, 19.24999999999998224, 3.750000000000000000 ) ) ;
#4520=ORIENTED_EDGE ( 'NONE', *, *, #28307, .F. ) ;
#4525=AXIS2_PLACEMENT_3D ( 'NONE', #17621, #60155, #55913 ) ;
#4538=DIRECTION ( 'NONE',  ( -0.000000000000000000, -0.000000000000000000, -1.000000000000000000 ) ) ;
#4580=CARTESIAN_POINT ( 'NONE',  ( 55.89999999999999147, 11.99999999999999822, 4.000000000000000000 ) ) ;
#4599=DIRECTION ( 'NONE',  ( -1.000000000000000000, 0.000000000000000000, 0.000000000000000000 ) ) ;
#4610=DIRECTION ( 'NONE',  ( -1.000000000000000000, 0.000000000000000000, 0.000000000000000000 ) ) ;
#4614=ORIENTED_EDGE ( 'NONE', *, *, #31995, .F. ) ;
#4640=DIRECTION ( 'NONE',  ( 0.000000000000000000, 0.000000000000000000, 1.000000000000000000 ) ) ;
#4651=CARTESIAN_POINT ( 'NONE',  ( 0.000000000000000000, 33.74999999999998579, 3.750000000000000000 ) ) ;
#4660=ORIENTED_EDGE ( 'NONE', *, *, #59155, .F. ) ;
#4697=TOROIDAL_SURFACE ( 'NONE', #35028, 0.5000000000000000000, 0.2500000000000000000 ) ;
#4699=CARTESIAN_POINT ( 'NONE',  ( 53.24999999999999289, 27.74999999999998579, -4.000000000000000000 ) ) ;
#4702=ORIENTED_EDGE ( 'NONE', *, *, #42406, .T. ) ;
#4715=AXIS2_PLACEMENT_3D ( 'NONE', #5962, #16564, #1681 ) ;
#4716=DIRECTION ( 'NONE',  ( -1.000000000000000000, -2.168404344971006896E-16, 0.000000000000000000 ) ) ;
#4718=ORIENTED_EDGE ( 'NONE', *, *, #40463, .T. ) ;
#4729=ORIENTED_EDGE ( 'NONE', *, *, #17795, .T. ) ;
#4734=( NAMED_UNIT ( * ) PLANE_ANGLE_UNIT ( ) SI_UNIT ( $, .RADIAN. ) );
#4735=CARTESIAN_POINT ( 'NONE',  ( 44.25000000000000000, 21.74999999999998579, -3.750000000000000000 ) ) ;
#4739=LINE ( 'NONE', #57887, #69609 ) ;
#4762=ADVANCED_FACE ( 'NONE', ( #67310, #3591, #41652 ), #24723, .F. ) ;
#4777=CIRCLE ( 'NONE', #13776, 0.2500000000000002220 ) ;
#4797=CARTESIAN_POINT ( 'NONE',  ( 30.25000000000000711, 18.74999999999997868, 3.750000000000000000 ) ) ;
#4801=EDGE_CURVE ( 'NONE', #25904, #5648, #66206, .T. ) ;
#4807=CARTESIAN_POINT ( 'NONE',  ( 1.000000000000000000, 36.74999999999999289, -4.000000000000000000 ) ) ;
#4817=AXIS2_PLACEMENT_3D ( 'NONE', #52808, #26037, #47575 ) ;
#4828=DIRECTION ( 'NONE',  ( 0.000000000000000000, -1.000000000000000000, 0.000000000000000000 ) ) ;
#4835=FACE_OUTER_BOUND ( 'NONE', #44840, .T. ) ;
#4849=ADVANCED_FACE ( 'NONE', ( #4293 ), #14200, .T. ) ;
#4865=AXIS2_PLACEMENT_3D ( 'NONE', #20725, #68226, #36611 ) ;
#4871=CARTESIAN_POINT ( 'NONE',  ( 0.2500000000000000000, 36.99999999999999289, -3.000000000000000000 ) ) ;
#4880=ORIENTED_EDGE ( 'NONE', *, *, #65751, .T. ) ;
#4905=AXIS2_PLACEMENT_3D ( 'NONE', #47949, #63369, #41592 ) ;
#4939=DIRECTION ( 'NONE',  ( -0.000000000000000000, -0.000000000000000000, 1.000000000000000000 ) ) ;
#4963=DIRECTION ( 'NONE',  ( -1.000000000000000000, 0.000000000000000000, 0.000000000000000000 ) ) ;
#4972=AXIS2_PLACEMENT_3D ( 'NONE', #23369, #44868, #65938 ) ;
#4975=CARTESIAN_POINT ( 'NONE',  ( 17.25000000000000711, 24.74999999999997868, -3.750000000000000000 ) ) ;
#4980=CARTESIAN_POINT ( 'NONE',  ( 0.000000000000000000, 33.74999999999999289, 4.000000000000000000 ) ) ;
#4981=EDGE_LOOP ( 'NONE', ( #42214, #2453, #69608, #54827 ) ) ;
#5008=DIRECTION ( 'NONE',  ( -0.000000000000000000, 0.000000000000000000, -1.000000000000000000 ) ) ;
#5017=ORIENTED_EDGE ( 'NONE', *, *, #65668, .T. ) ;
#5029=CARTESIAN_POINT ( 'NONE',  ( 39.24999999999999289, 16.24999999999997513, 3.750000000000000000 ) ) ;
#5032=DIRECTION ( 'NONE',  ( 0.000000000000000000, 0.000000000000000000, -1.000000000000000000 ) ) ;
#5039=AXIS2_PLACEMENT_3D ( 'NONE', #20995, #59288, #42493 ) ;
#5056=VECTOR ( 'NONE', #61101, 1000.000000000000000 ) ;
#5080=EDGE_LOOP ( 'NONE', ( #7769, #3777, #33373, #22096 ) ) ;
#5085=CARTESIAN_POINT ( 'NONE',  ( 66.74999999999998579, 36.75000000000000000, 3.750000000000000000 ) ) ;
#5104=EDGE_CURVE ( 'NONE', #1652, #46628, #35429, .T. ) ;
#5107=CYLINDRICAL_SURFACE ( 'NONE', #35717, 0.2500000000000002220 ) ;
#5128=LINE ( 'NONE', #43181, #51734 ) ;
#5133=AXIS2_PLACEMENT_3D ( 'NONE', #9533, #58060, #40505 ) ;
#5137=AXIS2_PLACEMENT_3D ( 'NONE', #17563, #60426, #12585 ) ;
#5173=DIRECTION ( 'NONE',  ( -1.000000000000000000, -1.445602896647336698E-16, 0.000000000000000000 ) ) ;
#5175=DIRECTION ( 'NONE',  ( 0.000000000000000000, 0.000000000000000000, -1.000000000000000000 ) ) ;
#5188=DIRECTION ( 'NONE',  ( 0.000000000000000000, 0.000000000000000000, -1.000000000000000000 ) ) ;
#5192=EDGE_CURVE ( 'NONE', #2770, #25430, #14086, .T. ) ;
#5208=CIRCLE ( 'NONE', #44589, 3.599999999999992095 ) ;
#5222=DIRECTION ( 'NONE',  ( 0.000000000000000000, 0.000000000000000000, -1.000000000000000000 ) ) ;
#5237=ORIENTED_EDGE ( 'NONE', *, *, #20348, .T. ) ;
#5249=ORIENTED_EDGE ( 'NONE', *, *, #38652, .F. ) ;
#5250=DIRECTION ( 'NONE',  ( -0.000000000000000000, 0.000000000000000000, -1.000000000000000000 ) ) ;
#5255=LINE ( 'NONE', #64008, #20755 ) ;
#5261=ORIENTED_EDGE ( 'NONE', *, *, #62101, .F. ) ;
#5271=LINE ( 'NONE', #16906, #44801 ) ;
#5273=EDGE_CURVE ( 'NONE', #69646, #64044, #32599, .T. ) ;
#5284=FACE_OUTER_BOUND ( 'NONE', #30715, .T. ) ;
#5307=EDGE_CURVE ( 'NONE', #29039, #37744, #53717, .T. ) ;
#5313=ORIENTED_EDGE ( 'NONE', *, *, #33898, .F. ) ;
#5324=CARTESIAN_POINT ( 'NONE',  ( 0.000000000000000000, 1.000000000000000222, 4.000000000000000000 ) ) ;
#5338=ORIENTED_EDGE ( 'NONE', *, *, #36758, .T. ) ;
#5357=AXIS2_PLACEMENT_3D ( 'NONE', #4735, #4361, #53622 ) ;
#5374=VERTEX_POINT ( 'NONE', #49506 ) ;
#5378=ADVANCED_FACE ( 'NONE', ( #27312 ), #48495, .F. ) ;
#5430=CIRCLE ( 'NONE', #32408, 0.2500000000000002220 ) ;
#5469=ORIENTED_EDGE ( 'NONE', *, *, #49330, .F. ) ;
#5473=ORIENTED_EDGE ( 'NONE', *, *, #65456, .T. ) ;
#5484=ORIENTED_EDGE ( 'NONE', *, *, #59951, .F. ) ;
#5486=CIRCLE ( 'NONE', #68446, 0.2500000000000002220 ) ;
#5500=DIRECTION ( 'NONE',  ( -1.000000000000000000, 0.000000000000000000, 0.000000000000000000 ) ) ;
#5511=DIRECTION ( 'NONE',  ( 0.000000000000000000, -0.000000000000000000, 1.000000000000000000 ) ) ;
#5520=EDGE_CURVE ( 'NONE', #41879, #60408, #35406, .T. ) ;
#5535=AXIS2_PLACEMENT_3D ( 'NONE', #21699, #59665, #7261 ) ;
#5562=ORIENTED_EDGE ( 'NONE', *, *, #64246, .T. ) ;
#5574=FACE_OUTER_BOUND ( 'NONE', #32871, .T. ) ;
#5576=( NAMED_UNIT ( * ) SI_UNIT ( $, .STERADIAN. ) SOLID_ANGLE_UNIT ( ) );
#5579=CARTESIAN_POINT ( 'NONE',  ( 8.000000000000001776, 31.24999999999998579, 3.750000000000000000 ) ) ;
#5593=DIRECTION ( 'NONE',  ( 0.000000000000000000, 0.000000000000000000, -1.000000000000000000 ) ) ;
#5602=TOROIDAL_SURFACE ( 'NONE', #51679, 0.5000000000000000000, 0.2500000000000000000 ) ;
#5603=ORIENTED_EDGE ( 'NONE', *, *, #68419, .F. ) ;
#5640=CARTESIAN_POINT ( 'NONE',  ( 68.99999999999998579, 36.75000000000000000, -3.000000000000000000 ) ) ;
#5648=VERTEX_POINT ( 'NONE', #50579 ) ;
#5651=ORIENTED_EDGE ( 'NONE', *, *, #10981, .T. ) ;
#5656=VECTOR ( 'NONE', #18860, 1000.000000000000000 ) ;
#5677=CARTESIAN_POINT ( 'NONE',  ( 48.74999999999999289, 24.99999999999998579, -3.750000000000000000 ) ) ;
#5681=CYLINDRICAL_SURFACE ( 'NONE', #10377, 0.2500000000000002220 ) ;
#5687=VERTEX_POINT ( 'NONE', #23164 ) ;
#5694=TOROIDAL_SURFACE ( 'NONE', #22534, 0.5000000000000000000, 0.2500000000000000000 ) ;
#5707=EDGE_CURVE ( 'NONE', #6066, #36322, #19747, .T. ) ;
#5734=EDGE_LOOP ( 'NONE', ( #31811, #12693, #52000, #2957 ) ) ;
#5741=CARTESIAN_POINT ( 'NONE',  ( 39.74999999999999289, 16.24999999999997513, -4.000000000000000000 ) ) ;
#5764=CARTESIAN_POINT ( 'NONE',  ( 26.25000000000001066, 19.24999999999997868, -3.750000000000000000 ) ) ;
#5778=EDGE_CURVE ( 'NONE', #51323, #48755, #18555, .T. ) ;
#5787=ADVANCED_FACE ( 'NONE', ( #30842 ), #34723, .T. ) ;
#5797=AXIS2_PLACEMENT_3D ( 'NONE', #21085, #15839, #10199 ) ;
#5808=CIRCLE ( 'NONE', #28229, 0.2500000000000002220 ) ;
#5826=VECTOR ( 'NONE', #60830, 1000.000000000000000 ) ;
#5829=AXIS2_PLACEMENT_3D ( 'NONE', #29090, #35459, #50585 ) ;
#5833=CYLINDRICAL_SURFACE ( 'NONE', #30935, 0.2500000000000002220 ) ;
#5853=VERTEX_POINT ( 'NONE', #4807 ) ;
#5854=CIRCLE ( 'NONE', #4715, 0.5000000000000004441 ) ;
#5858=DIRECTION ( 'NONE',  ( 1.000000000000000000, 0.000000000000000000, 0.000000000000000000 ) ) ;
#5869=DIRECTION ( 'NONE',  ( 0.000000000000000000, 0.000000000000000000, -1.000000000000000000 ) ) ;
#5875=CARTESIAN_POINT ( 'NONE',  ( 7.750000000000000000, 33.74999999999998579, 3.750000000000000000 ) ) ;
#5886=EDGE_CURVE ( 'NONE', #51660, #32231, #46670, .T. ) ;
#5909=EDGE_LOOP ( 'NONE', ( #66501, #67560, #27451, #36624 ) ) ;
#5920=ORIENTED_EDGE ( 'NONE', *, *, #40204, .T. ) ;
#5921=DIRECTION ( 'NONE',  ( 0.000000000000000000, 0.000000000000000000, -1.000000000000000000 ) ) ;
#5944=TOROIDAL_SURFACE ( 'NONE', #63257, 0.5000000000000000000, 0.2500000000000000000 ) ;
#5946=EDGE_LOOP ( 'NONE', ( #16127, #10788 ) ) ;
#5951=CIRCLE ( 'NONE', #20573, 0.2500000000000002220 ) ;
#5952=DIRECTION ( 'NONE',  ( -0.000000000000000000, 1.000000000000000000, -0.000000000000000000 ) ) ;
#5956=EDGE_CURVE ( 'NONE', #15190, #68534, #56717, .T. ) ;
#5962=CARTESIAN_POINT ( 'NONE',  ( 8.250000000000001776, 31.24999999999998579, -4.000000000000000000 ) ) ;
#5973=CARTESIAN_POINT ( 'NONE',  ( 12.25000000000000533, 28.24999999999998224, 4.000000000000000000 ) ) ;
#5980=DIRECTION ( 'NONE',  ( -1.000000000000000000, 0.000000000000000000, 0.000000000000000000 ) ) ;
#5987=DIRECTION ( 'NONE',  ( -1.000000000000000000, 0.000000000000000000, 0.000000000000000000 ) ) ;
#5997=CIRCLE ( 'NONE', #47653, 0.2500000000000002220 ) ;
#6020=DIRECTION ( 'NONE',  ( 0.000000000000000000, 0.000000000000000000, -1.000000000000000000 ) ) ;
#6028=ADVANCED_FACE ( 'NONE', ( #64928 ), #28928, .T. ) ;
#6041=DIRECTION ( 'NONE',  ( 0.000000000000000000, -1.000000000000000000, 0.000000000000000000 ) ) ;
#6045=LINE ( 'NONE', #38460, #1857 ) ;
#6066=VERTEX_POINT ( 'NONE', #509 ) ;
#6069=CARTESIAN_POINT ( 'NONE',  ( 26.25000000000001066, 18.74999999999997868, 4.000000000000000000 ) ) ;
#6075=AXIS2_PLACEMENT_3D ( 'NONE', #61912, #56286, #23254 ) ;
#6105=DIRECTION ( 'NONE',  ( 0.000000000000000000, -1.000000000000000000, 0.000000000000000000 ) ) ;
#6119=CIRCLE ( 'NONE', #45494, 0.2499999999999997780 ) ;
#6141=CARTESIAN_POINT ( 'NONE',  ( 16.75000000000000711, 27.99999999999998224, -3.750000000000000000 ) ) ;
#6176=TOROIDAL_SURFACE ( 'NONE', #1602, 0.7500000000000000000, 0.2500000000000000000 ) ;
#6181=CARTESIAN_POINT ( 'NONE',  ( 21.50000000000000711, 22.24999999999998224, 3.750000000000000000 ) ) ;
#6184=ADVANCED_FACE ( 'NONE', ( #25747 ), #14505, .F. ) ;
#6196=LINE ( 'NONE', #33962, #52965 ) ;
#6197=VERTEX_POINT ( 'NONE', #14882 ) ;
#6203=EDGE_CURVE ( 'NONE', #17336, #19236, #57785, .T. ) ;
#6208=CARTESIAN_POINT ( 'NONE',  ( 25.75000000000001066, 21.74999999999998224, 3.750000000000000000 ) ) ;
#6221=CARTESIAN_POINT ( 'NONE',  ( 66.49999999999998579, 36.75000000000000000, -3.750000000000000000 ) ) ;
#6230=DIRECTION ( 'NONE',  ( 0.000000000000000000, 0.000000000000000000, -1.000000000000000000 ) ) ;
#6268=CIRCLE ( 'NONE', #24248, 0.2500000000000002220 ) ;
#6285=FILL_AREA_STYLE ('',( #43301 ) ) ;
#6293=DIRECTION ( 'NONE',  ( 1.000000000000000000, 0.000000000000000000, 0.000000000000000000 ) ) ;
#6295=CARTESIAN_POINT ( 'NONE',  ( 10.99999999999999645, 11.99999999999999289, 4.000000000000000000 ) ) ;
#6310=CARTESIAN_POINT ( 'NONE',  ( 59.00000000000000000, 11.99999999999999822, 4.000000000000000000 ) ) ;
#6351=EDGE_CURVE ( 'NONE', #14037, #6066, #38087, .T. ) ;
#6384=ORIENTED_EDGE ( 'NONE', *, *, #12694, .T. ) ;
#6414=ADVANCED_FACE ( 'NONE', ( #66872 ), #60195, .F. ) ;
#6421=ADVANCED_FACE ( 'NONE', ( #50339 ), #61549, .F. ) ;
#6423=LINE ( 'NONE', #1073, #33235 ) ;
#6450=LINE ( 'NONE', #44156, #12717 ) ;
#6464=CARTESIAN_POINT ( 'NONE',  ( 25.75000000000001066, 21.74999999999998224, 3.750000000000000000 ) ) ;
#6486=EDGE_CURVE ( 'NONE', #5687, #64812, #56653, .T. ) ;
#6505=FACE_OUTER_BOUND ( 'NONE', #3884, .T. ) ;
#6516=ORIENTED_EDGE ( 'NONE', *, *, #30720, .F. ) ;
#6518=DIRECTION ( 'NONE',  ( -2.312964634635740689E-15, 1.000000000000000000, 0.000000000000000000 ) ) ;
#6524=EDGE_CURVE ( 'NONE', #26545, #42069, #38659, .T. ) ;
#6534=ORIENTED_EDGE ( 'NONE', *, *, #60276, .F. ) ;
#6538=DIRECTION ( 'NONE',  ( 0.000000000000000000, 0.000000000000000000, -1.000000000000000000 ) ) ;
#6543=DIRECTION ( 'NONE',  ( 0.000000000000000000, 1.000000000000000000, 0.000000000000000000 ) ) ;
#6547=ORIENTED_EDGE ( 'NONE', *, *, #56652, .F. ) ;
#6553=ORIENTED_EDGE ( 'NONE', *, *, #36067, .F. ) ;
#6559=CIRCLE ( 'NONE', #57138, 0.2500000000000002220 ) ;
#6563=CIRCLE ( 'NONE', #45934, 0.2500000000000002220 ) ;
#6601=FACE_OUTER_BOUND ( 'NONE', #45853, .T. ) ;
#6604=CARTESIAN_POINT ( 'NONE',  ( 43.75000000000000000, 18.99999999999998224, -3.750000000000000000 ) ) ;
#6607=VERTEX_POINT ( 'NONE', #5579 ) ;
#6618=CIRCLE ( 'NONE', #39217, 0.2500000000000002220 ) ;
#6625=CARTESIAN_POINT ( 'NONE',  ( 12.75000000000000533, 28.24999999999998224, -3.750000000000000000 ) ) ;
#6635=CARTESIAN_POINT ( 'NONE',  ( 53.24999999999999289, 27.74999999999998579, -3.750000000000000000 ) ) ;
#6654=VECTOR ( 'NONE', #45603, 1000.000000000000000 ) ;
#6689=DIRECTION ( 'NONE',  ( 0.000000000000000000, -1.000000000000000000, 0.000000000000000000 ) ) ;
#6691=TOROIDAL_SURFACE ( 'NONE', #57262, 0.5000000000000000000, 0.2500000000000000000 ) ;
#6692=DIRECTION ( 'NONE',  ( 0.000000000000000000, 1.000000000000000000, 0.000000000000000000 ) ) ;
#6703=AXIS2_PLACEMENT_3D ( 'NONE', #40464, #61882, #56620 ) ;
#6710=ORIENTED_EDGE ( 'NONE', *, *, #48274, .F. ) ;
#6716=ORIENTED_EDGE ( 'NONE', *, *, #22736, .T. ) ;
#6720=DIRECTION ( 'NONE',  ( 0.000000000000000000, -1.000000000000000000, 0.000000000000000000 ) ) ;
#6749=ORIENTED_EDGE ( 'NONE', *, *, #48408, .T. ) ;
#6752=FACE_OUTER_BOUND ( 'NONE', #48800, .T. ) ;
#6758=CIRCLE ( 'NONE', #69684, 0.2500000000000002220 ) ;
#6759=CARTESIAN_POINT ( 'NONE',  ( 21.50000000000001066, 24.74999999999998224, 3.750000000000000000 ) ) ;
#6770=ORIENTED_EDGE ( 'NONE', *, *, #38267, .T. ) ;
#6771=CARTESIAN_POINT ( 'NONE',  ( 26.25000000000001066, 19.24999999999997868, 3.750000000000000000 ) ) ;
#6808=ORIENTED_EDGE ( 'NONE', *, *, #64963, .T. ) ;
#6811=ORIENTED_EDGE ( 'NONE', *, *, #38759, .F. ) ;
#6819=EDGE_LOOP ( 'NONE', ( #3535, #44575, #10526, #62835 ) ) ;
#6828=CARTESIAN_POINT ( 'NONE',  ( 61.74999999999998579, 31.24999999999999289, -3.750000000000000000 ) ) ;
#6829=CIRCLE ( 'NONE', #49533, 0.2500000000000002220 ) ;
#6853=CARTESIAN_POINT ( 'NONE',  ( 30.50000000000000711, 18.99999999999997868, 3.750000000000000000 ) ) ;
#6876=DIRECTION ( 'NONE',  ( -1.000000000000000000, 0.000000000000000000, 0.000000000000000000 ) ) ;
#6879=AXIS2_PLACEMENT_3D ( 'NONE', #59548, #412, #55312 ) ;
#6889=CARTESIAN_POINT ( 'NONE',  ( 16.75000000000000711, 27.74999999999998224, -3.750000000000000000 ) ) ;
#6898=CARTESIAN_POINT ( 'NONE',  ( 69.99999999999998579, 8.572527594031471415E-15, 4.000000000000000000 ) ) ;
#6916=AXIS2_PLACEMENT_3D ( 'NONE', #32927, #43528, #54362 ) ;
#6939=DIRECTION ( 'NONE',  ( 0.000000000000000000, 1.000000000000000000, 0.000000000000000000 ) ) ;
#6943=CARTESIAN_POINT ( 'NONE',  ( 62.10000000000000142, 11.99999999999999822, 4.000000000000000000 ) ) ;
#6950=EDGE_LOOP ( 'NONE', ( #49253, #53968, #33211 ) ) ;
#6955=CYLINDRICAL_SURFACE ( 'NONE', #36061, 0.2500000000000002220 ) ;
#6974=DIRECTION ( 'NONE',  ( 0.000000000000000000, 0.000000000000000000, -1.000000000000000000 ) ) ;
#6976=VECTOR ( 'NONE', #40424, 1000.000000000000000 ) ;
#6996=DIRECTION ( 'NONE',  ( -0.000000000000000000, 0.000000000000000000, -1.000000000000000000 ) ) ;
#7004=ORIENTED_EDGE ( 'NONE', *, *, #28513, .F. ) ;
#7019=DIRECTION ( 'NONE',  ( -1.000000000000000000, 0.000000000000000000, 0.000000000000000000 ) ) ;
#7035=DIRECTION ( 'NONE',  ( 0.000000000000000000, 0.000000000000000000, 1.000000000000000000 ) ) ;
#7049=CARTESIAN_POINT ( 'NONE',  ( 8.000000000000000000, 33.99999999999998579, 4.000000000000000000 ) ) ;
#7056=ORIENTED_EDGE ( 'NONE', *, *, #33865, .T. ) ;
#7064=ADVANCED_FACE ( 'NONE', ( #37230 ), #521, .T. ) ;
#7089=ADVANCED_FACE ( 'NONE', ( #17145 ), #12868, .F. ) ;
#7092=CYLINDRICAL_SURFACE ( 'NONE', #12628, 0.2500000000000002220 ) ;
#7094=ADVANCED_FACE ( 'NONE', ( #16795 ), #22744, .T. ) ;
#7101=ORIENTED_EDGE ( 'NONE', *, *, #68629, .T. ) ;
#7106=VERTEX_POINT ( 'NONE', #45272 ) ;
#7120=DIRECTION ( 'NONE',  ( -1.000000000000000000, 0.000000000000000000, 0.000000000000000000 ) ) ;
#7128=AXIS2_PLACEMENT_3D ( 'NONE', #51002, #45071, #35163 ) ;
#7129=CARTESIAN_POINT ( 'NONE',  ( 57.74999999999998579, 30.74999999999999289, -3.750000000000000000 ) ) ;
#7139=CARTESIAN_POINT ( 'NONE',  ( 66.74999999999998579, 37.00000000000000000, 3.750000000000000000 ) ) ;
#7145=ORIENTED_EDGE ( 'NONE', *, *, #21079, .F. ) ;
#7154=ADVANCED_FACE ( 'NONE', ( #27638 ), #39634, .F. ) ;
#7155=VECTOR ( 'NONE', #56037, 1000.000000000000000 ) ;
#7167=EDGE_CURVE ( 'NONE', #37329, #61605, #68850, .T. ) ;
#7188=ORIENTED_EDGE ( 'NONE', *, *, #43920, .F. ) ;
#7200=ORIENTED_EDGE ( 'NONE', *, *, #45078, .F. ) ;
#7217=DIRECTION ( 'NONE',  ( 0.000000000000000000, 0.000000000000000000, 1.000000000000000000 ) ) ;
#7229=DIRECTION ( 'NONE',  ( -1.000000000000000000, 0.000000000000000000, 0.000000000000000000 ) ) ;
#7233=EDGE_CURVE ( 'NONE', #28073, #24442, #50859, .T. ) ;
#7234=ORIENTED_EDGE ( 'NONE', *, *, #48728, .F. ) ;
#7261=DIRECTION ( 'NONE',  ( 1.000000000000000000, 0.000000000000000000, 0.000000000000000000 ) ) ;
#7267=ORIENTED_EDGE ( 'NONE', *, *, #37229, .F. ) ;
#7271=AXIS2_PLACEMENT_3D ( 'NONE', #55719, #17424, #1497 ) ;
#7274=DIRECTION ( 'NONE',  ( 0.000000000000000000, 0.000000000000000000, 1.000000000000000000 ) ) ;
#7285=ORIENTED_EDGE ( 'NONE', *, *, #24038, .T. ) ;
#7297=CYLINDRICAL_SURFACE ( 'NONE', #49488, 0.2500000000000002220 ) ;
#7299=AXIS2_PLACEMENT_3D ( 'NONE', #57639, #3786, #9462 ) ;
#7310=ADVANCED_FACE ( 'NONE', ( #48391 ), #3788, .T. ) ;
#7312=EDGE_CURVE ( 'NONE', #51526, #5648, #32494, .T. ) ;
#7313=CIRCLE ( 'NONE', #2799, 0.2500000000000002220 ) ;
#7318=ORIENTED_EDGE ( 'NONE', *, *, #38319, .F. ) ;
#7323=CARTESIAN_POINT ( 'NONE',  ( 26.25000000000001066, 18.99999999999997868, 4.000000000000000000 ) ) ;
#7334=ORIENTED_EDGE ( 'NONE', *, *, #12935, .F. ) ;
#7346=FACE_OUTER_BOUND ( 'NONE', #59226, .T. ) ;
#7370=TOROIDAL_SURFACE ( 'NONE', #23137, 0.5000000000000000000, 0.2500000000000000000 ) ;
#7371=ORIENTED_EDGE ( 'NONE', *, *, #15052, .T. ) ;
#7379=CARTESIAN_POINT ( 'NONE',  ( 30.25000000000000711, 18.99999999999997868, 4.000000000000000000 ) ) ;
#7390=CARTESIAN_POINT ( 'NONE',  ( 66.24999999999998579, 33.99999999999999289, -3.750000000000000000 ) ) ;
#7391=CARTESIAN_POINT ( 'NONE',  ( 52.75000000000000000, 25.24999999999998579, 3.750000000000000000 ) ) ;
#7430=CIRCLE ( 'NONE', #34378, 0.2500000000000002220 ) ;
#7438=DIRECTION ( 'NONE',  ( -1.000000000000000000, 0.000000000000000000, 0.000000000000000000 ) ) ;
#7454=VERTEX_POINT ( 'NONE', #62691 ) ;
#7455=EDGE_LOOP ( 'NONE', ( #8315, #32600, #10237, #38297 ) ) ;
#7456=DIRECTION ( 'NONE',  ( 0.000000000000000000, 0.000000000000000000, 1.000000000000000000 ) ) ;
#7471=DIRECTION ( 'NONE',  ( -1.000000000000000000, 0.000000000000000000, 0.000000000000000000 ) ) ;
#7482=CARTESIAN_POINT ( 'NONE',  ( 12.50000000000000355, 30.74999999999998579, 3.750000000000000000 ) ) ;
#7485=LINE ( 'NONE', #66211, #24628 ) ;
#7489=EDGE_LOOP ( 'NONE', ( #55344, #33433, #240 ) ) ;
#7496=ORIENTED_EDGE ( 'NONE', *, *, #60988, .F. ) ;
#7546=ORIENTED_EDGE ( 'NONE', *, *, #69121, .T. ) ;
#7557=EDGE_CURVE ( 'NONE', #1034, #61310, #3224, .T. ) ;
#7563=CARTESIAN_POINT ( 'NONE',  ( 7.399999999999989697, 11.99999999999999289, -4.000000000000000000 ) ) ;
#7601=DIRECTION ( 'NONE',  ( -1.000000000000000000, -7.709882115452468306E-16, 0.000000000000000000 ) ) ;
#7605=DIRECTION ( 'NONE',  ( -1.000000000000000000, 0.000000000000000000, 0.000000000000000000 ) ) ;
#7624=FACE_OUTER_BOUND ( 'NONE', #49803, .T. ) ;
#7635=EDGE_CURVE ( 'NONE', #5374, #24854, #5255, .T. ) ;
#7657=CYLINDRICAL_SURFACE ( 'NONE', #5829, 0.2499999999999997780 ) ;
#7659=VERTEX_POINT ( 'NONE', #26375 ) ;
#7673=DIRECTION ( 'NONE',  ( -1.000000000000000000, -1.224646799147353207E-16, -0.000000000000000000 ) ) ;
#7698=DIRECTION ( 'NONE',  ( -1.000000000000000000, 0.000000000000000000, 0.000000000000000000 ) ) ;
#7701=ORIENTED_EDGE ( 'NONE', *, *, #15758, .T. ) ;
#7710=DIRECTION ( 'NONE',  ( 1.000000000000000000, 2.312964634635740689E-15, -0.000000000000000000 ) ) ;
#7722=CARTESIAN_POINT ( 'NONE',  ( 26.00000000000001066, 21.99999999999998224, 4.000000000000000000 ) ) ;
#7735=FACE_OUTER_BOUND ( 'NONE', #17708, .T. ) ;
#7736=CIRCLE ( 'NONE', #47100, 0.2500000000000002220 ) ;
#7743=ORIENTED_EDGE ( 'NONE', *, *, #64819, .F. ) ;
#7747=DIRECTION ( 'NONE',  ( -0.000000000000000000, -0.000000000000000000, 1.000000000000000000 ) ) ;
#7767=DIRECTION ( 'NONE',  ( 0.000000000000000000, 0.000000000000000000, 1.000000000000000000 ) ) ;
#7769=ORIENTED_EDGE ( 'NONE', *, *, #16469, .T. ) ;
#7782=EDGE_CURVE ( 'NONE', #38988, #1652, #54422, .T. ) ;
#7794=DIRECTION ( 'NONE',  ( 0.000000000000000000, 0.000000000000000000, 1.000000000000000000 ) ) ;
#7815=AXIS2_PLACEMENT_3D ( 'NONE', #27862, #69102, #16352 ) ;
#7820=DIRECTION ( 'NONE',  ( -0.000000000000000000, 0.000000000000000000, -1.000000000000000000 ) ) ;
#7821=DIRECTION ( 'NONE',  ( -1.000000000000000000, 0.000000000000000000, 0.000000000000000000 ) ) ;
#7851=DIRECTION ( 'NONE',  ( 0.000000000000000000, -1.000000000000000000, 0.000000000000000000 ) ) ;
#7852=ORIENTED_EDGE ( 'NONE', *, *, #5956, .T. ) ;
#7895=TOROIDAL_SURFACE ( 'NONE', #43894, 0.5000000000000000000, 0.2500000000000000000 ) ;
#7897=CARTESIAN_POINT ( 'NONE',  ( 48.25000000000000000, 22.24999999999998579, -3.750000000000000000 ) ) ;
#7902=PRODUCT_DEFINITION_CONTEXT ( 'detailed design', #63519, 'design' ) ;
#7915=DIRECTION ( 'NONE',  ( 0.000000000000000000, -0.000000000000000000, 1.000000000000000000 ) ) ;
#7925=CARTESIAN_POINT ( 'NONE',  ( 30.75000000000001066, 16.24999999999997513, 3.750000000000000000 ) ) ;
#7926=VERTEX_POINT ( 'NONE', #35476 ) ;
#7935=ORIENTED_EDGE ( 'NONE', *, *, #45166, .T. ) ;
#7944=( GEOMETRIC_REPRESENTATION_CONTEXT ( 3 ) GLOBAL_UNCERTAINTY_ASSIGNED_CONTEXT ( ( #24161 ) ) GLOBAL_UNIT_ASSIGNED_CONTEXT ( ( #18113, #45584, #9301 ) ) REPRESENTATION_CONTEXT ( 'NONE', 'WORKASPACE' ) );
#7947=VERTEX_POINT ( 'NONE', #32260 ) ;
#7948=EDGE_CURVE ( 'NONE', #5853, #51660, #32969, .T. ) ;
#7990=CARTESIAN_POINT ( 'NONE',  ( 69.99999999999998579, 36.75000000000000000, -3.000000000000000000 ) ) ;
#8000=CARTESIAN_POINT ( 'NONE',  ( 7.750000000000000000, 33.74999999999998579, -3.750000000000000000 ) ) ;
#8033=ORIENTED_EDGE ( 'NONE', *, *, #61104, .F. ) ;
#8043=CARTESIAN_POINT ( 'NONE',  ( 39.24999999999999289, 16.24999999999997513, 4.000000000000000000 ) ) ;
#8044=ADVANCED_FACE ( 'NONE', ( #40274 ), #23728, .F. ) ;
#8085=VECTOR ( 'NONE', #26950, 1000.000000000000000 ) ;
#8092=CARTESIAN_POINT ( 'NONE',  ( 0.000000000000000000, 36.75000000000000000, 4.000000000000000000 ) ) ;
#8095=DIRECTION ( 'NONE',  ( -0.000000000000000000, 0.000000000000000000, -1.000000000000000000 ) ) ;
#8135=LINE ( 'NONE', #51048, #52472 ) ;
#8144=EDGE_CURVE ( 'NONE', #2770, #3825, #11799, .T. ) ;
#8146=DIRECTION ( 'NONE',  ( 0.000000000000000000, 0.000000000000000000, -1.000000000000000000 ) ) ;
#8147=LINE ( 'NONE', #34182, #29854 ) ;
#8197=VERTEX_POINT ( 'NONE', #12621 ) ;
#8216=AXIS2_PLACEMENT_3D ( 'NONE', #45028, #18253, #8405 ) ;
#8234=CARTESIAN_POINT ( 'NONE',  ( 30.75000000000001066, 15.74999999999997513, -4.000000000000000000 ) ) ;
#8255=CARTESIAN_POINT ( 'NONE',  ( 62.10000000000000142, 11.99999999999999822, 3.499999999999992895 ) ) ;
#8256=EDGE_LOOP ( 'NONE', ( #36198, #24335, #18800, #18838 ) ) ;
#8273=AXIS2_PLACEMENT_3D ( 'NONE', #24042, #7851, #14193 ) ;
#8274=AXIS2_PLACEMENT_3D ( 'NONE', #29651, #50083, #34921 ) ;
#8283=CARTESIAN_POINT ( 'NONE',  ( 69.99999999999998579, 1.000000000000008660, -3.000000000000000000 ) ) ;
#8298=CARTESIAN_POINT ( 'NONE',  ( 43.75000000000000000, 19.24999999999998224, 4.000000000000000000 ) ) ;
#8302=PRESENTATION_STYLE_ASSIGNMENT (( #46305 ) ) ;
#8315=ORIENTED_EDGE ( 'NONE', *, *, #58464, .F. ) ;
#8336=ORIENTED_EDGE ( 'NONE', *, *, #26539, .T. ) ;
#8362=FACE_OUTER_BOUND ( 'NONE', #42527, .T. ) ;
#8364=EDGE_LOOP ( 'NONE', ( #35451, #25054, #29546, #42946 ) ) ;
#8376=DIRECTION ( 'NONE',  ( 0.000000000000000000, 0.000000000000000000, -1.000000000000000000 ) ) ;
#8402=EDGE_LOOP ( 'NONE', ( #17058, #65125, #67459, #40947 ) ) ;
#8403=CIRCLE ( 'NONE', #44347, 0.2500000000000002220 ) ;
#8405=DIRECTION ( 'NONE',  ( 0.000000000000000000, -0.000000000000000000, -1.000000000000000000 ) ) ;
#8419=AXIS2_PLACEMENT_3D ( 'NONE', #56979, #8793, #63975 ) ;
#8427=CARTESIAN_POINT ( 'NONE',  ( 25.75000000000001066, 19.24999999999997868, -4.000000000000000000 ) ) ;
#8433=AXIS2_PLACEMENT_3D ( 'NONE', #27539, #26163, #26511 ) ;
#8439=ADVANCED_FACE ( 'NONE', ( #22768 ), #42887, .T. ) ;
#8444=FILL_AREA_STYLE_COLOUR ( '', #24755 ) ;
#8445=ORIENTED_EDGE ( 'NONE', *, *, #24228, .T. ) ;
#8449=LINE ( 'NONE', #29884, #57277 ) ;
#8450=ADVANCED_FACE ( 'NONE', ( #44613 ), #51234, .T. ) ;
#8453=ORIENTED_EDGE ( 'NONE', *, *, #57178, .F. ) ;
#8455=CARTESIAN_POINT ( 'NONE',  ( -2.139492287038055877E-14, 27.74999999999994316, 3.750000000000000000 ) ) ;
#8475=DIRECTION ( 'NONE',  ( 0.000000000000000000, -0.000000000000000000, 1.000000000000000000 ) ) ;
#8484=CARTESIAN_POINT ( 'NONE',  ( 21.75000000000001066, 21.74999999999998224, 4.000000000000000000 ) ) ;
#8488=CIRCLE ( 'NONE', #33179, 0.5000000000000004441 ) ;
#8493=CARTESIAN_POINT ( 'NONE',  ( 21.25000000000001066, 24.74999999999998224, -3.750000000000000000 ) ) ;
#8515=EDGE_CURVE ( 'NONE', #60522, #40281, #15262, .T. ) ;
#8520=CIRCLE ( 'NONE', #68028, 0.7499999999999997780 ) ;
#8541=FACE_OUTER_BOUND ( 'NONE', #6819, .T. ) ;
#8553=PLANE ( 'NONE',  #13959 ) ;
#8581=DIRECTION ( 'NONE',  ( 2.312964634635740689E-15, -1.000000000000000000, 0.000000000000000000 ) ) ;
#8621=DIRECTION ( 'NONE',  ( -1.000000000000000000, 0.000000000000000000, 0.000000000000000000 ) ) ;
#8652=ORIENTED_EDGE ( 'NONE', *, *, #17662, .T. ) ;
#8669=CARTESIAN_POINT ( 'NONE',  ( 68.99999999999998579, 1.000000000000008438, 4.000000000000000000 ) ) ;
#8670=CARTESIAN_POINT ( 'NONE',  ( 44.00000000000000000, 21.99999999999998579, 4.000000000000000000 ) ) ;
#8684=EDGE_CURVE ( 'NONE', #57903, #37864, #6268, .T. ) ;
#8700=ORIENTED_EDGE ( 'NONE', *, *, #5104, .T. ) ;
#8725=ORIENTED_EDGE ( 'NONE', *, *, #67837, .F. ) ;
#8744=CIRCLE ( 'NONE', #69450, 0.2500000000000002220 ) ;
#8749=EDGE_CURVE ( 'NONE', #67943, #51712, #17549, .T. ) ;
#8756=DIRECTION ( 'NONE',  ( 0.000000000000000000, 0.000000000000000000, 1.000000000000000000 ) ) ;
#8793=DIRECTION ( 'NONE',  ( -0.000000000000000000, 0.000000000000000000, -1.000000000000000000 ) ) ;
#8818=CARTESIAN_POINT ( 'NONE',  ( 30.75000000000001066, 16.24999999999997513, 4.000000000000000000 ) ) ;
#8828=DIRECTION ( 'NONE',  ( 0.000000000000000000, 0.000000000000000000, 1.000000000000000000 ) ) ;
#8832=EDGE_LOOP ( 'NONE', ( #61920, #6710, #31880, #24021 ) ) ;
#8844=ORIENTED_EDGE ( 'NONE', *, *, #21544, .F. ) ;
#8845=EDGE_CURVE ( 'NONE', #21355, #38142, #55742, .T. ) ;
#8851=AXIS2_PLACEMENT_3D ( 'NONE', #65235, #65584, #29690 ) ;
#8868=EDGE_CURVE ( 'NONE', #10730, #47241, #66490, .T. ) ;
#8870=CARTESIAN_POINT ( 'NONE',  ( 48.49999999999999289, 24.99999999999998579, 4.000000000000000000 ) ) ;
#8899=TOROIDAL_SURFACE ( 'NONE', #17884, 0.5000000000000000000, 0.2500000000000000000 ) ;
#8946=SURFACE_STYLE_USAGE ( .BOTH. , #30040 ) ;
#8961=LINE ( 'NONE', #13887, #59473 ) ;
#8984=AXIS2_PLACEMENT_3D ( 'NONE', #5640, #17297, #33434 ) ;
#8993=ORIENTED_EDGE ( 'NONE', *, *, #67361, .F. ) ;
#9010=CARTESIAN_POINT ( 'NONE',  ( 8.000000000000000000, 33.99999999999998579, 3.750000000000000000 ) ) ;
#9016=CARTESIAN_POINT ( 'NONE',  ( 48.25000000000000000, 21.74999999999998579, -4.000000000000000000 ) ) ;
#9039=CARTESIAN_POINT ( 'NONE',  ( 68.99999999999998579, 8.450062914116736267E-15, -3.000000000000000000 ) ) ;
#9043=CARTESIAN_POINT ( 'NONE',  ( 8.000000000000000000, 33.74999999999998579, 4.000000000000000000 ) ) ;
#9051=DIRECTION ( 'NONE',  ( -2.312964634635740689E-15, 1.000000000000000000, -0.000000000000000000 ) ) ;
#9055=CIRCLE ( 'NONE', #61788, 1.000000000000000000 ) ;
#9100=ORIENTED_EDGE ( 'NONE', *, *, #37357, .F. ) ;
#9109=CONICAL_SURFACE ( 'NONE', #64124, 3.100000000000005418, 0.7853981633974445042 ) ;
#9114=AXIS2_PLACEMENT_3D ( 'NONE', #67781, #51957, #45669 ) ;
#9128=DIRECTION ( 'NONE',  ( 0.000000000000000000, 0.000000000000000000, -1.000000000000000000 ) ) ;
#9129=PRESENTATION_STYLE_ASSIGNMENT (( #20356 ) ) ;
#9143=ORIENTED_EDGE ( 'NONE', *, *, #40417, .T. ) ;
#9147=ADVANCED_FACE ( 'NONE', ( #61699 ), #25796, .T. ) ;
#9148=CARTESIAN_POINT ( 'NONE',  ( 21.50000000000001066, 24.74999999999998224, 4.000000000000000000 ) ) ;
#9158=EDGE_CURVE ( 'NONE', #26382, #12261, #26872, .T. ) ;
#9161=LINE ( 'NONE', #51717, #29846 ) ;
#9162=EDGE_LOOP ( 'NONE', ( #13971, #46859, #49685 ) ) ;
#9172=CARTESIAN_POINT ( 'NONE',  ( 25.75000000000001066, 19.24999999999997868, -4.000000000000000000 ) ) ;
#9196=CIRCLE ( 'NONE', #46271, 0.2500000000000002220 ) ;
#9225=ORIENTED_EDGE ( 'NONE', *, *, #8845, .F. ) ;
#9231=PLANE ( 'NONE',  #28115 ) ;
#9246=EDGE_CURVE ( 'NONE', #68919, #10058, #24096, .T. ) ;
#9259=FACE_OUTER_BOUND ( 'NONE', #26650, .T. ) ;
#9283=PLANE ( 'NONE',  #56106 ) ;
#9299=CARTESIAN_POINT ( 'NONE',  ( 62.24999999999998579, 33.74999999999999289, 4.000000000000000000 ) ) ;
#9301=( NAMED_UNIT ( * ) SI_UNIT ( $, .STERADIAN. ) SOLID_ANGLE_UNIT ( ) );
#9322=DIRECTION ( 'NONE',  ( 0.000000000000000000, 0.000000000000000000, 1.000000000000000000 ) ) ;
#9336=DIRECTION ( 'NONE',  ( -1.000000000000000000, 0.000000000000000000, 0.000000000000000000 ) ) ;
#9339=VECTOR ( 'NONE', #69288, 1000.000000000000000 ) ;
#9340=EDGE_LOOP ( 'NONE', ( #28613, #41434, #21065, #15070 ) ) ;
#9345=DIRECTION ( 'NONE',  ( 0.000000000000000000, 0.000000000000000000, 1.000000000000000000 ) ) ;
#9367=DIRECTION ( 'NONE',  ( 0.000000000000000000, 1.000000000000000000, 0.000000000000000000 ) ) ;
#9409=ORIENTED_EDGE ( 'NONE', *, *, #35742, .T. ) ;
#9427=VERTEX_POINT ( 'NONE', #10696 ) ;
#9444=ADVANCED_FACE ( 'NONE', ( #53934 ), #53601, .T. ) ;
#9448=CARTESIAN_POINT ( 'NONE',  ( 21.25000000000001066, 24.99999999999998579, -3.750000000000000000 ) ) ;
#9462=DIRECTION ( 'NONE',  ( -1.000000000000000000, 0.000000000000000000, 0.000000000000000000 ) ) ;
#9480=CIRCLE ( 'NONE', #17371, 0.2500000000000002220 ) ;
#9487=ORIENTED_EDGE ( 'NONE', *, *, #52980, .T. ) ;
#9533=CARTESIAN_POINT ( 'NONE',  ( 66.24999999999998579, 34.24999999999999289, -4.000000000000000000 ) ) ;
#9550=ORIENTED_EDGE ( 'NONE', *, *, #12210, .F. ) ;
#9559=AXIS2_PLACEMENT_3D ( 'NONE', #11017, #63461, #15311 ) ;
#9565=CIRCLE ( 'NONE', #45532, 0.2500000000000002220 ) ;
#9615=( LENGTH_UNIT ( ) NAMED_UNIT ( * ) SI_UNIT ( .MILLI., .METRE. ) );
#9670=ORIENTED_EDGE ( 'NONE', *, *, #31348, .F. ) ;
#9684=ORIENTED_EDGE ( 'NONE', *, *, #22959, .T. ) ;
#9691=ORIENTED_EDGE ( 'NONE', *, *, #37719, .F. ) ;
#9695=ORIENTED_EDGE ( 'NONE', *, *, #68419, .T. ) ;
#9702=VERTEX_POINT ( 'NONE', #67623 ) ;
#9753=CARTESIAN_POINT ( 'NONE',  ( 8.000000000000001776, 31.24999999999998579, -4.000000000000000000 ) ) ;
#9762=CARTESIAN_POINT ( 'NONE',  ( 62.24999999999998579, 33.74999999999999289, 3.750000000000000000 ) ) ;
#9768=DIRECTION ( 'NONE',  ( 1.445602896647337931E-16, -1.000000000000000000, -0.000000000000000000 ) ) ;
#9796=CARTESIAN_POINT ( 'NONE',  ( 10.99999999999999645, 11.99999999999999289, 4.000000000000000000 ) ) ;
#9812=EDGE_CURVE ( 'NONE', #14179, #13223, #52850, .T. ) ;
#9829=FACE_OUTER_BOUND ( 'NONE', #59119, .T. ) ;
#9831=CIRCLE ( 'NONE', #49152, 0.2500000000000002220 ) ;
#9844=ORIENTED_EDGE ( 'NONE', *, *, #36154, .F. ) ;
#9859=CARTESIAN_POINT ( 'NONE',  ( 30.25000000000000711, 18.74999999999997868, -4.000000000000000000 ) ) ;
#9878=ORIENTED_EDGE ( 'NONE', *, *, #57912, .T. ) ;
#9890=CARTESIAN_POINT ( 'NONE',  ( 53.00000000000000000, 24.99999999999998579, 4.000000000000000000 ) ) ;
#9893=EDGE_LOOP ( 'NONE', ( #21773, #5562, #21619, #15783 ) ) ;
#9901=FACE_OUTER_BOUND ( 'NONE', #22838, .T. ) ;
#9903=LINE ( 'NONE', #20797, #44073 ) ;
#9908=DIRECTION ( 'NONE',  ( -1.000000000000000000, 0.000000000000000000, 0.000000000000000000 ) ) ;
#9919=CARTESIAN_POINT ( 'NONE',  ( 8.250000000000001776, 30.74999999999998579, 3.750000000000000000 ) ) ;
#9969=VERTEX_POINT ( 'NONE', #65461 ) ;
#9978=CARTESIAN_POINT ( 'NONE',  ( 30.25000000000000711, 18.74999999999997868, 3.750000000000000000 ) ) ;
#9980=AXIS2_PLACEMENT_3D ( 'NONE', #17602, #55550, #7698 ) ;
#9990=AXIS2_PLACEMENT_3D ( 'NONE', #56422, #51167, #2912 ) ;
#10011=PRESENTATION_STYLE_ASSIGNMENT (( #42753 ) ) ;
#10019=CYLINDRICAL_SURFACE ( 'NONE', #57390, 0.2500000000000002220 ) ;
#10034=( LENGTH_UNIT ( ) NAMED_UNIT ( * ) SI_UNIT ( .MILLI., .METRE. ) );
#10058=VERTEX_POINT ( 'NONE', #61537 ) ;
#10066=CIRCLE ( 'NONE', #34727, 0.2500000000000002220 ) ;
#10071=DIRECTION ( 'NONE',  ( -1.000000000000000000, 0.000000000000000000, 0.000000000000000000 ) ) ;
#10087=EDGE_CURVE ( 'NONE', #24854, #7947, #18321, .T. ) ;
#10089=CARTESIAN_POINT ( 'NONE',  ( 26.25000000000001066, 18.99999999999997868, -3.750000000000000000 ) ) ;
#10090=ORIENTED_EDGE ( 'NONE', *, *, #17209, .F. ) ;
#10095=EDGE_CURVE ( 'NONE', #20493, #59308, #23926, .T. ) ;
#10101=ORIENTED_EDGE ( 'NONE', *, *, #57431, .T. ) ;
#10102=ORIENTED_EDGE ( 'NONE', *, *, #49426, .T. ) ;
#10104=EDGE_CURVE ( 'NONE', #42659, #55156, #64994, .T. ) ;
#10113=DIRECTION ( 'NONE',  ( 0.000000000000000000, 0.000000000000000000, -1.000000000000000000 ) ) ;
#10125=ORIENTED_EDGE ( 'NONE', *, *, #51267, .T. ) ;
#10126=CARTESIAN_POINT ( 'NONE',  ( 25.75000000000001066, 21.74999999999998224, -4.000000000000000000 ) ) ;
#10132=DIRECTION ( 'NONE',  ( -0.000000000000000000, -0.000000000000000000, 1.000000000000000000 ) ) ;
#10133=DIRECTION ( 'NONE',  ( 0.000000000000000000, 0.000000000000000000, -1.000000000000000000 ) ) ;
#10137=DIRECTION ( 'NONE',  ( -0.000000000000000000, 0.000000000000000000, -1.000000000000000000 ) ) ;
#10168=VECTOR ( 'NONE', #48862, 1000.000000000000000 ) ;
#10169=ADVANCED_FACE ( 'NONE', ( #56982 ), #35182, .T. ) ;
#10189=CIRCLE ( 'NONE', #34883, 0.2500000000000002220 ) ;
#10199=DIRECTION ( 'NONE',  ( -1.000000000000000000, 0.000000000000000000, 0.000000000000000000 ) ) ;
#10202=ORIENTED_EDGE ( 'NONE', *, *, #10279, .F. ) ;
#10204=FACE_OUTER_BOUND ( 'NONE', #3501, .T. ) ;
#10230=ORIENTED_EDGE ( 'NONE', *, *, #54926, .T. ) ;
#10232=CYLINDRICAL_SURFACE ( 'NONE', #39408, 3.100000000000000533 ) ;
#10237=ORIENTED_EDGE ( 'NONE', *, *, #36356, .T. ) ;
#10244=DIRECTION ( 'NONE',  ( -0.000000000000000000, 1.000000000000000000, -0.000000000000000000 ) ) ;
#10278=ORIENTED_EDGE ( 'NONE', *, *, #4204, .T. ) ;
#10279=EDGE_CURVE ( 'NONE', #31185, #14977, #67272, .T. ) ;
#10282=CARTESIAN_POINT ( 'NONE',  ( 3.249999999999999112, 34.24999999999998579, -4.000000000000000000 ) ) ;
#10292=EDGE_LOOP ( 'NONE', ( #53621, #42125, #47000 ) ) ;
#10296=( NAMED_UNIT ( * ) SI_UNIT ( $, .STERADIAN. ) SOLID_ANGLE_UNIT ( ) );
#10305=CARTESIAN_POINT ( 'NONE',  ( 39.24999999999999289, 16.24999999999997513, -3.750000000000000000 ) ) ;
#10314=CARTESIAN_POINT ( 'NONE',  ( 3.249999999999998668, 36.99999999999999289, -3.750000000000000000 ) ) ;
#10336=EDGE_CURVE ( 'NONE', #39701, #60504, #597, .T. ) ;
#10341=CARTESIAN_POINT ( 'NONE',  ( 21.75000000000001066, 22.24999999999998224, -4.000000000000000000 ) ) ;
#10342=TOROIDAL_SURFACE ( 'NONE', #61807, 0.5000000000000000000, 0.2500000000000000000 ) ;
#10349=ORIENTED_EDGE ( 'NONE', *, *, #568, .F. ) ;
#10354=CIRCLE ( 'NONE', #5797, 0.2500000000000002220 ) ;
#10377=AXIS2_PLACEMENT_3D ( 'NONE', #48308, #21178, #31734 ) ;
#10388=ORIENTED_EDGE ( 'NONE', *, *, #55881, .T. ) ;
#10406=CARTESIAN_POINT ( 'NONE',  ( 53.24999999999999289, 27.99999999999998579, 3.750000000000000000 ) ) ;
#10420=VECTOR ( 'NONE', #60544, 1000.000000000000000 ) ;
#10427=DIRECTION ( 'NONE',  ( 0.000000000000000000, -0.000000000000000000, 1.000000000000000000 ) ) ;
#10429=VECTOR ( 'NONE', #1319, 1000.000000000000000 ) ;
#10430=AXIS2_PLACEMENT_3D ( 'NONE', #55050, #23071, #17796 ) ;
#10438=CIRCLE ( 'NONE', #49757, 0.2500000000000002220 ) ;
#10448=EDGE_LOOP ( 'NONE', ( #60854, #18106, #12544, #30309 ) ) ;
#10483=ORIENTED_EDGE ( 'NONE', *, *, #20972, .T. ) ;
#10496=ORIENTED_EDGE ( 'NONE', *, *, #65603, .F. ) ;
#10497=AXIS2_PLACEMENT_3D ( 'NONE', #16204, #5250, #69626 ) ;
#10505=ADVANCED_FACE ( 'NONE', ( #44245 ), #16797, .T. ) ;
#10508=EDGE_CURVE ( 'NONE', #19236, #823, #65648, .T. ) ;
#10511=EDGE_CURVE ( 'NONE', #51968, #35469, #37929, .T. ) ;
#10513=VECTOR ( 'NONE', #47115, 1000.000000000000000 ) ;
#10526=ORIENTED_EDGE ( 'NONE', *, *, #62572, .F. ) ;
#10538=CARTESIAN_POINT ( 'NONE',  ( 21.25000000000001066, 24.99999999999998579, 4.000000000000000000 ) ) ;
#10554=FACE_OUTER_BOUND ( 'NONE', #55788, .T. ) ;
#10555=ORIENTED_EDGE ( 'NONE', *, *, #22876, .F. ) ;
#10571=DIRECTION ( 'NONE',  ( 0.000000000000000000, -0.000000000000000000, 1.000000000000000000 ) ) ;
#10577=FACE_OUTER_BOUND ( 'NONE', #49099, .T. ) ;
#10593=DIRECTION ( 'NONE',  ( 0.000000000000000000, 0.000000000000000000, -1.000000000000000000 ) ) ;
#10608=DIRECTION ( 'NONE',  ( 0.000000000000000000, 0.000000000000000000, -1.000000000000000000 ) ) ;
#10635=AXIS2_PLACEMENT_3D ( 'NONE', #8455, #67525, #3453 ) ;
#10640=CIRCLE ( 'NONE', #29709, 0.2500000000000002220 ) ;
#10644=DIRECTION ( 'NONE',  ( -1.000000000000000000, 0.000000000000000000, 0.000000000000000000 ) ) ;
#10670=AXIS2_PLACEMENT_3D ( 'NONE', #43464, #27185, #49376 ) ;
#10696=CARTESIAN_POINT ( 'NONE',  ( 12.25000000000000355, 30.74999999999998579, 4.000000000000000000 ) ) ;
#10706=EDGE_LOOP ( 'NONE', ( #67577, #7101, #48727, #13233 ) ) ;
#10714=ORIENTED_EDGE ( 'NONE', *, *, #16715, .T. ) ;
#10730=VERTEX_POINT ( 'NONE', #63149 ) ;
#10731=EDGE_CURVE ( 'NONE', #66069, #59058, #40373, .T. ) ;
#10753=CARTESIAN_POINT ( 'NONE',  ( 1.000000000000000000, 0.000000000000000000, 3.000000000000000000 ) ) ;
#10788=ORIENTED_EDGE ( 'NONE', *, *, #23196, .T. ) ;
#10794=DIRECTION ( 'NONE',  ( 0.000000000000000000, 0.000000000000000000, -1.000000000000000000 ) ) ;
#10832=VECTOR ( 'NONE', #3956, 1000.000000000000000 ) ;
#10834=VERTEX_POINT ( 'NONE', #31463 ) ;
#10847=CARTESIAN_POINT ( 'NONE',  ( 48.50000000000000000, 22.24999999999998579, 3.750000000000000000 ) ) ;
#10867=ORIENTED_EDGE ( 'NONE', *, *, #33921, .F. ) ;
#10878=CARTESIAN_POINT ( 'NONE',  ( 61.74999999999998579, 30.74999999999999289, 4.000000000000000000 ) ) ;
#10888=DIRECTION ( 'NONE',  ( 0.000000000000000000, 1.000000000000000000, 0.000000000000000000 ) ) ;
#10889=CARTESIAN_POINT ( 'NONE',  ( -1.224646799147353207E-16, 1.000000000000000000, 3.000000000000000000 ) ) ;
#10910=ADVANCED_FACE ( 'NONE', ( #39444 ), #53844, .F. ) ;
#10913=EDGE_LOOP ( 'NONE', ( #68514, #53354, #47068, #36354 ) ) ;
#10919=CARTESIAN_POINT ( 'NONE',  ( 1.000000000000000000, 1.000000000000000222, -3.000000000000000000 ) ) ;
#10959=EDGE_LOOP ( 'NONE', ( #50162, #9684, #35282, #35946 ) ) ;
#10974=ADVANCED_FACE ( 'NONE', ( #11635 ), #1008, .T. ) ;
#10981=EDGE_CURVE ( 'NONE', #67106, #3926, #14605, .T. ) ;
#10982=EDGE_LOOP ( 'NONE', ( #48835, #37610, #52512, #14906 ) ) ;
#10983=DIRECTION ( 'NONE',  ( 0.000000000000000000, 0.000000000000000000, -1.000000000000000000 ) ) ;
#10997=DIRECTION ( 'NONE',  ( -0.000000000000000000, 0.000000000000000000, -1.000000000000000000 ) ) ;
#11017=CARTESIAN_POINT ( 'NONE',  ( 30.25000000000002842, 3.498359009886561184E-14, 3.750000000000000000 ) ) ;
#11023=EDGE_CURVE ( 'NONE', #25558, #29227, #666, .T. ) ;
#11041=CARTESIAN_POINT ( 'NONE',  ( 68.99999999999998579, 0.000000000000000000, 4.000000000000000000 ) ) ;
#11050=EDGE_CURVE ( 'NONE', #47241, #19502, #22540, .T. ) ;
#11052=DIRECTION ( 'NONE',  ( 2.312964634635740689E-15, -1.000000000000000000, 0.000000000000000000 ) ) ;
#11067=ORIENTED_EDGE ( 'NONE', *, *, #68710, .T. ) ;
#11070=CIRCLE ( 'NONE', #40320, 0.2500000000000002220 ) ;
#11082=CARTESIAN_POINT ( 'NONE',  ( 26.25000000000001066, 19.24999999999997868, 4.000000000000000000 ) ) ;
#11086=EDGE_CURVE ( 'NONE', #17986, #42973, #55051, .T. ) ;
#11103=ORIENTED_EDGE ( 'NONE', *, *, #35177, .F. ) ;
#11112=EDGE_CURVE ( 'NONE', #69269, #37989, #14661, .T. ) ;
#11120=CARTESIAN_POINT ( 'NONE',  ( 43.75000000000000000, 19.24999999999998224, 4.000000000000000000 ) ) ;
#11122=EDGE_CURVE ( 'NONE', #64166, #68610, #59094, .T. ) ;
#11159=DIRECTION ( 'NONE',  ( -0.000000000000000000, -1.000000000000000000, -0.000000000000000000 ) ) ;
#11180=CIRCLE ( 'NONE', #50510, 0.2500000000000002220 ) ;
#11185=VERTEX_POINT ( 'NONE', #30974 ) ;
#11198=ORIENTED_EDGE ( 'NONE', *, *, #1464, .F. ) ;
#11247=DIRECTION ( 'NONE',  ( -1.000000000000000000, 0.000000000000000000, 0.000000000000000000 ) ) ;
#11250=FACE_OUTER_BOUND ( 'NONE', #66139, .T. ) ;
#11251=CARTESIAN_POINT ( 'NONE',  ( 10.99999999999999645, 11.99999999999999289, 4.000000000000000000 ) ) ;
#11255=CIRCLE ( 'NONE', #45041, 0.2500000000000002220 ) ;
#11256=DIRECTION ( 'NONE',  ( -1.000000000000000000, 0.000000000000000000, 0.000000000000000000 ) ) ;
#11261=PLANE ( 'NONE',  #24103 ) ;
#11265=ADVANCED_FACE ( 'NONE', ( #11250 ), #65762, .T. ) ;
#11282=ORIENTED_EDGE ( 'NONE', *, *, #66005, .T. ) ;
#11316=CARTESIAN_POINT ( 'NONE',  ( 8.000000000000001776, 30.99999999999998579, 4.000000000000000000 ) ) ;
#11368=VECTOR ( 'NONE', #16781, 1000.000000000000000 ) ;
#11381=DIRECTION ( 'NONE',  ( 0.000000000000000000, 0.000000000000000000, -1.000000000000000000 ) ) ;
#11406=CARTESIAN_POINT ( 'NONE',  ( 0.2500000000000000000, 36.99999999999999289, 4.000000000000000000 ) ) ;
#11407=DIRECTION ( 'NONE',  ( 0.000000000000000000, 1.000000000000000000, 0.000000000000000000 ) ) ;
#11452=CIRCLE ( 'NONE', #66547, 0.2500000000000002220 ) ;
#11454=FACE_OUTER_BOUND ( 'NONE', #26589, .T. ) ;
#11456=STYLED_ITEM ( 'NONE', ( #57155 ), #24240 ) ;
#11461=VERTEX_POINT ( 'NONE', #57633 ) ;
#11464=AXIS2_PLACEMENT_3D ( 'NONE', #7391, #60479, #65436 ) ;
#11471=FACE_OUTER_BOUND ( 'NONE', #22310, .T. ) ;
#11473=VERTEX_POINT ( 'NONE', #20694 ) ;
#11505=EDGE_CURVE ( 'NONE', #6607, #20333, #9196, .T. ) ;
#11510=LINE ( 'NONE', #200, #29630 ) ;
#11517=EDGE_CURVE ( 'NONE', #67683, #68764, #32774, .T. ) ;
#11554=CYLINDRICAL_SURFACE ( 'NONE', #2889, 0.2500000000000002220 ) ;
#11555=ORIENTED_EDGE ( 'NONE', *, *, #30195, .F. ) ;
#11587=CIRCLE ( 'NONE', #59890, 0.2500000000000002220 ) ;
#11599=EDGE_CURVE ( 'NONE', #50938, #62878, #17030, .T. ) ;
#11605=VECTOR ( 'NONE', #44007, 1000.000000000000000 ) ;
#11611=DIRECTION ( 'NONE',  ( 1.000000000000000000, 0.000000000000000000, 0.000000000000000000 ) ) ;
#11625=ORIENTED_EDGE ( 'NONE', *, *, #17291, .T. ) ;
#11632=ORIENTED_EDGE ( 'NONE', *, *, #2824, .T. ) ;
#11635=FACE_OUTER_BOUND ( 'NONE', #54201, .T. ) ;
#11640=CYLINDRICAL_SURFACE ( 'NONE', #30803, 0.2500000000000002220 ) ;
#11644=AXIS2_PLACEMENT_3D ( 'NONE', #51964, #41782, #57216 ) ;
#11647=VERTEX_POINT ( 'NONE', #13491 ) ;
#11665=DIRECTION ( 'NONE',  ( 0.000000000000000000, -1.000000000000000000, 0.000000000000000000 ) ) ;
#11669=DIRECTION ( 'NONE',  ( -0.000000000000000000, -0.000000000000000000, 1.000000000000000000 ) ) ;
#11686=VECTOR ( 'NONE', #52959, 1000.000000000000000 ) ;
#11704=DIRECTION ( 'NONE',  ( -0.000000000000000000, 1.000000000000000000, -0.000000000000000000 ) ) ;
#11706=VECTOR ( 'NONE', #62008, 1000.000000000000000 ) ;
#11720=CARTESIAN_POINT ( 'NONE',  ( 17.00000000000000711, 25.24999999999998224, -3.750000000000000000 ) ) ;
#11721=DIRECTION ( 'NONE',  ( 1.000000000000000000, 1.224646799147353207E-16, 0.000000000000000000 ) ) ;
#11728=ORIENTED_EDGE ( 'NONE', *, *, #17180, .T. ) ;
#11737=UNCERTAINTY_MEASURE_WITH_UNIT (LENGTH_MEASURE( 1.000000000000000082E-05 ), #10034, 'distance_accuracy_value', 'NONE');
#11774=CARTESIAN_POINT ( 'NONE',  ( 7.750000000000000000, 33.99999999999998579, -3.750000000000000000 ) ) ;
#11779=EDGE_CURVE ( 'NONE', #22240, #6197, #20522, .T. ) ;
#11796=PRODUCT_CONTEXT ( 'NONE', #28885, 'mechanical' ) ;
#11799=CIRCLE ( 'NONE', #31983, 0.5000000000000004441 ) ;
#11803=DIRECTION ( 'NONE',  ( 0.000000000000000000, 0.000000000000000000, 1.000000000000000000 ) ) ;
#11816=ORIENTED_EDGE ( 'NONE', *, *, #18790, .T. ) ;
#11826=EDGE_CURVE ( 'NONE', #60007, #67106, #65195, .T. ) ;
#11828=DIRECTION ( 'NONE',  ( 0.000000000000000000, -0.000000000000000000, 1.000000000000000000 ) ) ;
#11829=AXIS2_PLACEMENT_3D ( 'NONE', #61011, #2574, #23056 ) ;
#11834=DIRECTION ( 'NONE',  ( 0.000000000000000000, 0.000000000000000000, -1.000000000000000000 ) ) ;
#11835=ADVANCED_FACE ( 'NONE', ( #31398 ), #10342, .T. ) ;
#11868=CARTESIAN_POINT ( 'NONE',  ( 30.50000000000000711, 18.74999999999997868, 3.750000000000000000 ) ) ;
#11872=DIRECTION ( 'NONE',  ( 0.000000000000000000, 0.000000000000000000, -1.000000000000000000 ) ) ;
#11883=DIRECTION ( 'NONE',  ( -1.000000000000000000, 0.000000000000000000, 0.000000000000000000 ) ) ;
#11919=ORIENTED_EDGE ( 'NONE', *, *, #26564, .T. ) ;
#11931=AXIS2_PLACEMENT_3D ( 'NONE', #36386, #47283, #42015 ) ;
#11942=ORIENTED_EDGE ( 'NONE', *, *, #68333, .F. ) ;
#11950=FACE_OUTER_BOUND ( 'NONE', #24876, .T. ) ;
#11969=EDGE_LOOP ( 'NONE', ( #60760, #161, #66521, #28880 ) ) ;
#12002=DIRECTION ( 'NONE',  ( 0.000000000000000000, 0.000000000000000000, 1.000000000000000000 ) ) ;
#12009=DIRECTION ( 'NONE',  ( 0.000000000000000000, -0.000000000000000000, -1.000000000000000000 ) ) ;
#12023=CARTESIAN_POINT ( 'NONE',  ( 7.750000000000001776, 31.24999999999998579, -4.000000000000000000 ) ) ;
#12038=DIRECTION ( 'NONE',  ( 0.000000000000000000, 0.000000000000000000, -1.000000000000000000 ) ) ;
#12049=EDGE_LOOP ( 'NONE', ( #42778, #68262, #36480 ) ) ;
#12101=EDGE_CURVE ( 'NONE', #30410, #27898, #9903, .T. ) ;
#12127=ADVANCED_FACE ( 'NONE', ( #64388 ), #21473, .F. ) ;
#12128=DIRECTION ( 'NONE',  ( 2.312964634635740689E-15, -1.000000000000000000, 0.000000000000000000 ) ) ;
#12150=CARTESIAN_POINT ( 'NONE',  ( 0.000000000000000000, 36.74999999999999289, -3.000000000000000000 ) ) ;
#12154=SPHERICAL_SURFACE ( 'NONE', #29951, 0.2500000000000000000 ) ;
#12162=CARTESIAN_POINT ( 'NONE',  ( 17.00000000000000711, 27.74999999999998224, 4.000000000000000000 ) ) ;
#12174=AXIS2_PLACEMENT_3D ( 'NONE', #14343, #4828, #36556 ) ;
#12177=ORIENTED_EDGE ( 'NONE', *, *, #21684, .F. ) ;
#12186=DIRECTION ( 'NONE',  ( -1.000000000000000000, 0.000000000000000000, 0.000000000000000000 ) ) ;
#12187=CARTESIAN_POINT ( 'NONE',  ( 59.00000000000000000, 11.99999999999999822, 3.499999999999992895 ) ) ;
#12210=EDGE_CURVE ( 'NONE', #5687, #66803, #65250, .T. ) ;
#12215=AXIS2_PLACEMENT_3D ( 'NONE', #3467, #39803, #61218 ) ;
#12261=VERTEX_POINT ( 'NONE', #60470 ) ;
#12271=DIRECTION ( 'NONE',  ( 0.000000000000000000, 0.000000000000000000, -1.000000000000000000 ) ) ;
#12273=ORIENTED_EDGE ( 'NONE', *, *, #20310, .F. ) ;
#12289=LINE ( 'NONE', #28823, #5826 ) ;
#12305=AXIS2_PLACEMENT_3D ( 'NONE', #19399, #14842, #25028 ) ;
#12327=VERTEX_POINT ( 'NONE', #23537 ) ;
#12343=EDGE_LOOP ( 'NONE', ( #35332, #39013, #24784, #16592 ) ) ;
#12366=LINE ( 'NONE', #60908, #62747 ) ;
#12367=DIRECTION ( 'NONE',  ( -0.000000000000000000, 0.000000000000000000, -1.000000000000000000 ) ) ;
#12372=CIRCLE ( 'NONE', #4482, 0.2500000000000002220 ) ;
#12374=CARTESIAN_POINT ( 'NONE',  ( 53.24999999999999289, 27.74999999999998579, 3.750000000000000000 ) ) ;
#12382=EDGE_CURVE ( 'NONE', #17887, #40838, #3071, .T. ) ;
#12390=DIRECTION ( 'NONE',  ( 0.000000000000000000, 0.000000000000000000, -1.000000000000000000 ) ) ;
#12419=ORIENTED_EDGE ( 'NONE', *, *, #24684, .T. ) ;
#12430=FACE_OUTER_BOUND ( 'NONE', #30703, .T. ) ;
#12463=VECTOR ( 'NONE', #7747, 1000.000000000000000 ) ;
#12511=AXIS2_PLACEMENT_3D ( 'NONE', #40972, #3243, #47298 ) ;
#12517=ORIENTED_EDGE ( 'NONE', *, *, #64819, .T. ) ;
#12544=ORIENTED_EDGE ( 'NONE', *, *, #43444, .F. ) ;
#12545=AXIS2_PLACEMENT_3D ( 'NONE', #66794, #1316, #12965 ) ;
#12548=DIRECTION ( 'NONE',  ( 0.000000000000000000, -1.000000000000000000, 0.000000000000000000 ) ) ;
#12550=ADVANCED_FACE ( 'NONE', ( #28011 ), #49522, .F. ) ;
#12564=ORIENTED_EDGE ( 'NONE', *, *, #21267, .F. ) ;
#12575=ORIENTED_EDGE ( 'NONE', *, *, #39837, .F. ) ;
#12578=SPHERICAL_SURFACE ( 'NONE', #27509, 1.000000000000000000 ) ;
#12581=ORIENTED_EDGE ( 'NONE', *, *, #61937, .T. ) ;
#12585=DIRECTION ( 'NONE',  ( -1.000000000000000000, 0.000000000000000000, 0.000000000000000000 ) ) ;
#12601=ORIENTED_EDGE ( 'NONE', *, *, #31995, .T. ) ;
#12614=LINE ( 'NONE', #60452, #10429 ) ;
#12621=CARTESIAN_POINT ( 'NONE',  ( 25.75000000000001066, 21.99999999999998224, 3.750000000000000000 ) ) ;
#12626=AXIS2_PLACEMENT_3D ( 'NONE', #35550, #8475, #50678 ) ;
#12628=AXIS2_PLACEMENT_3D ( 'NONE', #55263, #364, #21894 ) ;
#12639=CARTESIAN_POINT ( 'NONE',  ( 17.25000000000000711, 24.99999999999998224, 4.000000000000000000 ) ) ;
#12658=EDGE_LOOP ( 'NONE', ( #67135, #55323, #24517, #63603 ) ) ;
#12671=ORIENTED_EDGE ( 'NONE', *, *, #36879, .T. ) ;
#12680=ORIENTED_EDGE ( 'NONE', *, *, #25736, .T. ) ;
#12686=DIRECTION ( 'NONE',  ( 0.000000000000000000, 0.000000000000000000, 1.000000000000000000 ) ) ;
#12693=ORIENTED_EDGE ( 'NONE', *, *, #38726, .F. ) ;
#12694=EDGE_CURVE ( 'NONE', #32736, #48045, #55816, .T. ) ;
#12706=EDGE_LOOP ( 'NONE', ( #36528, #36659, #8453, #54685 ) ) ;
#12717=VECTOR ( 'NONE', #65554, 1000.000000000000000 ) ;
#12719=DIRECTION ( 'NONE',  ( 1.000000000000000000, -0.000000000000000000, 0.000000000000000000 ) ) ;
#12721=EDGE_CURVE ( 'NONE', #24442, #47284, #57424, .T. ) ;
#12749=DIRECTION ( 'NONE',  ( 7.709882115452441682E-16, -1.000000000000000000, 0.000000000000000000 ) ) ;
#12803=AXIS2_PLACEMENT_3D ( 'NONE', #61412, #13229, #12186 ) ;
#12837=AXIS2_PLACEMENT_3D ( 'NONE', #57957, #63815, #37141 ) ;
#12855=ORIENTED_EDGE ( 'NONE', *, *, #27212, .T. ) ;
#12858=AXIS2_PLACEMENT_3D ( 'NONE', #52126, #52476, #20793 ) ;
#12865=ORIENTED_EDGE ( 'NONE', *, *, #7233, .F. ) ;
#12868=PLANE ( 'NONE',  #30656 ) ;
#12888=DIRECTION ( 'NONE',  ( 0.000000000000000000, -0.000000000000000000, 1.000000000000000000 ) ) ;
#12914=CARTESIAN_POINT ( 'NONE',  ( 52.75000000000000000, 25.24999999999998579, -3.750000000000000000 ) ) ;
#12921=ORIENTED_EDGE ( 'NONE', *, *, #7782, .F. ) ;
#12935=EDGE_CURVE ( 'NONE', #67106, #59375, #55027, .T. ) ;
#12936=EDGE_LOOP ( 'NONE', ( #7004, #58923, #52180, #46669 ) ) ;
#12940=DIRECTION ( 'NONE',  ( 0.000000000000000000, 0.000000000000000000, 1.000000000000000000 ) ) ;
#12957=CARTESIAN_POINT ( 'NONE',  ( 1.000000000000000888, 1.000000000000000222, -4.000000000000000000 ) ) ;
#12965=DIRECTION ( 'NONE',  ( 0.000000000000000000, 0.000000000000000000, -1.000000000000000000 ) ) ;
#12967=PLANE ( 'NONE',  #8216 ) ;
#12988=DIRECTION ( 'NONE',  ( 0.000000000000000000, 0.000000000000000000, -1.000000000000000000 ) ) ;
#12994=LINE ( 'NONE', #12639, #65166 ) ;
#13012=TOROIDAL_SURFACE ( 'NONE', #23169, 0.5000000000000000000, 0.2500000000000000000 ) ;
#13022=CARTESIAN_POINT ( 'NONE',  ( 16.75000000000000711, 27.74999999999998224, 3.750000000000000000 ) ) ;
#13029=DIRECTION ( 'NONE',  ( -1.000000000000000000, 0.000000000000000000, 0.000000000000000000 ) ) ;
#13043=ORIENTED_EDGE ( 'NONE', *, *, #69649, .T. ) ;
#13127=CARTESIAN_POINT ( 'NONE',  ( 57.49999999999998579, 30.74999999999999289, 3.750000000000000000 ) ) ;
#13135=EDGE_LOOP ( 'NONE', ( #9409, #19790, #8844, #59837 ) ) ;
#13157=CARTESIAN_POINT ( 'NONE',  ( 48.75000000000004974, 1.127570259384924864E-13, 3.750000000000000000 ) ) ;
#13162=CARTESIAN_POINT ( 'NONE',  ( 61.99999999999998579, 30.99999999999999289, 4.000000000000000000 ) ) ;
#13189=CARTESIAN_POINT ( 'NONE',  ( 25.75000000000001066, 21.74999999999998224, -3.750000000000000000 ) ) ;
#13210=CARTESIAN_POINT ( 'NONE',  ( 21.25000000000000711, 22.24999999999998224, 4.000000000000000000 ) ) ;
#13223=VERTEX_POINT ( 'NONE', #9299 ) ;
#13224=CARTESIAN_POINT ( 'NONE',  ( 17.00000000000000711, 27.74999999999998224, -3.750000000000000000 ) ) ;
#13229=DIRECTION ( 'NONE',  ( 0.000000000000000000, 1.000000000000000000, 0.000000000000000000 ) ) ;
#13233=ORIENTED_EDGE ( 'NONE', *, *, #17116, .T. ) ;
#13247=CARTESIAN_POINT ( 'NONE',  ( 17.25000000000000711, 24.99999999999998224, -3.750000000000000000 ) ) ;
#13285=DIRECTION ( 'NONE',  ( -1.000000000000000000, 0.000000000000000000, 0.000000000000000000 ) ) ;
#13290=ORIENTED_EDGE ( 'NONE', *, *, #54481, .F. ) ;
#13306=AXIS2_PLACEMENT_3D ( 'NONE', #42619, #32022, #292 ) ;
#13311=ORIENTED_EDGE ( 'NONE', *, *, #51136, .F. ) ;
#13313=( NAMED_UNIT ( * ) PLANE_ANGLE_UNIT ( ) SI_UNIT ( $, .RADIAN. ) );
#13317=CARTESIAN_POINT ( 'NONE',  ( 39.24999999999999289, 15.74999999999997513, -4.000000000000000000 ) ) ;
#13341=ADVANCED_FACE ( 'NONE', ( #54852 ), #28109, .T. ) ;
#13347=ADVANCED_FACE ( 'NONE', ( #34458 ), #68787, .T. ) ;
#13355=DIRECTION ( 'NONE',  ( -0.000000000000000000, -0.000000000000000000, 1.000000000000000000 ) ) ;
#13357=AXIS2_PLACEMENT_3D ( 'NONE', #16493, #21365, #26298 ) ;
#13366=CARTESIAN_POINT ( 'NONE',  ( 0.000000000000000000, 36.74999999999999289, 4.000000000000000000 ) ) ;
#13369=EDGE_CURVE ( 'NONE', #48755, #10834, #12289, .T. ) ;
#13371=ORIENTED_EDGE ( 'NONE', *, *, #30604, .F. ) ;
#13377=ORIENTED_EDGE ( 'NONE', *, *, #23700, .T. ) ;
#13381=LINE ( 'NONE', #56660, #40776 ) ;
#13383=ORIENTED_EDGE ( 'NONE', *, *, #1274, .F. ) ;
#13390=CARTESIAN_POINT ( 'NONE',  ( 30.25000000000000711, 18.74999999999997868, -3.750000000000000000 ) ) ;
#13393=AXIS2_PLACEMENT_3D ( 'NONE', #18200, #39686, #34709 ) ;
#13413=VECTOR ( 'NONE', #27236, 1000.000000000000000 ) ;
#13432=ORIENTED_EDGE ( 'NONE', *, *, #61433, .F. ) ;
#13480=CARTESIAN_POINT ( 'NONE',  ( 7.750000000000000000, 33.99999999999998579, 3.750000000000000000 ) ) ;
#13491=CARTESIAN_POINT ( 'NONE',  ( 14.59999999999998721, 11.99999999999999289, 4.000000000000000000 ) ) ;
#13501=DIRECTION ( 'NONE',  ( 0.000000000000000000, 0.000000000000000000, -1.000000000000000000 ) ) ;
#13504=CYLINDRICAL_SURFACE ( 'NONE', #25735, 0.2500000000000002220 ) ;
#13528=EDGE_LOOP ( 'NONE', ( #7285, #5313, #68088, #20437 ) ) ;
#13546=SURFACE_STYLE_FILL_AREA ( #61040 ) ;
#13554=ORIENTED_EDGE ( 'NONE', *, *, #48169, .T. ) ;
#13557=CARTESIAN_POINT ( 'NONE',  ( 66.49999999999998579, 33.74999999999999289, -3.750000000000000000 ) ) ;
#13558=ORIENTED_EDGE ( 'NONE', *, *, #68972, .T. ) ;
#13565=AXIS2_PLACEMENT_3D ( 'NONE', #1943, #50908, #1621 ) ;
#13589=EDGE_CURVE ( 'NONE', #21322, #9702, #21054, .T. ) ;
#13633=ORIENTED_EDGE ( 'NONE', *, *, #1057, .F. ) ;
#13649=VERTEX_POINT ( 'NONE', #10847 ) ;
#13668=CARTESIAN_POINT ( 'NONE',  ( 12.50000000000000533, 28.24999999999998224, -4.000000000000000000 ) ) ;
#13675=ADVANCED_FACE ( 'NONE', ( #31950 ), #64303, .T. ) ;
#13712=AXIS2_PLACEMENT_3D ( 'NONE', #54995, #33227, #28245 ) ;
#13716=CARTESIAN_POINT ( 'NONE',  ( 61.99999999999998579, 31.24999999999999289, 4.000000000000000000 ) ) ;
#13719=ORIENTED_EDGE ( 'NONE', *, *, #43920, .T. ) ;
#13725=VERTEX_POINT ( 'NONE', #4871 ) ;
#13734=DIRECTION ( 'NONE',  ( -1.000000000000000000, 0.000000000000000000, 0.000000000000000000 ) ) ;
#13744=VERTEX_POINT ( 'NONE', #61103 ) ;
#13746=ORIENTED_EDGE ( 'NONE', *, *, #67837, .T. ) ;
#13762=EDGE_CURVE ( 'NONE', #51323, #61490, #36107, .T. ) ;
#13776=AXIS2_PLACEMENT_3D ( 'NONE', #10305, #43405, #10644 ) ;
#13777=CARTESIAN_POINT ( 'NONE',  ( 44.00000000000000000, 18.99999999999998224, 3.750000000000000000 ) ) ;
#13785=EDGE_CURVE ( 'NONE', #34416, #46628, #33820, .T. ) ;
#13796=ORIENTED_EDGE ( 'NONE', *, *, #29619, .F. ) ;
#13828=DIRECTION ( 'NONE',  ( -0.000000000000000000, 1.000000000000000000, -0.000000000000000000 ) ) ;
#13838=EDGE_LOOP ( 'NONE', ( #56436, #37906, #44247, #68388 ) ) ;
#13861=DIRECTION ( 'NONE',  ( 0.000000000000000000, 0.000000000000000000, -1.000000000000000000 ) ) ;
#13867=PLANE ( 'NONE',  #16785 ) ;
#13868=CIRCLE ( 'NONE', #47622, 0.2500000000000002220 ) ;
#13887=CARTESIAN_POINT ( 'NONE',  ( 43.75000000000000000, 18.74999999999998224, -4.000000000000000000 ) ) ;
#13890=ORIENTED_EDGE ( 'NONE', *, *, #55881, .F. ) ;
#13891=DIRECTION ( 'NONE',  ( -0.000000000000000000, 0.000000000000000000, -1.000000000000000000 ) ) ;
#13892=CARTESIAN_POINT ( 'NONE',  ( 1.908195823574488119E-14, 24.75000000000002487, 4.000000000000000000 ) ) ;
#13934=ORIENTED_EDGE ( 'NONE', *, *, #11122, .F. ) ;
#13959=AXIS2_PLACEMENT_3D ( 'NONE', #3200, #1811, #44824 ) ;
#13971=ORIENTED_EDGE ( 'NONE', *, *, #17309, .F. ) ;
#14002=ORIENTED_EDGE ( 'NONE', *, *, #8868, .T. ) ;
#14017=DIRECTION ( 'NONE',  ( -0.000000000000000000, -0.000000000000000000, -1.000000000000000000 ) ) ;
#14024=DIRECTION ( 'NONE',  ( 0.000000000000000000, -1.000000000000000000, 0.000000000000000000 ) ) ;
#14031=CARTESIAN_POINT ( 'NONE',  ( 17.25000000000000711, 25.24999999999998224, -3.750000000000000000 ) ) ;
#14037=VERTEX_POINT ( 'NONE', #25535 ) ;
#14053=CARTESIAN_POINT ( 'NONE',  ( 7.750000000000000000, 33.74999999999998579, 3.750000000000000000 ) ) ;
#14054=DIRECTION ( 'NONE',  ( 0.000000000000000000, 0.000000000000000000, 1.000000000000000000 ) ) ;
#14065=ORIENTED_EDGE ( 'NONE', *, *, #10511, .F. ) ;
#14077=CIRCLE ( 'NONE', #43362, 0.2500000000000002220 ) ;
#14080=ORIENTED_EDGE ( 'NONE', *, *, #21828, .T. ) ;
#14086=CIRCLE ( 'NONE', #69124, 0.2500000000000002220 ) ;
#14093=DIRECTION ( 'NONE',  ( 0.000000000000000000, 1.000000000000000000, 0.000000000000000000 ) ) ;
#14104=ORIENTED_EDGE ( 'NONE', *, *, #55026, .T. ) ;
#14148=CIRCLE ( 'NONE', #567, 0.2500000000000002220 ) ;
#14149=DIRECTION ( 'NONE',  ( 0.000000000000000000, 0.000000000000000000, -1.000000000000000000 ) ) ;
#14153=AXIS2_PLACEMENT_3D ( 'NONE', #32660, #48553, #16534 ) ;
#14156=EDGE_CURVE ( 'NONE', #47284, #65666, #43176, .T. ) ;
#14173=ORIENTED_EDGE ( 'NONE', *, *, #47455, .T. ) ;
#14179=VERTEX_POINT ( 'NONE', #14229 ) ;
#14182=AXIS2_PLACEMENT_3D ( 'NONE', #22398, #27302, #65312 ) ;
#14193=DIRECTION ( 'NONE',  ( 0.000000000000000000, 0.000000000000000000, -1.000000000000000000 ) ) ;
#14198=ORIENTED_EDGE ( 'NONE', *, *, #4801, .F. ) ;
#14200=CYLINDRICAL_SURFACE ( 'NONE', #35909, 0.2500000000000002220 ) ;
#14229=CARTESIAN_POINT ( 'NONE',  ( 66.24999999999998579, 33.74999999999999289, 4.000000000000000000 ) ) ;
#14260=DIRECTION ( 'NONE',  ( 1.000000000000000000, 0.000000000000000000, 0.000000000000000000 ) ) ;
#14273=DIRECTION ( 'NONE',  ( -1.000000000000000000, 0.000000000000000000, 0.000000000000000000 ) ) ;
#14307=CARTESIAN_POINT ( 'NONE',  ( 1.000000000000000000, 36.74999999999999289, 4.000000000000000000 ) ) ;
#14324=DIRECTION ( 'NONE',  ( 1.000000000000000000, -0.000000000000000000, 0.000000000000000000 ) ) ;
#14332=LINE ( 'NONE', #51283, #38967 ) ;
#14343=CARTESIAN_POINT ( 'NONE',  ( 1.000000000000000000, 36.74999999999999289, 3.000000000000000000 ) ) ;
#14352=ORIENTED_EDGE ( 'NONE', *, *, #41502, .T. ) ;
#14354=ORIENTED_EDGE ( 'NONE', *, *, #44675, .F. ) ;
#14356=CARTESIAN_POINT ( 'NONE',  ( 52.75000000000000000, 25.24999999999998579, 4.000000000000000000 ) ) ;
#14417=VERTEX_POINT ( 'NONE', #41335 ) ;
#14429=DIRECTION ( 'NONE',  ( 1.000000000000000000, -0.000000000000000000, 0.000000000000000000 ) ) ;
#14431=VERTEX_POINT ( 'NONE', #15307 ) ;
#14450=VECTOR ( 'NONE', #26082, 1000.000000000000000 ) ;
#14455=EDGE_CURVE ( 'NONE', #59005, #22530, #27888, .T. ) ;
#14469=EDGE_CURVE ( 'NONE', #36379, #65996, #36767, .T. ) ;
#14474=AXIS2_PLACEMENT_3D ( 'NONE', #69237, #32604, #5188 ) ;
#14505=CYLINDRICAL_SURFACE ( 'NONE', #2555, 0.2500000000000002220 ) ;
#14510=CYLINDRICAL_SURFACE ( 'NONE', #23222, 0.2500000000000002220 ) ;
#14511=LINE ( 'NONE', #63407, #41039 ) ;
#14520=ORIENTED_EDGE ( 'NONE', *, *, #49330, .T. ) ;
#14531=DIRECTION ( 'NONE',  ( 1.000000000000000000, 0.000000000000000000, 0.000000000000000000 ) ) ;
#14539=VECTOR ( 'NONE', #54256, 1000.000000000000000 ) ;
#14563=EDGE_CURVE ( 'NONE', #23940, #60504, #6559, .T. ) ;
#14571=DIRECTION ( 'NONE',  ( 0.000000000000000000, 0.000000000000000000, 1.000000000000000000 ) ) ;
#14572=DIRECTION ( 'NONE',  ( 7.709882115452468306E-16, -1.000000000000000000, 0.000000000000000000 ) ) ;
#14573=EDGE_LOOP ( 'NONE', ( #3016, #1756, #34818, #3144 ) ) ;
#14585=CARTESIAN_POINT ( 'NONE',  ( 39.24999999999999289, 16.24999999999997513, -3.750000000000000000 ) ) ;
#14601=SPHERICAL_SURFACE ( 'NONE', #60812, 0.2500000000000000000 ) ;
#14605=CIRCLE ( 'NONE', #19042, 0.2500000000000002220 ) ;
#14630=AXIS2_PLACEMENT_3D ( 'NONE', #18281, #17276, #11611 ) ;
#14650=VERTEX_POINT ( 'NONE', #58237 ) ;
#14661=CIRCLE ( 'NONE', #22488, 0.9999999999999997780 ) ;
#14676=AXIS2_PLACEMENT_3D ( 'NONE', #33669, #6939, #64978 ) ;
#14752=ADVANCED_FACE ( 'NONE', ( #19190 ), #52634, .F. ) ;
#14774=DIRECTION ( 'NONE',  ( -1.000000000000000000, 0.000000000000000000, 0.000000000000000000 ) ) ;
#14775=ORIENTED_EDGE ( 'NONE', *, *, #15074, .F. ) ;
#14782=DIRECTION ( 'NONE',  ( -1.000000000000000000, 0.000000000000000000, 0.000000000000000000 ) ) ;
#14795=ORIENTED_EDGE ( 'NONE', *, *, #36154, .T. ) ;
#14833=LINE ( 'NONE', #35934, #60616 ) ;
#14837=CIRCLE ( 'NONE', #17105, 0.2500000000000002220 ) ;
#14841=CARTESIAN_POINT ( 'NONE',  ( 21.25000000000001066, 24.99999999999998579, -3.750000000000000000 ) ) ;
#14842=DIRECTION ( 'NONE',  ( -1.000000000000000000, 1.156482317317870344E-15, 0.000000000000000000 ) ) ;
#14843=VECTOR ( 'NONE', #48928, 1000.000000000000000 ) ;
#14856=CARTESIAN_POINT ( 'NONE',  ( 8.000000000000001776, 30.74999999999998579, -3.750000000000000000 ) ) ;
#14869=ORIENTED_EDGE ( 'NONE', *, *, #15850, .T. ) ;
#14882=CARTESIAN_POINT ( 'NONE',  ( 3.249999999999998668, 36.99999999999999289, 3.750000000000000000 ) ) ;
#14885=EDGE_CURVE ( 'NONE', #6197, #41879, #33240, .T. ) ;
#14891=EDGE_CURVE ( 'NONE', #60007, #3926, #10066, .T. ) ;
#14894=DIRECTION ( 'NONE',  ( -0.000000000000000000, -0.000000000000000000, 1.000000000000000000 ) ) ;
#14906=ORIENTED_EDGE ( 'NONE', *, *, #63838, .T. ) ;
#14944=LINE ( 'NONE', #68749, #20375 ) ;
#14967=LINE ( 'NONE', #64517, #15886 ) ;
#14977=VERTEX_POINT ( 'NONE', #6069 ) ;
#14978=AXIS2_PLACEMENT_3D ( 'NONE', #8493, #57006, #56668 ) ;
#15003=AXIS2_PLACEMENT_3D ( 'NONE', #69650, #38388, #21462 ) ;
#15004=CARTESIAN_POINT ( 'NONE',  ( 12.25000000000000355, 30.74999999999998579, -3.750000000000000000 ) ) ;
#15020=CIRCLE ( 'NONE', #34058, 0.2500000000000002220 ) ;
#15031=CARTESIAN_POINT ( 'NONE',  ( 3.499999999999998668, 36.74999999999999289, -3.750000000000000000 ) ) ;
#15040=LINE ( 'NONE', #9753, #26975 ) ;
#15043=EDGE_CURVE ( 'NONE', #60504, #51066, #63912, .T. ) ;
#15052=EDGE_CURVE ( 'NONE', #36322, #69269, #32810, .T. ) ;
#15056=ADVANCED_FACE ( 'NONE', ( #6752 ), #8899, .T. ) ;
#15060=CARTESIAN_POINT ( 'NONE',  ( 68.99999999999998579, 37.00000000000000000, 3.000000000000000000 ) ) ;
#15067=VECTOR ( 'NONE', #9051, 1000.000000000000000 ) ;
#15068=DIRECTION ( 'NONE',  ( -1.000000000000000000, 0.000000000000000000, 0.000000000000000000 ) ) ;
#15070=ORIENTED_EDGE ( 'NONE', *, *, #37464, .F. ) ;
#15072=LINE ( 'NONE', #52349, #45687 ) ;
#15074=EDGE_CURVE ( 'NONE', #13744, #12261, #59878, .T. ) ;
#15081=ORIENTED_EDGE ( 'NONE', *, *, #65990, .T. ) ;
#15084=CARTESIAN_POINT ( 'NONE',  ( 62.24999999999998579, 33.99999999999999289, 3.750000000000000000 ) ) ;
#15089=PLANE ( 'NONE',  #43203 ) ;
#15096=ORIENTED_EDGE ( 'NONE', *, *, #6486, .F. ) ;
#15097=DIRECTION ( 'NONE',  ( 0.000000000000000000, 0.000000000000000000, -1.000000000000000000 ) ) ;
#15133=CARTESIAN_POINT ( 'NONE',  ( 62.24999999999998579, 33.74999999999999289, 3.750000000000000000 ) ) ;
#15139=DIRECTION ( 'NONE',  ( 0.000000000000000000, -1.000000000000000000, 0.000000000000000000 ) ) ;
#15144=ADVANCED_FACE ( 'NONE', ( #49341 ), #39500, .T. ) ;
#15153=DIRECTION ( 'NONE',  ( 0.000000000000000000, 0.000000000000000000, -1.000000000000000000 ) ) ;
#15157=CARTESIAN_POINT ( 'NONE',  ( 39.49999999999999289, 18.74999999999997868, 3.750000000000000000 ) ) ;
#15161=CARTESIAN_POINT ( 'NONE',  ( 48.25000000000000000, 22.24999999999998579, 4.000000000000000000 ) ) ;
#15175=ORIENTED_EDGE ( 'NONE', *, *, #27124, .T. ) ;
#15190=VERTEX_POINT ( 'NONE', #19392 ) ;
#15191=DIRECTION ( 'NONE',  ( 1.000000000000000000, -7.709882115452468306E-16, 0.000000000000000000 ) ) ;
#15199=DIRECTION ( 'NONE',  ( 0.000000000000000000, 1.000000000000000000, 0.000000000000000000 ) ) ;
#15242=DIRECTION ( 'NONE',  ( 0.000000000000000000, 1.000000000000000000, -0.000000000000000000 ) ) ;
#15262=CIRCLE ( 'NONE', #54528, 1.000000000000000000 ) ;
#15288=CARTESIAN_POINT ( 'NONE',  ( 0.000000000000000000, 33.74999999999998579, 4.000000000000000000 ) ) ;
#15295=EDGE_CURVE ( 'NONE', #27359, #12327, #68289, .T. ) ;
#15302=EDGE_CURVE ( 'NONE', #29672, #14179, #52809, .T. ) ;
#15307=CARTESIAN_POINT ( 'NONE',  ( 3.749999999999999556, 33.74999999999998579, -4.000000000000000000 ) ) ;
#15311=DIRECTION ( 'NONE',  ( -1.000000000000000000, -1.156482317317878627E-15, 0.000000000000000000 ) ) ;
#15333=AXIS2_PLACEMENT_3D ( 'NONE', #22821, #44319, #49554 ) ;
#15343=FACE_OUTER_BOUND ( 'NONE', #41132, .T. ) ;
#15369=EDGE_CURVE ( 'NONE', #37989, #5853, #41945, .T. ) ;
#15371=LINE ( 'NONE', #43156, #13413 ) ;
#15373=EDGE_CURVE ( 'NONE', #51630, #21322, #31680, .T. ) ;
#15378=DIRECTION ( 'NONE',  ( -1.000000000000000000, 0.000000000000000000, 0.000000000000000000 ) ) ;
#15385=EDGE_CURVE ( 'NONE', #31871, #61605, #12994, .T. ) ;
#15389=LINE ( 'NONE', #9043, #56216 ) ;
#15412=ORIENTED_EDGE ( 'NONE', *, *, #39658, .F. ) ;
#15414=ADVANCED_FACE ( 'NONE', ( #44710 ), #970, .T. ) ;
#15419=CARTESIAN_POINT ( 'NONE',  ( 69.99999999999998579, 36.75000000000000000, 3.000000000000000000 ) ) ;
#15430=CYLINDRICAL_SURFACE ( 'NONE', #41817, 0.2500000000000002220 ) ;
#15438=EDGE_CURVE ( 'NONE', #59058, #61310, #57294, .T. ) ;
#15515=CARTESIAN_POINT ( 'NONE',  ( 66.74999999999998579, 36.75000000000000000, 4.000000000000000000 ) ) ;
#15558=ADVANCED_FACE ( 'NONE', ( #2745 ), #51329, .F. ) ;
#15559=CARTESIAN_POINT ( 'NONE',  ( 12.75000000000000533, 27.74999999999998224, -4.000000000000000000 ) ) ;
#15563=VECTOR ( 'NONE', #55299, 1000.000000000000000 ) ;
#15625=EDGE_LOOP ( 'NONE', ( #58553, #59462, #30679, #68358 ) ) ;
#15654=VECTOR ( 'NONE', #1241, 1000.000000000000000 ) ;
#15659=EDGE_CURVE ( 'NONE', #15190, #10730, #11255, .T. ) ;
#15674=ADVANCED_FACE ( 'NONE', ( #16501 ), #49525, .T. ) ;
#15699=CARTESIAN_POINT ( 'NONE',  ( 59.00000000000000000, 11.99999999999999822, -3.499999999999999556 ) ) ;
#15715=CYLINDRICAL_SURFACE ( 'NONE', #20341, 0.2500000000000002220 ) ;
#15735=CARTESIAN_POINT ( 'NONE',  ( 30.50000000000000711, 18.74999999999997868, 4.000000000000000000 ) ) ;
#15758=EDGE_CURVE ( 'NONE', #58413, #18810, #18188, .T. ) ;
#15783=ORIENTED_EDGE ( 'NONE', *, *, #38759, .T. ) ;
#15819=FACE_OUTER_BOUND ( 'NONE', #59224, .T. ) ;
#15823=EDGE_CURVE ( 'NONE', #31185, #60007, #2281, .T. ) ;
#15839=DIRECTION ( 'NONE',  ( 0.000000000000000000, 0.000000000000000000, -1.000000000000000000 ) ) ;
#15848=AXIS2_PLACEMENT_3D ( 'NONE', #49229, #60114, #16206 ) ;
#15850=EDGE_CURVE ( 'NONE', #3825, #56118, #57240, .T. ) ;
#15869=DIRECTION ( 'NONE',  ( -0.000000000000000000, -0.000000000000000000, -1.000000000000000000 ) ) ;
#15886=VECTOR ( 'NONE', #64, 1000.000000000000000 ) ;
#15889=AXIS2_PLACEMENT_3D ( 'NONE', #44213, #821, #11803 ) ;
#15901=ORIENTED_EDGE ( 'NONE', *, *, #34867, .F. ) ;
#15904=UNCERTAINTY_MEASURE_WITH_UNIT (LENGTH_MEASURE( 1.000000000000000082E-05 ), #28086, 'distance_accuracy_value', 'NONE');
#15924=ORIENTED_EDGE ( 'NONE', *, *, #46272, .T. ) ;
#15950=PRESENTATION_STYLE_ASSIGNMENT (( #47989 ) ) ;
#15977=LINE ( 'NONE', #37460, #14539 ) ;
#15978=CARTESIAN_POINT ( 'NONE',  ( 44.25000000000000000, 21.74999999999998579, 4.000000000000000000 ) ) ;
#15993=DIRECTION ( 'NONE',  ( 0.000000000000000000, 0.000000000000000000, -1.000000000000000000 ) ) ;
#16005=DIRECTION ( 'NONE',  ( 0.000000000000000000, 0.000000000000000000, 1.000000000000000000 ) ) ;
#16022=DIRECTION ( 'NONE',  ( 1.156482317317870344E-15, 1.000000000000000000, 0.000000000000000000 ) ) ;
#16055=DIRECTION ( 'NONE',  ( 0.000000000000000000, 0.000000000000000000, 1.000000000000000000 ) ) ;
#16057=DIRECTION ( 'NONE',  ( 1.000000000000000000, 0.000000000000000000, 0.000000000000000000 ) ) ;
#16070=( GEOMETRIC_REPRESENTATION_CONTEXT ( 3 ) GLOBAL_UNCERTAINTY_ASSIGNED_CONTEXT ( ( #31851 ) ) GLOBAL_UNIT_ASSIGNED_CONTEXT ( ( #24899, #40419, #46412 ) ) REPRESENTATION_CONTEXT ( 'NONE', 'WORKASPACE' ) );
#16076=FACE_OUTER_BOUND ( 'NONE', #53083, .T. ) ;
#16080=VECTOR ( 'NONE', #31269, 1000.000000000000000 ) ;
#16089=DIRECTION ( 'NONE',  ( -1.000000000000000000, 0.000000000000000000, 0.000000000000000000 ) ) ;
#16102=ORIENTED_EDGE ( 'NONE', *, *, #46904, .T. ) ;
#16119=AXIS2_PLACEMENT_3D ( 'NONE', #15004, #51928, #36478 ) ;
#16127=ORIENTED_EDGE ( 'NONE', *, *, #65603, .T. ) ;
#16128=EDGE_LOOP ( 'NONE', ( #18155, #2339 ) ) ;
#16145=DIRECTION ( 'NONE',  ( 0.000000000000000000, -1.000000000000000000, 0.000000000000000000 ) ) ;
#16190=EDGE_LOOP ( 'NONE', ( #67738, #6770, #63, #57552 ) ) ;
#16194=TOROIDAL_SURFACE ( 'NONE', #57748, 0.7500000000000000000, 0.2500000000000000000 ) ;
#16202=CYLINDRICAL_SURFACE ( 'NONE', #19756, 0.2500000000000002220 ) ;
#16204=CARTESIAN_POINT ( 'NONE',  ( 8.250000000000001776, 31.24999999999998579, -3.750000000000000000 ) ) ;
#16206=DIRECTION ( 'NONE',  ( -1.000000000000000000, 0.000000000000000000, 0.000000000000000000 ) ) ;
#16231=FACE_OUTER_BOUND ( 'NONE', #68759, .T. ) ;
#16243=DIRECTION ( 'NONE',  ( -2.312964634635740689E-15, 1.000000000000000000, 0.000000000000000000 ) ) ;
#16256=VECTOR ( 'NONE', #17029, 1000.000000000000000 ) ;
#16272=CIRCLE ( 'NONE', #42102, 0.2500000000000002220 ) ;
#16290=DIRECTION ( 'NONE',  ( -1.000000000000000000, 0.000000000000000000, 0.000000000000000000 ) ) ;
#16292=PRESENTATION_STYLE_ASSIGNMENT (( #20851 ) ) ;
#16296=ORIENTED_EDGE ( 'NONE', *, *, #34466, .T. ) ;
#16351=DIRECTION ( 'NONE',  ( -1.000000000000000000, 0.000000000000000000, 0.000000000000000000 ) ) ;
#16352=DIRECTION ( 'NONE',  ( 0.000000000000000000, 0.000000000000000000, 1.000000000000000000 ) ) ;
#16402=EDGE_CURVE ( 'NONE', #25558, #17986, #56129, .T. ) ;
#16424=CARTESIAN_POINT ( 'NONE',  ( 48.75000000000000000, 22.24999999999998579, 4.000000000000000000 ) ) ;
#16443=DIRECTION ( 'NONE',  ( 0.000000000000000000, 0.000000000000000000, -1.000000000000000000 ) ) ;
#16454=ORIENTED_EDGE ( 'NONE', *, *, #62101, .T. ) ;
#16456=DIRECTION ( 'NONE',  ( 0.000000000000000000, -1.000000000000000000, 0.000000000000000000 ) ) ;
#16469=EDGE_CURVE ( 'NONE', #16642, #47549, #57359, .T. ) ;
#16471=ORIENTED_EDGE ( 'NONE', *, *, #61146, .F. ) ;
#16485=DIRECTION ( 'NONE',  ( 7.709882115452468306E-16, -1.000000000000000000, 0.000000000000000000 ) ) ;
#16489=DIRECTION ( 'NONE',  ( 0.000000000000000000, -1.000000000000000000, 0.000000000000000000 ) ) ;
#16493=CARTESIAN_POINT ( 'NONE',  ( 30.25000000000000711, 18.74999999999997868, 4.000000000000000000 ) ) ;
#16501=FACE_OUTER_BOUND ( 'NONE', #9340, .T. ) ;
#16502=EDGE_CURVE ( 'NONE', #22240, #51729, #38311, .T. ) ;
#16510=ORIENTED_EDGE ( 'NONE', *, *, #68452, .T. ) ;
#16517=ORIENTED_EDGE ( 'NONE', *, *, #3878, .F. ) ;
#16534=DIRECTION ( 'NONE',  ( -1.000000000000000000, 0.000000000000000000, 0.000000000000000000 ) ) ;
#16538=( LENGTH_UNIT ( ) NAMED_UNIT ( * ) SI_UNIT ( .MILLI., .METRE. ) );
#16545=DIRECTION ( 'NONE',  ( -1.224646799147353207E-16, 1.000000000000000000, 0.000000000000000000 ) ) ;
#16564=DIRECTION ( 'NONE',  ( 0.000000000000000000, -0.000000000000000000, 1.000000000000000000 ) ) ;
#16576=DIRECTION ( 'NONE',  ( 1.000000000000000000, -0.000000000000000000, 0.000000000000000000 ) ) ;
#16592=ORIENTED_EDGE ( 'NONE', *, *, #34062, .T. ) ;
#16604=CIRCLE ( 'NONE', #48059, 0.2500000000000002220 ) ;
#16615=CARTESIAN_POINT ( 'NONE',  ( 62.24999999999998579, 33.74999999999999289, 3.750000000000000000 ) ) ;
#16626=DIRECTION ( 'NONE',  ( 1.000000000000000000, -0.000000000000000000, 0.000000000000000000 ) ) ;
#16635=EDGE_LOOP ( 'NONE', ( #42332, #44822, #38162 ) ) ;
#16642=VERTEX_POINT ( 'NONE', #20718 ) ;
#16674=CARTESIAN_POINT ( 'NONE',  ( 30.25000000000000711, 18.99999999999997868, 3.750000000000000000 ) ) ;
#16684=DIRECTION ( 'NONE',  ( -0.000000000000000000, -0.000000000000000000, 1.000000000000000000 ) ) ;
#16688=ORIENTED_EDGE ( 'NONE', *, *, #455, .F. ) ;
#16691=DIRECTION ( 'NONE',  ( 0.000000000000000000, 0.000000000000000000, -1.000000000000000000 ) ) ;
#16715=EDGE_CURVE ( 'NONE', #69269, #60522, #46360, .T. ) ;
#16717=ORIENTED_EDGE ( 'NONE', *, *, #22503, .F. ) ;
#16719=CARTESIAN_POINT ( 'NONE',  ( 7.750000000000000000, 33.74999999999998579, 3.750000000000000000 ) ) ;
#16761=EDGE_CURVE ( 'NONE', #45200, #31185, #54022, .T. ) ;
#16762=CARTESIAN_POINT ( 'NONE',  ( 48.50000000000000000, 21.99999999999998579, 4.000000000000000000 ) ) ;
#16773=DIRECTION ( 'NONE',  ( 1.156482317317870344E-15, -1.000000000000000000, -0.000000000000000000 ) ) ;
#16779=CARTESIAN_POINT ( 'NONE',  ( 48.74999999999999289, 24.74999999999998579, -3.750000000000000000 ) ) ;
#16781=DIRECTION ( 'NONE',  ( -0.000000000000000000, -0.000000000000000000, 1.000000000000000000 ) ) ;
#16785=AXIS2_PLACEMENT_3D ( 'NONE', #66647, #33926, #45579 ) ;
#16794=EDGE_CURVE ( 'NONE', #10834, #22530, #6829, .T. ) ;
#16795=FACE_OUTER_BOUND ( 'NONE', #22601, .T. ) ;
#16797=CYLINDRICAL_SURFACE ( 'NONE', #5535, 0.2500000000000002220 ) ;
#16798=CARTESIAN_POINT ( 'NONE',  ( 21.75000000000001066, 21.74999999999998224, 3.750000000000000000 ) ) ;
#16814=CIRCLE ( 'NONE', #29102, 0.2500000000000002220 ) ;
#16820=DIRECTION ( 'NONE',  ( -1.000000000000000000, 0.000000000000000000, 0.000000000000000000 ) ) ;
#16854=CARTESIAN_POINT ( 'NONE',  ( 3.749999999999999556, 33.99999999999998579, 4.000000000000000000 ) ) ;
#16883=ADVANCED_FACE ( 'NONE', ( #37193 ), #15715, .T. ) ;
#16906=CARTESIAN_POINT ( 'NONE',  ( 26.00000000000001066, 21.74999999999998224, -3.750000000000000000 ) ) ;
#16913=DIRECTION ( 'NONE',  ( -1.000000000000000000, 0.000000000000000000, 0.000000000000000000 ) ) ;
#16922=( GEOMETRIC_REPRESENTATION_CONTEXT ( 3 ) GLOBAL_UNCERTAINTY_ASSIGNED_CONTEXT ( ( #24937 ) ) GLOBAL_UNIT_ASSIGNED_CONTEXT ( ( #46089, #63278, #52737 ) ) REPRESENTATION_CONTEXT ( 'NONE', 'WORKASPACE' ) );
#16934=ORIENTED_EDGE ( 'NONE', *, *, #5104, .F. ) ;
#16949=AXIS2_PLACEMENT_3D ( 'NONE', #61151, #56561, #3039 ) ;
#16963=EDGE_LOOP ( 'NONE', ( #20728, #62670, #55445 ) ) ;
#16968=DIRECTION ( 'NONE',  ( -1.000000000000000000, 0.000000000000000000, 0.000000000000000000 ) ) ;
#16974=CARTESIAN_POINT ( 'NONE',  ( 43.75000000000000000, 18.99999999999998224, -4.000000000000000000 ) ) ;
#16981=VECTOR ( 'NONE', #63951, 1000.000000000000114 ) ;
#17029=DIRECTION ( 'NONE',  ( -1.000000000000000000, 0.000000000000000000, 0.000000000000000000 ) ) ;
#17030=CIRCLE ( 'NONE', #12511, 0.5000000000000004441 ) ;
#17044=VERTEX_POINT ( 'NONE', #7563 ) ;
#17054=EDGE_LOOP ( 'NONE', ( #31536, #68946, #59272, #7200 ) ) ;
#17055=CARTESIAN_POINT ( 'NONE',  ( 16.75000000000000711, 25.24999999999998224, -3.750000000000000000 ) ) ;
#17058=ORIENTED_EDGE ( 'NONE', *, *, #33793, .T. ) ;
#17067=CARTESIAN_POINT ( 'NONE',  ( 68.99999999999998579, 8.450062914116736267E-15, 3.000000000000000000 ) ) ;
#17084=ORIENTED_EDGE ( 'NONE', *, *, #42233, .F. ) ;
#17105=AXIS2_PLACEMENT_3D ( 'NONE', #41130, #67839, #30875 ) ;
#17116=EDGE_CURVE ( 'NONE', #24476, #22828, #18479, .T. ) ;
#17132=DIRECTION ( 'NONE',  ( 1.000000000000000000, -0.000000000000000000, 0.000000000000000000 ) ) ;
#17141=ORIENTED_EDGE ( 'NONE', *, *, #39438, .T. ) ;
#17145=FACE_OUTER_BOUND ( 'NONE', #52666, .T. ) ;
#17147=DIRECTION ( 'NONE',  ( -0.000000000000000000, -0.000000000000000000, 1.000000000000000000 ) ) ;
#17153=ORIENTED_EDGE ( 'NONE', *, *, #33836, .F. ) ;
#17162=FACE_OUTER_BOUND ( 'NONE', #54825, .T. ) ;
#17180=EDGE_CURVE ( 'NONE', #14431, #7659, #56334, .T. ) ;
#17191=AXIS2_PLACEMENT_3D ( 'NONE', #16615, #15242, #32074 ) ;
#17209=EDGE_CURVE ( 'NONE', #54091, #25430, #25468, .T. ) ;
#17230=ORIENTED_EDGE ( 'NONE', *, *, #8144, .F. ) ;
#17247=DIRECTION ( 'NONE',  ( -0.000000000000000000, 0.000000000000000000, -1.000000000000000000 ) ) ;
#17251=AXIS2_PLACEMENT_3D ( 'NONE', #62613, #14429, #58390 ) ;
#17276=DIRECTION ( 'NONE',  ( -0.000000000000000000, 0.000000000000000000, 1.000000000000000000 ) ) ;
#17291=EDGE_CURVE ( 'NONE', #9702, #17044, #22609, .T. ) ;
#17297=DIRECTION ( 'NONE',  ( 0.000000000000000000, -1.000000000000000000, 0.000000000000000000 ) ) ;
#17309=EDGE_CURVE ( 'NONE', #31359, #52155, #61910, .T. ) ;
#17332=ORIENTED_EDGE ( 'NONE', *, *, #10336, .F. ) ;
#17336=VERTEX_POINT ( 'NONE', #11720 ) ;
#17351=CARTESIAN_POINT ( 'NONE',  ( 69.99999999999998579, 36.75000000000000000, -3.750000000000000000 ) ) ;
#17355=EDGE_LOOP ( 'NONE', ( #59752, #869, #48531, #41978 ) ) ;
#17371=AXIS2_PLACEMENT_3D ( 'NONE', #59276, #142, #16443 ) ;
#17424=DIRECTION ( 'NONE',  ( -1.000000000000000000, 0.000000000000000000, 0.000000000000000000 ) ) ;
#17448=CYLINDRICAL_SURFACE ( 'NONE', #385, 0.2500000000000002220 ) ;
#17455=DIRECTION ( 'NONE',  ( -0.000000000000000000, 0.000000000000000000, -1.000000000000000000 ) ) ;
#17456=DIRECTION ( 'NONE',  ( 1.000000000000000000, 7.709882115452468306E-16, -0.000000000000000000 ) ) ;
#17463=DIRECTION ( 'NONE',  ( 0.000000000000000000, -0.000000000000000000, 1.000000000000000000 ) ) ;
#17494=ORIENTED_EDGE ( 'NONE', *, *, #39753, .F. ) ;
#17529=CARTESIAN_POINT ( 'NONE',  ( 68.99999999999998579, 36.75000000000000000, 3.750000000000000000 ) ) ;
#17536=DIRECTION ( 'NONE',  ( 1.000000000000000000, 0.000000000000000000, 0.000000000000000000 ) ) ;
#17546=EDGE_LOOP ( 'NONE', ( #40092, #46038, #38450, #42053 ) ) ;
#17549=CIRCLE ( 'NONE', #51227, 0.2500000000000000000 ) ;
#17551=DIRECTION ( 'NONE',  ( 0.000000000000000000, -1.000000000000000000, 0.000000000000000000 ) ) ;
#17557=ORIENTED_EDGE ( 'NONE', *, *, #3147, .T. ) ;
#17560=ORIENTED_EDGE ( 'NONE', *, *, #27934, .T. ) ;
#17563=CARTESIAN_POINT ( 'NONE',  ( 10.99999999999999645, 11.99999999999999289, -3.499999999999991118 ) ) ;
#17590=CIRCLE ( 'NONE', #20791, 0.2500000000000002220 ) ;
#17601=SURFACE_SIDE_STYLE ('',( #34438 ) ) ;
#17602=CARTESIAN_POINT ( 'NONE',  ( 57.24999999999999289, 28.24999999999998934, -3.750000000000000000 ) ) ;
#17621=CARTESIAN_POINT ( 'NONE',  ( 53.24999999999999289, 27.74999999999998579, 4.000000000000000000 ) ) ;
#17636=CARTESIAN_POINT ( 'NONE',  ( 3.249999999999998668, 36.74999999999999289, 3.750000000000000000 ) ) ;
#17662=EDGE_CURVE ( 'NONE', #10834, #47340, #64726, .T. ) ;
#17674=ADVANCED_FACE ( 'NONE', ( #69648 ), #10232, .F. ) ;
#17686=LINE ( 'NONE', #34870, #10420 ) ;
#17696=ADVANCED_FACE ( 'NONE', ( #65763 ), #9109, .F. ) ;
#17697=CARTESIAN_POINT ( 'NONE',  ( 66.49999999999998579, 37.00000000000000000, 3.750000000000000000 ) ) ;
#17707=DIRECTION ( 'NONE',  ( -0.000000000000000000, 0.000000000000000000, -1.000000000000000000 ) ) ;
#17708=EDGE_LOOP ( 'NONE', ( #49619, #68445, #2036, #66810 ) ) ;
#17711=DIRECTION ( 'NONE',  ( -1.000000000000000000, 0.000000000000000000, 0.000000000000000000 ) ) ;
#17741=AXIS2_PLACEMENT_3D ( 'NONE', #48858, #3888, #52817 ) ;
#17747=CIRCLE ( 'NONE', #43631, 0.2500000000000002220 ) ;
#17761=ORIENTED_EDGE ( 'NONE', *, *, #1773, .T. ) ;
#17775=FACE_OUTER_BOUND ( 'NONE', #68156, .T. ) ;
#17795=EDGE_CURVE ( 'NONE', #57518, #11461, #32625, .T. ) ;
#17796=DIRECTION ( 'NONE',  ( -1.000000000000000000, 0.000000000000000000, 0.000000000000000000 ) ) ;
#17807=EDGE_CURVE ( 'NONE', #21355, #14431, #55116, .T. ) ;
#17815=ORIENTED_EDGE ( 'NONE', *, *, #16715, .F. ) ;
#17836=DIRECTION ( 'NONE',  ( 0.000000000000000000, -1.000000000000000000, 0.000000000000000000 ) ) ;
#17840=CARTESIAN_POINT ( 'NONE',  ( 68.99999999999998579, 8.572527594031471415E-15, -4.000000000000000000 ) ) ;
#17860=FACE_OUTER_BOUND ( 'NONE', #19971, .T. ) ;
#17861=CIRCLE ( 'NONE', #42610, 0.5000000000000004441 ) ;
#17884=AXIS2_PLACEMENT_3D ( 'NONE', #34529, #12367, #2469 ) ;
#17887=VERTEX_POINT ( 'NONE', #10126 ) ;
#17895=EDGE_LOOP ( 'NONE', ( #56185, #46849, #48201, #58475 ) ) ;
#17916=EDGE_LOOP ( 'NONE', ( #26563, #45463, #52946, #11632 ) ) ;
#17929=TOROIDAL_SURFACE ( 'NONE', #47203, 0.5000000000000000000, 0.2500000000000000000 ) ;
#17935=VECTOR ( 'NONE', #10244, 1000.000000000000000 ) ;
#17937=CARTESIAN_POINT ( 'NONE',  ( 8.000000000000001776, 31.24999999999998579, -3.750000000000000000 ) ) ;
#17951=ORIENTED_EDGE ( 'NONE', *, *, #65456, .F. ) ;
#17968=ORIENTED_EDGE ( 'NONE', *, *, #23700, .F. ) ;
#17986=VERTEX_POINT ( 'NONE', #48836 ) ;
#18010=LINE ( 'NONE', #13777, #21224 ) ;
#18029=ORIENTED_EDGE ( 'NONE', *, *, #18451, .T. ) ;
#18030=DIRECTION ( 'NONE',  ( -1.000000000000000000, 0.000000000000000000, 0.000000000000000000 ) ) ;
#18071=ORIENTED_EDGE ( 'NONE', *, *, #36974, .F. ) ;
#18083=VERTEX_POINT ( 'NONE', #48134 ) ;
#18095=STYLED_ITEM ( 'NONE', ( #18794 ), #28762 ) ;
#18099=CARTESIAN_POINT ( 'NONE',  ( 48.25000000000000000, 21.74999999999998579, 3.750000000000000000 ) ) ;
#18100=DIRECTION ( 'NONE',  ( -0.000000000000000000, -0.000000000000000000, 1.000000000000000000 ) ) ;
#18104=AXIS2_PLACEMENT_3D ( 'NONE', #12914, #34028, #11883 ) ;
#18106=ORIENTED_EDGE ( 'NONE', *, *, #36079, .T. ) ;
#18113=( LENGTH_UNIT ( ) NAMED_UNIT ( * ) SI_UNIT ( .MILLI., .METRE. ) );
#18120=AXIS2_PLACEMENT_3D ( 'NONE', #56005, #29634, #50747 ) ;
#18129=AXIS2_PLACEMENT_3D ( 'NONE', #36768, #26151, #32134 ) ;
#18131=DIRECTION ( 'NONE',  ( -1.000000000000000000, 0.000000000000000000, 0.000000000000000000 ) ) ;
#18135=DIRECTION ( 'NONE',  ( -1.000000000000000000, 0.000000000000000000, 0.000000000000000000 ) ) ;
#18154=CARTESIAN_POINT ( 'NONE',  ( 0.000000000000000000, 21.74999999999998579, 3.750000000000000000 ) ) ;
#18155=ORIENTED_EDGE ( 'NONE', *, *, #61051, .T. ) ;
#18158=ORIENTED_EDGE ( 'NONE', *, *, #7557, .T. ) ;
#18159=ORIENTED_EDGE ( 'NONE', *, *, #21138, .F. ) ;
#18172=CARTESIAN_POINT ( 'NONE',  ( 66.49999999999998579, 36.75000000000000000, 4.000000000000000000 ) ) ;
#18176=DIRECTION ( 'NONE',  ( -1.000000000000000000, 0.000000000000000000, 0.000000000000000000 ) ) ;
#18186=DIRECTION ( 'NONE',  ( -0.000000000000000000, -0.000000000000000000, 1.000000000000000000 ) ) ;
#18188=LINE ( 'NONE', #66732, #5656 ) ;
#18195=DIRECTION ( 'NONE',  ( 0.000000000000000000, -0.000000000000000000, 1.000000000000000000 ) ) ;
#18200=CARTESIAN_POINT ( 'NONE',  ( 12.25000000000000533, 28.24999999999998224, -3.750000000000000000 ) ) ;
#18209=CIRCLE ( 'NONE', #2445, 0.2500000000000002220 ) ;
#18212=CYLINDRICAL_SURFACE ( 'NONE', #23824, 0.2500000000000002220 ) ;
#18235=ORIENTED_EDGE ( 'NONE', *, *, #59471, .T. ) ;
#18253=DIRECTION ( 'NONE',  ( 0.000000000000000000, -1.000000000000000000, 0.000000000000000000 ) ) ;
#18256=ORIENTED_EDGE ( 'NONE', *, *, #26119, .T. ) ;
#18270=CARTESIAN_POINT ( 'NONE',  ( 66.74999999999998579, 37.00000000000000000, -3.750000000000000000 ) ) ;
#18281=CARTESIAN_POINT ( 'NONE',  ( 68.99999999999998579, 1.000000000000008438, 3.000000000000000000 ) ) ;
#18296=DIRECTION ( 'NONE',  ( -1.000000000000000000, 0.000000000000000000, 0.000000000000000000 ) ) ;
#18308=COLOUR_RGB ( '', 0.40784314, 0.44705882, 0.49803922) ;
#18309=VERTEX_POINT ( 'NONE', #20138 ) ;
#18315=DIRECTION ( 'NONE',  ( -1.000000000000000000, 0.000000000000000000, 0.000000000000000000 ) ) ;
#18321=LINE ( 'NONE', #19337, #3193 ) ;
#18325=DIRECTION ( 'NONE',  ( 0.000000000000000000, 0.000000000000000000, 1.000000000000000000 ) ) ;
#18336=DIRECTION ( 'NONE',  ( 0.000000000000000000, -1.000000000000000000, 0.000000000000000000 ) ) ;
#18348=CARTESIAN_POINT ( 'NONE',  ( 21.50000000000000711, 21.99999999999998224, 4.000000000000000000 ) ) ;
#18395=LINE ( 'NONE', #50748, #33627 ) ;
#18396=DIRECTION ( 'NONE',  ( -1.000000000000000000, 0.000000000000000000, 0.000000000000000000 ) ) ;
#18451=EDGE_CURVE ( 'NONE', #50178, #58809, #50727, .T. ) ;
#18466=EDGE_CURVE ( 'NONE', #60291, #69646, #5808, .T. ) ;
#18479=LINE ( 'NONE', #45595, #40607 ) ;
#18491=ADVANCED_FACE ( 'NONE', ( #2455 ), #25005, .F. ) ;
#18498=DIRECTION ( 'NONE',  ( 1.000000000000000000, -7.709882115452468306E-16, -0.000000000000000000 ) ) ;
#18528=ORIENTED_EDGE ( 'NONE', *, *, #9158, .T. ) ;
#18529=CARTESIAN_POINT ( 'NONE',  ( 69.99999999999998579, 1.000000000000007772, -3.000000000000000000 ) ) ;
#18536=FACE_OUTER_BOUND ( 'NONE', #63436, .T. ) ;
#18542=DIRECTION ( 'NONE',  ( 0.000000000000000000, 0.000000000000000000, -1.000000000000000000 ) ) ;
#18555=CIRCLE ( 'NONE', #43319, 0.2500000000000002220 ) ;
#18571=CARTESIAN_POINT ( 'NONE',  ( 57.24999999999999289, 27.74999999999998934, -4.000000000000000000 ) ) ;
#18577=CARTESIAN_POINT ( 'NONE',  ( 52.75000000000000000, 24.74999999999998224, -3.750000000000000000 ) ) ;
#18590=EDGE_CURVE ( 'NONE', #29672, #14650, #20446, .T. ) ;
#18597=ADVANCED_FACE ( 'NONE', ( #20425 ), #41927, .F. ) ;
#18611=ORIENTED_EDGE ( 'NONE', *, *, #17309, .T. ) ;
#18612=DIRECTION ( 'NONE',  ( -1.000000000000000000, -5.782411586589331015E-16, 0.000000000000000000 ) ) ;
#18735=EDGE_LOOP ( 'NONE', ( #61132, #65004, #60925 ) ) ;
#18751=CIRCLE ( 'NONE', #33363, 0.2500000000000002220 ) ;
#18759=CARTESIAN_POINT ( 'NONE',  ( 39.49999999999999289, 16.24999999999997513, 3.750000000000000000 ) ) ;
#18773=CARTESIAN_POINT ( 'NONE',  ( 0.000000000000000000, 0.000000000000000000, 4.000000000000000000 ) ) ;
#18790=EDGE_CURVE ( 'NONE', #27898, #68919, #5854, .T. ) ;
#18794=PRESENTATION_STYLE_ASSIGNMENT (( #8946 ) ) ;
#18796=TOROIDAL_SURFACE ( 'NONE', #36822, 0.5000000000000000000, 0.2500000000000000000 ) ;
#18800=ORIENTED_EDGE ( 'NONE', *, *, #26210, .F. ) ;
#18810=VERTEX_POINT ( 'NONE', #38382 ) ;
#18819=DIRECTION ( 'NONE',  ( -1.000000000000000000, 0.000000000000000000, 0.000000000000000000 ) ) ;
#18821=DIRECTION ( 'NONE',  ( -1.000000000000000000, 0.000000000000000000, 0.000000000000000000 ) ) ;
#18838=ORIENTED_EDGE ( 'NONE', *, *, #8749, .T. ) ;
#18854=CYLINDRICAL_SURFACE ( 'NONE', #34710, 0.2500000000000002220 ) ;
#18860=DIRECTION ( 'NONE',  ( 0.000000000000000000, -1.000000000000000000, 0.000000000000000000 ) ) ;
#18869=EDGE_CURVE ( 'NONE', #2790, #14650, #44692, .T. ) ;
#18890=CARTESIAN_POINT ( 'NONE',  ( -1.445602896647333671E-14, 18.74999999999994671, 3.750000000000000000 ) ) ;
#18919=ORIENTED_EDGE ( 'NONE', *, *, #33928, .F. ) ;
#18938=AXIS2_PLACEMENT_3D ( 'NONE', #33924, #66280, #67326 ) ;
#18967=CARTESIAN_POINT ( 'NONE',  ( 25.75000000000001066, 19.24999999999997868, -3.750000000000000000 ) ) ;
#18978=DIRECTION ( 'NONE',  ( -1.000000000000000000, 0.000000000000000000, 0.000000000000000000 ) ) ;
#18979=ORIENTED_EDGE ( 'NONE', *, *, #33147, .F. ) ;
#18984=ORIENTED_EDGE ( 'NONE', *, *, #61694, .F. ) ;
#18999=DIRECTION ( 'NONE',  ( 0.000000000000000000, -0.000000000000000000, -1.000000000000000000 ) ) ;
#19042=AXIS2_PLACEMENT_3D ( 'NONE', #43369, #65451, #28122 ) ;
#19044=ORIENTED_EDGE ( 'NONE', *, *, #16794, .T. ) ;
#19047=EDGE_CURVE ( 'NONE', #37864, #9427, #29523, .T. ) ;
#19072=DIRECTION ( 'NONE',  ( -1.000000000000000000, 0.000000000000000000, 0.000000000000000000 ) ) ;
#19099=DIRECTION ( 'NONE',  ( 0.000000000000000000, 0.000000000000000000, -1.000000000000000000 ) ) ;
#19105=CARTESIAN_POINT ( 'NONE',  ( 30.50000000000001066, 16.24999999999997513, -3.750000000000000000 ) ) ;
#19132=PLANE ( 'NONE',  #29354 ) ;
#19145=DIRECTION ( 'NONE',  ( 0.000000000000000000, 0.000000000000000000, -1.000000000000000000 ) ) ;
#19170=EDGE_LOOP ( 'NONE', ( #58076, #377, #53853, #47878 ) ) ;
#19190=FACE_OUTER_BOUND ( 'NONE', #25322, .T. ) ;
#19197=VECTOR ( 'NONE', #13355, 1000.000000000000000 ) ;
#19206=CARTESIAN_POINT ( 'NONE',  ( 48.74999999999999289, 24.74999999999998579, 4.000000000000000000 ) ) ;
#19236=VERTEX_POINT ( 'NONE', #13224 ) ;
#19269=ORIENTED_EDGE ( 'NONE', *, *, #43256, .T. ) ;
#19291=VECTOR ( 'NONE', #1522, 1000.000000000000000 ) ;
#19330=DIRECTION ( 'NONE',  ( 0.000000000000000000, 0.000000000000000000, -1.000000000000000000 ) ) ;
#19333=VERTEX_POINT ( 'NONE', #18529 ) ;
#19334=FACE_OUTER_BOUND ( 'NONE', #13135, .T. ) ;
#19337=CARTESIAN_POINT ( 'NONE',  ( 61.99999999999998579, 33.74999999999999289, 4.000000000000000000 ) ) ;
#19343=VERTEX_POINT ( 'NONE', #40017 ) ;
#19346=CARTESIAN_POINT ( 'NONE',  ( 1.000000000000000000, 0.000000000000000000, -3.000000000000000000 ) ) ;
#19366=VECTOR ( 'NONE', #13828, 1000.000000000000000 ) ;
#19371=DIRECTION ( 'NONE',  ( 1.000000000000000000, 0.000000000000000000, -0.000000000000000000 ) ) ;
#19379=AXIS2_PLACEMENT_3D ( 'NONE', #17351, #18, #38120 ) ;
#19392=CARTESIAN_POINT ( 'NONE',  ( 68.99999999999998579, 37.00000000000000000, 3.750000000000000000 ) ) ;
#19399=CARTESIAN_POINT ( 'NONE',  ( 21.50000000000001066, 24.99999999999998579, 4.000000000000000000 ) ) ;
#19421=ORIENTED_EDGE ( 'NONE', *, *, #14563, .T. ) ;
#19444=ORIENTED_EDGE ( 'NONE', *, *, #69110, .T. ) ;
#19467=AXIS2_PLACEMENT_3D ( 'NONE', #6295, #6996, #49227 ) ;
#19497=CIRCLE ( 'NONE', #8274, 0.2500000000000002220 ) ;
#19500=FACE_OUTER_BOUND ( 'NONE', #46525, .T. ) ;
#19502=VERTEX_POINT ( 'NONE', #21633 ) ;
#19503=CARTESIAN_POINT ( 'NONE',  ( 44.25000000000000000, 19.24999999999998224, 3.750000000000000000 ) ) ;
#19506=ORIENTED_EDGE ( 'NONE', *, *, #63387, .F. ) ;
#19516=EDGE_LOOP ( 'NONE', ( #58758, #10388, #26854, #35745 ) ) ;
#19536=VERTEX_POINT ( 'NONE', #11774 ) ;
#19567=DIRECTION ( 'NONE',  ( -0.000000000000000000, -1.000000000000000000, -0.000000000000000000 ) ) ;
#19626=FACE_OUTER_BOUND ( 'NONE', #69227, .T. ) ;
#19633=CARTESIAN_POINT ( 'NONE',  ( 7.750000000000000000, 33.74999999999998579, 4.000000000000000000 ) ) ;
#19646=DIRECTION ( 'NONE',  ( -0.000000000000000000, 0.000000000000000000, -1.000000000000000000 ) ) ;
#19658=CARTESIAN_POINT ( 'NONE',  ( 1.000000000000000222, 1.224646799147373175E-16, -3.000000000000000000 ) ) ;
#19698=CARTESIAN_POINT ( 'NONE',  ( 57.74999999999998579, 30.99999999999999289, 4.000000000000000000 ) ) ;
#19731=LINE ( 'NONE', #60625, #39010 ) ;
#19736=DIRECTION ( 'NONE',  ( 0.000000000000000000, 0.000000000000000000, 1.000000000000000000 ) ) ;
#19740=LINE ( 'NONE', #25363, #21857 ) ;
#19746=AXIS2_PLACEMENT_3D ( 'NONE', #63885, #53014, #47070 ) ;
#19747=CIRCLE ( 'NONE', #64695, 1.000000000000000000 ) ;
#19756=AXIS2_PLACEMENT_3D ( 'NONE', #69623, #42593, #59763 ) ;
#19763=CIRCLE ( 'NONE', #14153, 0.2500000000000002220 ) ;
#19770=ORIENTED_EDGE ( 'NONE', *, *, #11086, .F. ) ;
#19785=EDGE_CURVE ( 'NONE', #24442, #28025, #37797, .T. ) ;
#19790=ORIENTED_EDGE ( 'NONE', *, *, #68246, .F. ) ;
#19817=EDGE_CURVE ( 'NONE', #24442, #28382, #7736, .T. ) ;
#19821=ORIENTED_EDGE ( 'NONE', *, *, #20950, .F. ) ;
#19827=DIRECTION ( 'NONE',  ( 0.000000000000000000, -1.000000000000000000, 0.000000000000000000 ) ) ;
#19831=ORIENTED_EDGE ( 'NONE', *, *, #35373, .F. ) ;
#19842=ORIENTED_EDGE ( 'NONE', *, *, #43771, .T. ) ;
#19891=ORIENTED_EDGE ( 'NONE', *, *, #4252, .F. ) ;
#19909=DIRECTION ( 'NONE',  ( -0.000000000000000000, 0.000000000000000000, -1.000000000000000000 ) ) ;
#19971=EDGE_LOOP ( 'NONE', ( #48584, #31259, #60905, #5469 ) ) ;
#20010=ORIENTED_EDGE ( 'NONE', *, *, #35035, .T. ) ;
#20025=DIRECTION ( 'NONE',  ( -0.000000000000000000, -0.000000000000000000, 1.000000000000000000 ) ) ;
#20032=DIRECTION ( 'NONE',  ( -0.000000000000000000, 0.000000000000000000, -1.000000000000000000 ) ) ;
#20079=UNCERTAINTY_MEASURE_WITH_UNIT (LENGTH_MEASURE( 1.000000000000000082E-05 ), #41639, 'distance_accuracy_value', 'NONE');
#20091=ORIENTED_EDGE ( 'NONE', *, *, #11050, .T. ) ;
#20092=ORIENTED_EDGE ( 'NONE', *, *, #33674, .T. ) ;
#20093=ADVANCED_FACE ( 'NONE', ( #44276 ), #18854, .T. ) ;
#20106=LINE ( 'NONE', #63391, #42819 ) ;
#20108=AXIS2_PLACEMENT_3D ( 'NONE', #64591, #22362, #818 ) ;
#20115=EDGE_LOOP ( 'NONE', ( #48275, #42459, #51044, #69294 ) ) ;
#20124=LINE ( 'NONE', #29746, #36764 ) ;
#20138=CARTESIAN_POINT ( 'NONE',  ( 7.400000000000003908, 11.99999999999999289, 4.000000000000000000 ) ) ;
#20174=CIRCLE ( 'NONE', #57225, 0.2500000000000002220 ) ;
#20180=CARTESIAN_POINT ( 'NONE',  ( 48.25000000000000000, 21.74999999999998579, -4.000000000000000000 ) ) ;
#20197=AXIS2_PLACEMENT_3D ( 'NONE', #6635, #45030, #2722 ) ;
#20218=SURFACE_STYLE_FILL_AREA ( #68094 ) ;
#20220=DIRECTION ( 'NONE',  ( -1.000000000000000000, 0.000000000000000000, 0.000000000000000000 ) ) ;
#20221=AXIS2_PLACEMENT_3D ( 'NONE', #44635, #66379, #45672 ) ;
#20255=DIRECTION ( 'NONE',  ( 0.000000000000000000, 0.000000000000000000, -1.000000000000000000 ) ) ;
#20264=DIRECTION ( 'NONE',  ( -0.000000000000000000, -0.000000000000000000, 1.000000000000000000 ) ) ;
#20276=MECHANICAL_DESIGN_GEOMETRIC_PRESENTATION_REPRESENTATION('',(#28134),#50625);
#20283=EDGE_CURVE ( 'NONE', #64812, #7926, #22378, .T. ) ;
#20295=CIRCLE ( 'NONE', #57417, 0.2500000000000002220 ) ;
#20310=EDGE_CURVE ( 'NONE', #68610, #11473, #49355, .T. ) ;
#20324=CARTESIAN_POINT ( 'NONE',  ( 44.25000000000000000, 21.99999999999998579, -3.750000000000000000 ) ) ;
#20330=DIRECTION ( 'NONE',  ( -1.000000000000000000, 0.000000000000000000, 0.000000000000000000 ) ) ;
#20333=VERTEX_POINT ( 'NONE', #41058 ) ;
#20341=AXIS2_PLACEMENT_3D ( 'NONE', #53347, #31508, #58258 ) ;
#20344=DIRECTION ( 'NONE',  ( 2.312964634635740689E-15, -1.000000000000000000, 0.000000000000000000 ) ) ;
#20348=EDGE_CURVE ( 'NONE', #28793, #38116, #44915, .T. ) ;
#20356=SURFACE_STYLE_USAGE ( .BOTH. , #68564 ) ;
#20374=CARTESIAN_POINT ( 'NONE',  ( 66.49999999999998579, 36.75000000000000000, 3.750000000000000000 ) ) ;
#20375=VECTOR ( 'NONE', #37113, 1000.000000000000000 ) ;
#20377=CARTESIAN_POINT ( 'NONE',  ( 17.25000000000000711, 24.99999999999998224, 3.750000000000000000 ) ) ;
#20386=ORIENTED_EDGE ( 'NONE', *, *, #43444, .T. ) ;
#20406=DIRECTION ( 'NONE',  ( 0.000000000000000000, 0.000000000000000000, -1.000000000000000000 ) ) ;
#20425=FACE_OUTER_BOUND ( 'NONE', #43538, .T. ) ;
#20431=ADVANCED_FACE ( 'NONE', ( #65597 ), #60317, .F. ) ;
#20436=DIRECTION ( 'NONE',  ( 0.000000000000000000, 0.000000000000000000, -1.000000000000000000 ) ) ;
#20437=ORIENTED_EDGE ( 'NONE', *, *, #45552, .F. ) ;
#20440=DIRECTION ( 'NONE',  ( 0.000000000000000000, -1.000000000000000000, 0.000000000000000000 ) ) ;
#20446=CIRCLE ( 'NONE', #1287, 0.2500000000000002220 ) ;
#20462=CONICAL_SURFACE ( 'NONE', #47480, 3.599999999999992095, 0.7853981633974375098 ) ;
#20464=DIRECTION ( 'NONE',  ( -1.000000000000000000, 0.000000000000000000, 0.000000000000000000 ) ) ;
#20493=VERTEX_POINT ( 'NONE', #62040 ) ;
#20505=FACE_OUTER_BOUND ( 'NONE', #91, .T. ) ;
#20512=ADVANCED_FACE ( 'NONE', ( #17775 ), #13867, .F. ) ;
#20515=AXIS2_PLACEMENT_3D ( 'NONE', #63671, #26705, #69635 ) ;
#20520=CARTESIAN_POINT ( 'NONE',  ( 17.00000000000000711, 24.99999999999998224, 4.000000000000000000 ) ) ;
#20522=LINE ( 'NONE', #48005, #21525 ) ;
#20543=LINE ( 'NONE', #69430, #34071 ) ;
#20554=AXIS2_PLACEMENT_3D ( 'NONE', #8043, #61479, #50610 ) ;
#20573=AXIS2_PLACEMENT_3D ( 'NONE', #13390, #50697, #34851 ) ;
#20610=VECTOR ( 'NONE', #22806, 1000.000000000000000 ) ;
#20614=CARTESIAN_POINT ( 'NONE',  ( 12.75000000000000533, 28.24999999999998224, -4.000000000000000000 ) ) ;
#20617=DIRECTION ( 'NONE',  ( 0.000000000000000000, 0.000000000000000000, 1.000000000000000000 ) ) ;
#20629=ADVANCED_FACE ( 'NONE', ( #45223 ), #13504, .T. ) ;
#20647=FACE_OUTER_BOUND ( 'NONE', #31699, .T. ) ;
#20655=EDGE_LOOP ( 'NONE', ( #11067, #9844, #64254, #11198 ) ) ;
#20664=ORIENTED_EDGE ( 'NONE', *, *, #40930, .T. ) ;
#20672=ADVANCED_FACE ( 'NONE', ( #29211 ), #66525, .F. ) ;
#20679=CARTESIAN_POINT ( 'NONE',  ( 66.49999999999998579, 34.24999999999999289, -3.750000000000000000 ) ) ;
#20686=FACE_OUTER_BOUND ( 'NONE', #13528, .T. ) ;
#20694=CARTESIAN_POINT ( 'NONE',  ( 62.10000000000000142, 11.99999999999999822, -3.499999999999999556 ) ) ;
#20718=CARTESIAN_POINT ( 'NONE',  ( 8.000000000000000000, 33.74999999999998579, 3.750000000000000000 ) ) ;
#20720=EDGE_LOOP ( 'NONE', ( #19421, #17332, #41465, #61809 ) ) ;
#20725=CARTESIAN_POINT ( 'NONE',  ( 7.750000000000000000, 33.74999999999998579, 4.000000000000000000 ) ) ;
#20728=ORIENTED_EDGE ( 'NONE', *, *, #8684, .F. ) ;
#20755=VECTOR ( 'NONE', #5952, 1000.000000000000000 ) ;
#20787=MECHANICAL_DESIGN_GEOMETRIC_PRESENTATION_REPRESENTATION('',(#33135),#29752);
#20791=AXIS2_PLACEMENT_3D ( 'NONE', #67444, #31450, #26179 ) ;
#20793=DIRECTION ( 'NONE',  ( 0.000000000000000000, 0.000000000000000000, -1.000000000000000000 ) ) ;
#20797=CARTESIAN_POINT ( 'NONE',  ( 7.750000000000001776, 31.24999999999998579, -4.000000000000000000 ) ) ;
#20798=DIRECTION ( 'NONE',  ( -0.000000000000000000, -0.000000000000000000, 1.000000000000000000 ) ) ;
#20804=CARTESIAN_POINT ( 'NONE',  ( 66.24999999999998579, 34.24999999999999289, -3.750000000000000000 ) ) ;
#20851=SURFACE_STYLE_USAGE ( .BOTH. , #52182 ) ;
#20902=LINE ( 'NONE', #59550, #42666 ) ;
#20928=CARTESIAN_POINT ( 'NONE',  ( 14.09999999999999609, 11.99999999999999289, 3.500000000000004885 ) ) ;
#20934=VECTOR ( 'NONE', #42424, 1000.000000000000114 ) ;
#20950=EDGE_CURVE ( 'NONE', #62934, #25473, #48338, .T. ) ;
#20957=CIRCLE ( 'NONE', #60257, 0.2500000000000002220 ) ;
#20962=DIRECTION ( 'NONE',  ( 0.000000000000000000, 1.000000000000000000, 0.000000000000000000 ) ) ;
#20970=EDGE_CURVE ( 'NONE', #21622, #50178, #8449, .T. ) ;
#20972=EDGE_CURVE ( 'NONE', #67683, #54091, #62236, .T. ) ;
#20990=DIRECTION ( 'NONE',  ( 0.000000000000000000, 0.000000000000000000, -1.000000000000000000 ) ) ;
#20995=CARTESIAN_POINT ( 'NONE',  ( 3.249999999999998668, 36.74999999999999289, -3.750000000000000000 ) ) ;
#20997=ORIENTED_EDGE ( 'NONE', *, *, #1281, .T. ) ;
#21022=EDGE_CURVE ( 'NONE', #19333, #40281, #31452, .T. ) ;
#21024=DIRECTION ( 'NONE',  ( -1.000000000000000000, 0.000000000000000000, 0.000000000000000000 ) ) ;
#21028=FACE_OUTER_BOUND ( 'NONE', #33152, .T. ) ;
#21044=DIRECTION ( 'NONE',  ( 0.000000000000000000, 0.000000000000000000, -1.000000000000000000 ) ) ;
#21054=LINE ( 'NONE', #59348, #16981 ) ;
#21065=ORIENTED_EDGE ( 'NONE', *, *, #1860, .F. ) ;
#21079=EDGE_CURVE ( 'NONE', #36379, #59308, #25838, .T. ) ;
#21085=CARTESIAN_POINT ( 'NONE',  ( 62.24999999999998579, 33.74999999999999289, 3.750000000000000000 ) ) ;
#21113=DIRECTION ( 'NONE',  ( 0.000000000000000000, 0.000000000000000000, -1.000000000000000000 ) ) ;
#21120=CARTESIAN_POINT ( 'NONE',  ( 57.74999999999999289, 28.24999999999998934, -3.750000000000000000 ) ) ;
#21125=CARTESIAN_POINT ( 'NONE',  ( 69.74999999999998579, 36.75000000000000000, -3.000000000000000000 ) ) ;
#21130=DIRECTION ( 'NONE',  ( -0.000000000000000000, 0.000000000000000000, -1.000000000000000000 ) ) ;
#21137=DIRECTION ( 'NONE',  ( -0.000000000000000000, -1.000000000000000000, -0.000000000000000000 ) ) ;
#21138=EDGE_CURVE ( 'NONE', #51968, #5374, #12372, .T. ) ;
#21140=CARTESIAN_POINT ( 'NONE',  ( 66.74999999999998579, 36.75000000000000000, -3.750000000000000000 ) ) ;
#21178=DIRECTION ( 'NONE',  ( 0.000000000000000000, 1.000000000000000000, 0.000000000000000000 ) ) ;
#21182=VECTOR ( 'NONE', #60654, 1000.000000000000000 ) ;
#21186=ORIENTED_EDGE ( 'NONE', *, *, #51951, .T. ) ;
#21224=VECTOR ( 'NONE', #2103, 1000.000000000000000 ) ;
#21233=ORIENTED_EDGE ( 'NONE', *, *, #11517, .T. ) ;
#21255=EDGE_CURVE ( 'NONE', #64131, #65411, #50654, .T. ) ;
#21256=ORIENTED_EDGE ( 'NONE', *, *, #21828, .F. ) ;
#21267=EDGE_CURVE ( 'NONE', #19236, #25473, #10189, .T. ) ;
#21276=CARTESIAN_POINT ( 'NONE',  ( 12.25000000000000355, 30.74999999999998579, 3.750000000000000000 ) ) ;
#21282=EDGE_CURVE ( 'NONE', #21325, #47241, #45070, .T. ) ;
#21287=DIRECTION ( 'NONE',  ( 0.000000000000000000, 0.000000000000000000, 1.000000000000000000 ) ) ;
#21315=SHAPE_REPRESENTATION ( '6. Lower Jaw', ( #42840 ), #7944 ) ;
#21322=VERTEX_POINT ( 'NONE', #27861 ) ;
#21325=VERTEX_POINT ( 'NONE', #7139 ) ;
#21330=DIRECTION ( 'NONE',  ( -0.000000000000000000, 0.000000000000000000, -1.000000000000000000 ) ) ;
#21334=DIRECTION ( 'NONE',  ( -0.000000000000000000, -0.000000000000000000, -1.000000000000000000 ) ) ;
#21341=CARTESIAN_POINT ( 'NONE',  ( 12.25000000000000355, 30.74999999999998579, -3.750000000000000000 ) ) ;
#21351=DIRECTION ( 'NONE',  ( -1.000000000000000000, -7.709882115452468306E-16, 0.000000000000000000 ) ) ;
#21355=VERTEX_POINT ( 'NONE', #1799 ) ;
#21358=DIRECTION ( 'NONE',  ( 1.000000000000000000, 7.709882115452468306E-16, 0.000000000000000000 ) ) ;
#21365=DIRECTION ( 'NONE',  ( 0.000000000000000000, 0.000000000000000000, -1.000000000000000000 ) ) ;
#21379=AXIS2_PLACEMENT_3D ( 'NONE', #33943, #50154, #7229 ) ;
#21385=DIRECTION ( 'NONE',  ( -1.000000000000000000, 0.000000000000000000, 0.000000000000000000 ) ) ;
#21407=ADVANCED_FACE ( 'NONE', ( #8541 ), #5694, .T. ) ;
#21427=ORIENTED_EDGE ( 'NONE', *, *, #34466, .F. ) ;
#21429=CARTESIAN_POINT ( 'NONE',  ( 53.24999999999999289, 27.99999999999998579, 4.000000000000000000 ) ) ;
#21435=ADVANCED_FACE ( 'NONE', ( #2495 ), #9231, .F. ) ;
#21440=CARTESIAN_POINT ( 'NONE',  ( 30.25000000000000711, 18.74999999999997868, 4.000000000000000000 ) ) ;
#21457=DIRECTION ( 'NONE',  ( 1.000000000000000000, 0.000000000000000000, 0.000000000000000000 ) ) ;
#21460=CARTESIAN_POINT ( 'NONE',  ( 1.000000000000000000, 1.000000000000000222, -3.000000000000000000 ) ) ;
#21462=DIRECTION ( 'NONE',  ( 0.000000000000000000, 1.000000000000000000, 0.000000000000000000 ) ) ;
#21466=CARTESIAN_POINT ( 'NONE',  ( 12.25000000000000355, 30.74999999999998579, 3.750000000000000000 ) ) ;
#21473=CYLINDRICAL_SURFACE ( 'NONE', #3440, 3.100000000000005418 ) ;
#21492=ORIENTED_EDGE ( 'NONE', *, *, #6351, .T. ) ;
#21508=CARTESIAN_POINT ( 'NONE',  ( 39.74999999999999289, 0.000000000000000000, 3.750000000000000000 ) ) ;
#21511=EDGE_CURVE ( 'NONE', #59375, #68323, #3394, .T. ) ;
#21525=VECTOR ( 'NONE', #54248, 1000.000000000000000 ) ;
#21544=EDGE_CURVE ( 'NONE', #31555, #31871, #50715, .T. ) ;
#21550=AXIS2_PLACEMENT_3D ( 'NONE', #29936, #34865, #56314 ) ;
#21584=DIRECTION ( 'NONE',  ( 1.000000000000000000, 0.000000000000000000, 0.000000000000000000 ) ) ;
#21601=ADVANCED_FACE ( 'NONE', ( #39446 ), #668, .T. ) ;
#21612=ORIENTED_EDGE ( 'NONE', *, *, #68089, .F. ) ;
#21619=ORIENTED_EDGE ( 'NONE', *, *, #56938, .T. ) ;
#21622=VERTEX_POINT ( 'NONE', #60849 ) ;
#21633=CARTESIAN_POINT ( 'NONE',  ( 66.74999999999998579, 34.24999999999999289, 4.000000000000000000 ) ) ;
#21682=DIRECTION ( 'NONE',  ( 0.000000000000000000, 0.000000000000000000, -1.000000000000000000 ) ) ;
#21684=EDGE_CURVE ( 'NONE', #38142, #32231, #38063, .T. ) ;
#21696=FACE_OUTER_BOUND ( 'NONE', #51917, .T. ) ;
#21699=CARTESIAN_POINT ( 'NONE',  ( 30.25000000000000711, 18.99999999999997868, -3.750000000000000000 ) ) ;
#21713=DIRECTION ( 'NONE',  ( -5.782411586589351722E-16, 1.000000000000000000, 0.000000000000000000 ) ) ;
#21725=LINE ( 'NONE', #59016, #38615 ) ;
#21738=LINE ( 'NONE', #63942, #66287 ) ;
#21741=AXIS2_PLACEMENT_3D ( 'NONE', #46456, #58344, #30556 ) ;
#21756=DIRECTION ( 'NONE',  ( 0.000000000000000000, 0.000000000000000000, -1.000000000000000000 ) ) ;
#21773=ORIENTED_EDGE ( 'NONE', *, *, #10511, .T. ) ;
#21780=ORIENTED_EDGE ( 'NONE', *, *, #65011, .F. ) ;
#21781=EDGE_CURVE ( 'NONE', #6197, #34838, #47333, .T. ) ;
#21787=CARTESIAN_POINT ( 'NONE',  ( 59.00000000000000000, 11.99999999999999822, -4.000000000000000000 ) ) ;
#21796=VECTOR ( 'NONE', #61914, 1000.000000000000000 ) ;
#21802=ORIENTED_EDGE ( 'NONE', *, *, #455, .T. ) ;
#21821=DIRECTION ( 'NONE',  ( -1.000000000000000000, 0.000000000000000000, 0.000000000000000000 ) ) ;
#21828=EDGE_CURVE ( 'NONE', #4257, #59022, #57436, .T. ) ;
#21830=DIRECTION ( 'NONE',  ( -0.000000000000000000, 0.000000000000000000, -1.000000000000000000 ) ) ;
#21833=AXIS2_PLACEMENT_3D ( 'NONE', #57671, #15139, #36617 ) ;
#21850=VECTOR ( 'NONE', #30828, 1000.000000000000000 ) ;
#21857=VECTOR ( 'NONE', #68636, 1000.000000000000000 ) ;
#21871=EDGE_CURVE ( 'NONE', #26545, #67683, #57314, .T. ) ;
#21894=DIRECTION ( 'NONE',  ( 0.000000000000000000, 0.000000000000000000, -1.000000000000000000 ) ) ;
#21916=DIRECTION ( 'NONE',  ( 0.000000000000000000, 0.000000000000000000, -1.000000000000000000 ) ) ;
#21920=AXIS2_PLACEMENT_3D ( 'NONE', #49955, #12271, #7019 ) ;
#21931=ADVANCED_FACE ( 'NONE', ( #61891 ), #48478, .T. ) ;
#21954=FACE_OUTER_BOUND ( 'NONE', #39920, .T. ) ;
#21955=CARTESIAN_POINT ( 'NONE',  ( 48.74999999999999289, 24.74999999999998579, -3.750000000000000000 ) ) ;
#22029=ORIENTED_EDGE ( 'NONE', *, *, #31120, .F. ) ;
#22039=CARTESIAN_POINT ( 'NONE',  ( 3.499999999999998668, 36.99999999999999289, 3.750000000000000000 ) ) ;
#22046=VECTOR ( 'NONE', #3721, 1000.000000000000000 ) ;
#22052=VECTOR ( 'NONE', #47819, 1000.000000000000000 ) ;
#22096=ORIENTED_EDGE ( 'NONE', *, *, #47973, .F. ) ;
#22107=EDGE_LOOP ( 'NONE', ( #50949, #1909, #46382 ) ) ;
#22108=ORIENTED_EDGE ( 'NONE', *, *, #50065, .F. ) ;
#22127=ORIENTED_EDGE ( 'NONE', *, *, #45632, .T. ) ;
#22169=DIRECTION ( 'NONE',  ( 0.000000000000000000, 0.000000000000000000, -1.000000000000000000 ) ) ;
#22173=VECTOR ( 'NONE', #13285, 1000.000000000000000 ) ;
#22174=EDGE_CURVE ( 'NONE', #66803, #31185, #56529, .T. ) ;
#22178=ADVANCED_FACE ( 'NONE', ( #23476 ), #18212, .T. ) ;
#22180=CARTESIAN_POINT ( 'NONE',  ( 21.50000000000000711, 21.74999999999998224, -3.750000000000000000 ) ) ;
#22191=ORIENTED_EDGE ( 'NONE', *, *, #44133, .T. ) ;
#22194=CARTESIAN_POINT ( 'NONE',  ( 68.99999999999998579, 0.000000000000000000, 3.000000000000000000 ) ) ;
#22202=VERTEX_POINT ( 'NONE', #18571 ) ;
#22204=EDGE_LOOP ( 'NONE', ( #31286, #22462, #53385, #45367 ) ) ;
#22212=ADVANCED_FACE ( 'NONE', ( #40053 ), #35449, .T. ) ;
#22240=VERTEX_POINT ( 'NONE', #2681 ) ;
#22246=ADVANCED_FACE ( 'NONE', ( #58271 ), #4697, .T. ) ;
#22249=ORIENTED_EDGE ( 'NONE', *, *, #39482, .T. ) ;
#22282=DIRECTION ( 'NONE',  ( 0.000000000000000000, 1.000000000000000000, 0.000000000000000000 ) ) ;
#22310=EDGE_LOOP ( 'NONE', ( #14352, #28417, #66569, #18984 ) ) ;
#22317=ADVANCED_FACE ( 'NONE', ( #63881 ), #57948, .T. ) ;
#22359=FACE_OUTER_BOUND ( 'NONE', #68876, .T. ) ;
#22361=PLANE ( 'NONE',  #40502 ) ;
#22362=DIRECTION ( 'NONE',  ( 0.000000000000000000, -1.000000000000000000, 0.000000000000000000 ) ) ;
#22378=CIRCLE ( 'NONE', #33622, 0.2500000000000002220 ) ;
#22387=DIRECTION ( 'NONE',  ( -0.000000000000000000, 0.000000000000000000, -1.000000000000000000 ) ) ;
#22390=DIRECTION ( 'NONE',  ( 1.000000000000000000, 0.000000000000000000, 0.000000000000000000 ) ) ;
#22395=EDGE_LOOP ( 'NONE', ( #3415, #27108, #30617, #4424 ) ) ;
#22398=CARTESIAN_POINT ( 'NONE',  ( 39.74999999999999289, 18.74999999999997868, 3.750000000000000000 ) ) ;
#22413=CARTESIAN_POINT ( 'NONE',  ( 3.499999999999999112, 34.24999999999998579, 3.750000000000000000 ) ) ;
#22422=CIRCLE ( 'NONE', #52719, 0.2500000000000002220 ) ;
#22439=DIRECTION ( 'NONE',  ( -0.7071067811865398012, 0.000000000000000000, -0.7071067811865552333 ) ) ;
#22458=ORIENTED_EDGE ( 'NONE', *, *, #38319, .T. ) ;
#22462=ORIENTED_EDGE ( 'NONE', *, *, #9812, .F. ) ;
#22464=SPHERICAL_SURFACE ( 'NONE', #15333, 0.2500000000000000000 ) ;
#22474=DIRECTION ( 'NONE',  ( -1.000000000000000000, 0.000000000000000000, 0.000000000000000000 ) ) ;
#22482=CARTESIAN_POINT ( 'NONE',  ( 44.00000000000000000, 21.74999999999998579, -3.750000000000000000 ) ) ;
#22488=AXIS2_PLACEMENT_3D ( 'NONE', #21460, #58407, #42615 ) ;
#22503=EDGE_CURVE ( 'NONE', #24854, #13223, #58676, .T. ) ;
#22509=CARTESIAN_POINT ( 'NONE',  ( 0.000000000000000000, 36.74999999999999289, 4.000000000000000000 ) ) ;
#22512=DIRECTION ( 'NONE',  ( 0.000000000000000000, 1.000000000000000000, 0.000000000000000000 ) ) ;
#22525=FACE_OUTER_BOUND ( 'NONE', #5734, .T. ) ;
#22530=VERTEX_POINT ( 'NONE', #26436 ) ;
#22534=AXIS2_PLACEMENT_3D ( 'NONE', #30292, #7820, #34905 ) ;
#22540=LINE ( 'NONE', #60169, #62890 ) ;
#22545=FACE_OUTER_BOUND ( 'NONE', #15625, .T. ) ;
#22580=LINE ( 'NONE', #16974, #35105 ) ;
#22601=EDGE_LOOP ( 'NONE', ( #45480, #58109, #66847, #10555 ) ) ;
#22605=CARTESIAN_POINT ( 'NONE',  ( 39.74999999999999289, 18.74999999999997868, -3.750000000000000000 ) ) ;
#22609=CIRCLE ( 'NONE', #6879, 3.600000000000005862 ) ;
#22625=AXIS2_PLACEMENT_3D ( 'NONE', #8298, #25488, #25151 ) ;
#22663=DIRECTION ( 'NONE',  ( 0.000000000000000000, 1.000000000000000000, 0.000000000000000000 ) ) ;
#22686=DIRECTION ( 'NONE',  ( -1.000000000000000000, 0.000000000000000000, 0.000000000000000000 ) ) ;
#22719=DIRECTION ( 'NONE',  ( -2.168404344971009361E-16, 1.000000000000000000, 0.000000000000000000 ) ) ;
#22730=ORIENTED_EDGE ( 'NONE', *, *, #568, .T. ) ;
#22732=ORIENTED_EDGE ( 'NONE', *, *, #64963, .F. ) ;
#22733=DIRECTION ( 'NONE',  ( -1.000000000000000000, 0.000000000000000000, 0.000000000000000000 ) ) ;
#22736=EDGE_CURVE ( 'NONE', #22202, #32850, #30596, .T. ) ;
#22744=CYLINDRICAL_SURFACE ( 'NONE', #55381, 0.2500000000000002220 ) ;
#22746=ORIENTED_EDGE ( 'NONE', *, *, #58223, .F. ) ;
#22768=FACE_OUTER_BOUND ( 'NONE', #24995, .T. ) ;
#22771=SPHERICAL_SURFACE ( 'NONE', #12803, 0.2500000000000000000 ) ;
#22772=DIRECTION ( 'NONE',  ( 0.000000000000000000, 0.000000000000000000, 1.000000000000000000 ) ) ;
#22781=CARTESIAN_POINT ( 'NONE',  ( 39.49999999999999289, 18.99999999999997868, 4.000000000000000000 ) ) ;
#22785=DIRECTION ( 'NONE',  ( 1.000000000000000000, 0.000000000000000000, 0.000000000000000000 ) ) ;
#22790=CARTESIAN_POINT ( 'NONE',  ( 52.75000000000000000, 25.24999999999998579, -4.000000000000000000 ) ) ;
#22806=DIRECTION ( 'NONE',  ( -0.000000000000000000, -0.000000000000000000, 1.000000000000000000 ) ) ;
#22808=ADVANCED_FACE ( 'NONE', ( #5574 ), #43297, .F. ) ;
#22817=DIRECTION ( 'NONE',  ( 0.000000000000000000, 0.000000000000000000, 1.000000000000000000 ) ) ;
#22821=CARTESIAN_POINT ( 'NONE',  ( 62.24999999999998579, 33.74999999999999289, -3.750000000000000000 ) ) ;
#22823=AXIS2_PLACEMENT_3D ( 'NONE', #40476, #34133, #29545 ) ;
#22824=DIRECTION ( 'NONE',  ( 1.000000000000000000, -0.000000000000000000, 0.000000000000000000 ) ) ;
#22828=VERTEX_POINT ( 'NONE', #15157 ) ;
#22833=CARTESIAN_POINT ( 'NONE',  ( 21.25000000000001066, 24.74999999999998224, -3.750000000000000000 ) ) ;
#22838=EDGE_LOOP ( 'NONE', ( #26509, #37252, #28682, #24308 ) ) ;
#22839=CIRCLE ( 'NONE', #60875, 0.2500000000000002220 ) ;
#22847=EDGE_CURVE ( 'NONE', #51729, #37003, #63309, .T. ) ;
#22876=EDGE_CURVE ( 'NONE', #52155, #39296, #63986, .T. ) ;
#22885=LINE ( 'NONE', #53708, #22928 ) ;
#22893=ADVANCED_FACE ( 'NONE', ( #31980 ), #5944, .T. ) ;
#22904=CARTESIAN_POINT ( 'NONE',  ( 3.499999999999998668, 36.74999999999999289, -3.750000000000000000 ) ) ;
#22918=EDGE_LOOP ( 'NONE', ( #33202, #12855, #19831, #27145 ) ) ;
#22926=CARTESIAN_POINT ( 'NONE',  ( 10.99999999999999645, 11.99999999999999289, 3.500000000000004885 ) ) ;
#22928=VECTOR ( 'NONE', #21351, 1000.000000000000000 ) ;
#22955=CARTESIAN_POINT ( 'NONE',  ( 44.25000000000000000, 0.000000000000000000, 4.000000000000000000 ) ) ;
#22959=EDGE_CURVE ( 'NONE', #61482, #44763, #43076, .T. ) ;
#22961=CIRCLE ( 'NONE', #56648, 0.2500000000000002220 ) ;
#22982=CARTESIAN_POINT ( 'NONE',  ( 30.75000000000001066, 15.99999999999997691, -3.750000000000000000 ) ) ;
#23047=EDGE_CURVE ( 'NONE', #39296, #13649, #10438, .T. ) ;
#23055=CARTESIAN_POINT ( 'NONE',  ( 55.89999999999999147, 11.99999999999999822, 3.499999999999992895 ) ) ;
#23056=DIRECTION ( 'NONE',  ( 0.000000000000000000, 0.000000000000000000, 1.000000000000000000 ) ) ;
#23071=DIRECTION ( 'NONE',  ( -0.000000000000000000, 0.000000000000000000, -1.000000000000000000 ) ) ;
#23079=CYLINDRICAL_SURFACE ( 'NONE', #56666, 0.2500000000000002220 ) ;
#23091=VECTOR ( 'NONE', #56985, 1000.000000000000000 ) ;
#23092=EDGE_CURVE ( 'NONE', #55156, #1652, #34403, .T. ) ;
#23096=CIRCLE ( 'NONE', #11829, 0.2500000000000002220 ) ;
#23112=AXIS2_PLACEMENT_3D ( 'NONE', #64280, #37256, #27660 ) ;
#23119=ADVANCED_FACE ( 'NONE', ( #55856 ), #7657, .F. ) ;
#23137=AXIS2_PLACEMENT_3D ( 'NONE', #42661, #32753, #58455 ) ;
#23145=CIRCLE ( 'NONE', #5137, 3.100000000000000533 ) ;
#23164=CARTESIAN_POINT ( 'NONE',  ( 26.25000000000001066, 18.74999999999997868, -4.000000000000000000 ) ) ;
#23167=ORIENTED_EDGE ( 'NONE', *, *, #58931, .T. ) ;
#23169=AXIS2_PLACEMENT_3D ( 'NONE', #39722, #38358, #43629 ) ;
#23175=DIRECTION ( 'NONE',  ( -0.000000000000000000, -0.000000000000000000, 1.000000000000000000 ) ) ;
#23196=EDGE_CURVE ( 'NONE', #9969, #41177, #30538, .T. ) ;
#23208=CARTESIAN_POINT ( 'NONE',  ( 55.89999999999999147, 11.99999999999999822, 3.499999999999992895 ) ) ;
#23222=AXIS2_PLACEMENT_3D ( 'NONE', #52526, #57074, #68338 ) ;
#23237=DIRECTION ( 'NONE',  ( 5.782411586589351722E-16, -1.000000000000000000, 0.000000000000000000 ) ) ;
#23241=DIRECTION ( 'NONE',  ( -0.000000000000000000, 0.000000000000000000, -1.000000000000000000 ) ) ;
#23250=CARTESIAN_POINT ( 'NONE',  ( 57.24999999999999289, 27.74999999999998934, 3.750000000000000000 ) ) ;
#23253=ORIENTED_EDGE ( 'NONE', *, *, #52149, .T. ) ;
#23254=DIRECTION ( 'NONE',  ( -1.000000000000000000, 0.000000000000000000, 0.000000000000000000 ) ) ;
#23275=LINE ( 'NONE', #26024, #49592 ) ;
#23282=EDGE_CURVE ( 'NONE', #61605, #62693, #22839, .T. ) ;
#23305=DIRECTION ( 'NONE',  ( -1.000000000000000000, 0.000000000000000000, 0.000000000000000000 ) ) ;
#23317=VERTEX_POINT ( 'NONE', #53370 ) ;
#23353=CARTESIAN_POINT ( 'NONE',  ( 17.00000000000000711, 25.24999999999998224, 3.750000000000000000 ) ) ;
#23369=CARTESIAN_POINT ( 'NONE',  ( 61.99999999999998579, 30.74999999999999289, -3.750000000000000000 ) ) ;
#23387=CARTESIAN_POINT ( 'NONE',  ( 0.000000000000000000, 0.000000000000000000, 4.000000000000000000 ) ) ;
#23392=ORIENTED_EDGE ( 'NONE', *, *, #17807, .T. ) ;
#23467=CARTESIAN_POINT ( 'NONE',  ( 25.75000000000001066, 21.74999999999998224, 4.000000000000000000 ) ) ;
#23471=AXIS2_PLACEMENT_3D ( 'NONE', #38340, #1284, #5921 ) ;
#23476=FACE_OUTER_BOUND ( 'NONE', #5909, .T. ) ;
#23493=CARTESIAN_POINT ( 'NONE',  ( 61.74999999999998579, 30.99999999999999289, -3.750000000000000000 ) ) ;
#23504=ADVANCED_FACE ( 'NONE', ( #62443 ), #56411, .F. ) ;
#23505=EDGE_LOOP ( 'NONE', ( #4614, #51380, #67187, #63725 ) ) ;
#23510=VECTOR ( 'NONE', #68102, 1000.000000000000000 ) ;
#23514=FACE_OUTER_BOUND ( 'NONE', #36933, .T. ) ;
#23516=CARTESIAN_POINT ( 'NONE',  ( 43.75000000000000000, 18.99999999999998224, 3.750000000000000000 ) ) ;
#23537=CARTESIAN_POINT ( 'NONE',  ( 53.00000000000000000, 25.24999999999998579, -3.750000000000000000 ) ) ;
#23586=CARTESIAN_POINT ( 'NONE',  ( 3.749999999999999556, 33.99999999999998579, 3.750000000000000000 ) ) ;
#23600=ORIENTED_EDGE ( 'NONE', *, *, #65439, .F. ) ;
#23700=EDGE_CURVE ( 'NONE', #27009, #28073, #42427, .T. ) ;
#23728=PLANE ( 'NONE',  #25257 ) ;
#23730=CARTESIAN_POINT ( 'NONE',  ( 30.75000000000001066, 16.24999999999997513, 4.000000000000000000 ) ) ;
#23740=LINE ( 'NONE', #44561, #28078 ) ;
#23749=CARTESIAN_POINT ( 'NONE',  ( 26.00000000000001066, 19.24999999999997868, -3.750000000000000000 ) ) ;
#23758=FACE_OUTER_BOUND ( 'NONE', #38433, .T. ) ;
#23793=CARTESIAN_POINT ( 'NONE',  ( 62.24999999999998579, 31.24999999999999289, 3.750000000000000000 ) ) ;
#23819=AXIS2_PLACEMENT_3D ( 'NONE', #49615, #976, #49971 ) ;
#23820=MECHANICAL_DESIGN_GEOMETRIC_PRESENTATION_REPRESENTATION('',(#1323),#62027);
#23824=AXIS2_PLACEMENT_3D ( 'NONE', #61117, #62146, #66753 ) ;
#23879=DIRECTION ( 'NONE',  ( 0.000000000000000000, 0.000000000000000000, 1.000000000000000000 ) ) ;
#23893=DIRECTION ( 'NONE',  ( -2.312964634635740689E-15, 1.000000000000000000, 0.000000000000000000 ) ) ;
#23907=EDGE_LOOP ( 'NONE', ( #39047, #14173, #26106, #17557 ) ) ;
#23926=LINE ( 'NONE', #67188, #45961 ) ;
#23929=ORIENTED_EDGE ( 'NONE', *, *, #16469, .F. ) ;
#23940=VERTEX_POINT ( 'NONE', #41634 ) ;
#23957=ADVANCED_FACE ( 'NONE', ( #36377 ), #52533, .T. ) ;
#23964=CARTESIAN_POINT ( 'NONE',  ( 21.75000000000001066, 22.24999999999998224, 4.000000000000000000 ) ) ;
#23965=DIRECTION ( 'NONE',  ( -5.782411586589351722E-16, 1.000000000000000000, 0.000000000000000000 ) ) ;
#23969=CIRCLE ( 'NONE', #22823, 0.2500000000000002220 ) ;
#23983=FACE_OUTER_BOUND ( 'NONE', #12936, .T. ) ;
#23993=AXIS2_PLACEMENT_3D ( 'NONE', #47179, #68599, #13734 ) ;
#23995=DIRECTION ( 'NONE',  ( -0.000000000000000000, -0.000000000000000000, 1.000000000000000000 ) ) ;
#24008=LINE ( 'NONE', #66936, #44920 ) ;
#24021=ORIENTED_EDGE ( 'NONE', *, *, #5273, .F. ) ;
#24038=EDGE_CURVE ( 'NONE', #34838, #33800, #61963, .T. ) ;
#24042=CARTESIAN_POINT ( 'NONE',  ( 25.75000000000001066, 21.74999999999998224, -3.750000000000000000 ) ) ;
#24065=AXIS2_PLACEMENT_3D ( 'NONE', #4218, #58088, #20436 ) ;
#24068=CARTESIAN_POINT ( 'NONE',  ( 3.249999999999999556, 34.24999999999998579, 3.750000000000000000 ) ) ;
#24073=LINE ( 'NONE', #8255, #49348 ) ;
#24081=EDGE_CURVE ( 'NONE', #7106, #35167, #29425, .T. ) ;
#24090=AXIS2_PLACEMENT_3D ( 'NONE', #62223, #24244, #66466 ) ;
#24096=LINE ( 'NONE', #51518, #6654 ) ;
#24103=AXIS2_PLACEMENT_3D ( 'NONE', #37361, #48243, #21830 ) ;
#24105=CARTESIAN_POINT ( 'NONE',  ( 44.25000000000000000, 21.74999999999998579, -3.750000000000000000 ) ) ;
#24124=VECTOR ( 'NONE', #35358, 1000.000000000000000 ) ;
#24132=VECTOR ( 'NONE', #42665, 1000.000000000000000 ) ;
#24150=DIRECTION ( 'NONE',  ( -1.000000000000000000, -7.709882115452468306E-16, 0.000000000000000000 ) ) ;
#24161=UNCERTAINTY_MEASURE_WITH_UNIT (LENGTH_MEASURE( 1.000000000000000082E-05 ), #18113, 'distance_accuracy_value', 'NONE');
#24180=DIRECTION ( 'NONE',  ( 5.782411586589351722E-16, -1.000000000000000000, 0.000000000000000000 ) ) ;
#24218=DIRECTION ( 'NONE',  ( 0.000000000000000000, 0.000000000000000000, -1.000000000000000000 ) ) ;
#24228=EDGE_CURVE ( 'NONE', #34547, #47241, #58606, .T. ) ;
#24240=ADVANCED_FACE ( 'NONE', ( #15343 ), #63129, .F. ) ;
#24244=DIRECTION ( 'NONE',  ( 0.000000000000000000, 0.000000000000000000, -1.000000000000000000 ) ) ;
#24248=AXIS2_PLACEMENT_3D ( 'NONE', #21276, #53326, #32520 ) ;
#24250=VERTEX_POINT ( 'NONE', #69127 ) ;
#24253=VECTOR ( 'NONE', #31693, 1000.000000000000000 ) ;
#24274=ORIENTED_EDGE ( 'NONE', *, *, #10087, .T. ) ;
#24290=ORIENTED_EDGE ( 'NONE', *, *, #59802, .F. ) ;
#24308=ORIENTED_EDGE ( 'NONE', *, *, #8684, .T. ) ;
#24310=DIRECTION ( 'NONE',  ( 0.000000000000000000, 0.000000000000000000, -1.000000000000000000 ) ) ;
#24327=PLANE ( 'NONE',  #12305 ) ;
#24335=ORIENTED_EDGE ( 'NONE', *, *, #59802, .T. ) ;
#24341=CARTESIAN_POINT ( 'NONE',  ( -1.908195823574483386E-14, 24.74999999999996803, 3.750000000000000000 ) ) ;
#24343=ORIENTED_EDGE ( 'NONE', *, *, #68006, .T. ) ;
#24351=CYLINDRICAL_SURFACE ( 'NONE', #53373, 0.2500000000000002220 ) ;
#24354=DIRECTION ( 'NONE',  ( 1.000000000000000000, 0.000000000000000000, 0.000000000000000000 ) ) ;
#24403=CARTESIAN_POINT ( 'NONE',  ( 69.99999999999998579, 36.75000000000000000, -3.000000000000000000 ) ) ;
#24414=EDGE_LOOP ( 'NONE', ( #21233, #16688, #35220, #42334 ) ) ;
#24425=EDGE_LOOP ( 'NONE', ( #54467, #42370, #13719, #43401 ) ) ;
#24442=VERTEX_POINT ( 'NONE', #13127 ) ;
#24459=CARTESIAN_POINT ( 'NONE',  ( 0.000000000000000000, 21.74999999999998579, 4.000000000000000000 ) ) ;
#24476=VERTEX_POINT ( 'NONE', #18759 ) ;
#24484=DIRECTION ( 'NONE',  ( 0.000000000000000000, -0.000000000000000000, 1.000000000000000000 ) ) ;
#24504=ORIENTED_EDGE ( 'NONE', *, *, #41265, .F. ) ;
#24517=ORIENTED_EDGE ( 'NONE', *, *, #45528, .T. ) ;
#24525=AXIS2_PLACEMENT_3D ( 'NONE', #42467, #10427, #31856 ) ;
#24530=DIRECTION ( 'NONE',  ( -0.000000000000000000, 1.000000000000000000, -0.000000000000000000 ) ) ;
#24540=DIRECTION ( 'NONE',  ( -5.782411586589351722E-16, 1.000000000000000000, 0.000000000000000000 ) ) ;
#24548=DIRECTION ( 'NONE',  ( 0.000000000000000000, 0.000000000000000000, -1.000000000000000000 ) ) ;
#24574=FACE_OUTER_BOUND ( 'NONE', #48944, .T. ) ;
#24587=VERTEX_POINT ( 'NONE', #30002 ) ;
#24591=DIRECTION ( 'NONE',  ( -1.000000000000000000, 0.000000000000000000, 0.000000000000000000 ) ) ;
#24593=FACE_OUTER_BOUND ( 'NONE', #43366, .T. ) ;
#24602=LINE ( 'NONE', #68244, #53462 ) ;
#24621=VERTEX_POINT ( 'NONE', #1035 ) ;
#24628=VECTOR ( 'NONE', #40207, 1000.000000000000000 ) ;
#24682=CARTESIAN_POINT ( 'NONE',  ( 53.00000000000000000, 25.24999999999998579, 3.750000000000000000 ) ) ;
#24684=EDGE_CURVE ( 'NONE', #28127, #39701, #22580, .T. ) ;
#24716=DIRECTION ( 'NONE',  ( 1.000000000000000000, 7.709882115452469292E-16, 0.000000000000000000 ) ) ;
#24723=PLANE ( 'NONE',  #26870 ) ;
#24724=VECTOR ( 'NONE', #15869, 1000.000000000000000 ) ;
#24743=AXIS2_PLACEMENT_3D ( 'NONE', #57300, #35158, #9128 ) ;
#24755=COLOUR_RGB ( '', 0.72549020, 0.75294118, 0.79215686) ;
#24768=CYLINDRICAL_SURFACE ( 'NONE', #52232, 1.000000000000000000 ) ;
#24779=EDGE_CURVE ( 'NONE', #19343, #37744, #4777, .T. ) ;
#24784=ORIENTED_EDGE ( 'NONE', *, *, #54775, .F. ) ;
#24811=ADVANCED_FACE ( 'NONE', ( #69388 ), #5681, .T. ) ;
#24820=AXIS2_PLACEMENT_3D ( 'NONE', #53079, #32291, #58018 ) ;
#24854=VERTEX_POINT ( 'NONE', #39141 ) ;
#24876=EDGE_LOOP ( 'NONE', ( #56038, #7743, #61989, #61702 ) ) ;
#24882=ORIENTED_EDGE ( 'NONE', *, *, #54170, .F. ) ;
#24892=DIRECTION ( 'NONE',  ( -1.000000000000000000, 0.000000000000000000, 0.000000000000000000 ) ) ;
#24898=CIRCLE ( 'NONE', #12545, 0.2500000000000002220 ) ;
#24899=( LENGTH_UNIT ( ) NAMED_UNIT ( * ) SI_UNIT ( .MILLI., .METRE. ) );
#24900=CARTESIAN_POINT ( 'NONE',  ( 30.25000000000000711, 18.74999999999997868, -3.750000000000000000 ) ) ;
#24935=VECTOR ( 'NONE', #1116, 1000.000000000000000 ) ;
#24937=UNCERTAINTY_MEASURE_WITH_UNIT (LENGTH_MEASURE( 1.000000000000000082E-05 ), #46089, 'distance_accuracy_value', 'NONE');
#24947=AXIS2_PLACEMENT_3D ( 'NONE', #33905, #55372, #2175 ) ;
#24949=FACE_OUTER_BOUND ( 'NONE', #17546, .T. ) ;
#24986=DIRECTION ( 'NONE',  ( -1.000000000000000000, 0.000000000000000000, 0.000000000000000000 ) ) ;
#24992=DIRECTION ( 'NONE',  ( 2.312964634635740689E-15, -1.000000000000000000, 0.000000000000000000 ) ) ;
#24995=EDGE_LOOP ( 'NONE', ( #40000, #7234, #2869, #27350 ) ) ;
#25005=CYLINDRICAL_SURFACE ( 'NONE', #21550, 0.2500000000000002220 ) ;
#25023=EDGE_CURVE ( 'NONE', #59058, #36322, #63669, .T. ) ;
#25026=FACE_OUTER_BOUND ( 'NONE', #13838, .T. ) ;
#25027=AXIS2_PLACEMENT_3D ( 'NONE', #48487, #38633, #60036 ) ;
#25028=DIRECTION ( 'NONE',  ( -1.156482317317870344E-15, -1.000000000000000000, 0.000000000000000000 ) ) ;
#25054=ORIENTED_EDGE ( 'NONE', *, *, #24779, .F. ) ;
#25067=DIRECTION ( 'NONE',  ( 0.000000000000000000, 1.000000000000000000, 0.000000000000000000 ) ) ;
#25077=CIRCLE ( 'NONE', #16119, 0.2500000000000002220 ) ;
#25088=DIRECTION ( 'NONE',  ( 0.000000000000000000, 1.000000000000000000, 0.000000000000000000 ) ) ;
#25098=VECTOR ( 'NONE', #24992, 1000.000000000000000 ) ;
#25102=EDGE_LOOP ( 'NONE', ( #59275, #58933, #42241 ) ) ;
#25111=ORIENTED_EDGE ( 'NONE', *, *, #2415, .F. ) ;
#25122=AXIS2_PLACEMENT_3D ( 'NONE', #46108, #55589, #28839 ) ;
#25145=ORIENTED_EDGE ( 'NONE', *, *, #17291, .F. ) ;
#25151=DIRECTION ( 'NONE',  ( 1.000000000000000000, 0.000000000000000000, 0.000000000000000000 ) ) ;
#25160=VECTOR ( 'NONE', #52613, 1000.000000000000000 ) ;
#25169=EDGE_CURVE ( 'NONE', #68919, #61482, #24898, .T. ) ;
#25179=LINE ( 'NONE', #9010, #36373 ) ;
#25194=CARTESIAN_POINT ( 'NONE',  ( 30.25000000000000711, 18.74999999999997868, -3.750000000000000000 ) ) ;
#25213=LINE ( 'NONE', #46733, #61145 ) ;
#25223=ORIENTED_EDGE ( 'NONE', *, *, #65758, .T. ) ;
#25224=EDGE_LOOP ( 'NONE', ( #59994, #64341, #17951 ) ) ;
#25231=VECTOR ( 'NONE', #50443, 1000.000000000000000 ) ;
#25257=AXIS2_PLACEMENT_3D ( 'NONE', #13162, #29704, #2570 ) ;
#25261=ORIENTED_EDGE ( 'NONE', *, *, #58396, .T. ) ;
#25268=CARTESIAN_POINT ( 'NONE',  ( 44.00000000000000000, 19.24999999999998224, 3.750000000000000000 ) ) ;
#25301=ORIENTED_EDGE ( 'NONE', *, *, #63216, .T. ) ;
#25322=EDGE_LOOP ( 'NONE', ( #63022, #7701, #17141, #32102 ) ) ;
#25325=CARTESIAN_POINT ( 'NONE',  ( 17.00000000000000711, 25.24999999999998224, -4.000000000000000000 ) ) ;
#25327=EDGE_CURVE ( 'NONE', #29227, #37744, #40656, .T. ) ;
#25333=DIRECTION ( 'NONE',  ( 0.000000000000000000, -1.000000000000000000, 0.000000000000000000 ) ) ;
#25334=VECTOR ( 'NONE', #29552, 1000.000000000000000 ) ;
#25363=CARTESIAN_POINT ( 'NONE',  ( 66.24999999999998579, 33.99999999999999289, -4.000000000000000000 ) ) ;
#25365=CARTESIAN_POINT ( 'NONE',  ( 53.00000000000000000, 25.24999999999998579, -3.750000000000000000 ) ) ;
#25387=ORIENTED_EDGE ( 'NONE', *, *, #10981, .F. ) ;
#25399=DIRECTION ( 'NONE',  ( 0.000000000000000000, 0.000000000000000000, -1.000000000000000000 ) ) ;
#25425=CARTESIAN_POINT ( 'NONE',  ( 43.75000000000000000, 18.74999999999998224, -4.000000000000000000 ) ) ;
#25430=VERTEX_POINT ( 'NONE', #33563 ) ;
#25449=ADVANCED_FACE ( 'NONE', ( #42191 ), #44519, .F. ) ;
#25468=LINE ( 'NONE', #52582, #26002 ) ;
#25473=VERTEX_POINT ( 'NONE', #6141 ) ;
#25488=DIRECTION ( 'NONE',  ( 0.000000000000000000, 0.000000000000000000, 1.000000000000000000 ) ) ;
#25521=CIRCLE ( 'NONE', #29994, 3.100000000000000533 ) ;
#25535=CARTESIAN_POINT ( 'NONE',  ( 0.000000000000000000, 1.000000000000000222, -3.000000000000000000 ) ) ;
#25545=DIRECTION ( 'NONE',  ( -1.156482317317870344E-15, 1.000000000000000000, 0.000000000000000000 ) ) ;
#25558=VERTEX_POINT ( 'NONE', #8234 ) ;
#25571=VERTEX_POINT ( 'NONE', #13480 ) ;
#25584=CIRCLE ( 'NONE', #28939, 3.100000000000000533 ) ;
#25594=DIRECTION ( 'NONE',  ( -1.000000000000000000, 0.000000000000000000, 0.000000000000000000 ) ) ;
#25621=SURFACE_STYLE_FILL_AREA ( #3084 ) ;
#25622=EDGE_LOOP ( 'NONE', ( #51210, #11555, #1601, #15096 ) ) ;
#25650=EDGE_CURVE ( 'NONE', #12327, #38988, #69062, .T. ) ;
#25666=CIRCLE ( 'NONE', #9980, 0.2500000000000002220 ) ;
#25668=ORIENTED_EDGE ( 'NONE', *, *, #61941, .T. ) ;
#25678=CARTESIAN_POINT ( 'NONE',  ( 57.49999999999999289, 28.24999999999998934, 3.750000000000000000 ) ) ;
#25685=EDGE_LOOP ( 'NONE', ( #48892, #62241, #1003, #53397 ) ) ;
#25688=AXIS2_PLACEMENT_3D ( 'NONE', #66502, #40836, #66861 ) ;
#25693=EDGE_CURVE ( 'NONE', #57903, #9427, #11452, .T. ) ;
#25697=TOROIDAL_SURFACE ( 'NONE', #63901, 0.5000000000000000000, 0.2500000000000000000 ) ;
#25719=ORIENTED_EDGE ( 'NONE', *, *, #67033, .F. ) ;
#25723=FACE_OUTER_BOUND ( 'NONE', #17054, .T. ) ;
#25735=AXIS2_PLACEMENT_3D ( 'NONE', #13157, #34975, #56426 ) ;
#25736=EDGE_CURVE ( 'NONE', #14037, #69269, #51990, .T. ) ;
#25747=FACE_OUTER_BOUND ( 'NONE', #38009, .T. ) ;
#25757=VECTOR ( 'NONE', #52213, 1000.000000000000000 ) ;
#25796=TOROIDAL_SURFACE ( 'NONE', #62838, 0.5000000000000000000, 0.2500000000000000000 ) ;
#25806=DIRECTION ( 'NONE',  ( 0.000000000000000000, 0.000000000000000000, 1.000000000000000000 ) ) ;
#25813=DIRECTION ( 'NONE',  ( 1.000000000000000000, 0.000000000000000000, 0.000000000000000000 ) ) ;
#25814=CARTESIAN_POINT ( 'NONE',  ( 66.74999999999998579, 36.75000000000000000, 3.750000000000000000 ) ) ;
#25819=LINE ( 'NONE', #46651, #58938 ) ;
#25832=ORIENTED_EDGE ( 'NONE', *, *, #8868, .F. ) ;
#25838=CIRCLE ( 'NONE', #65154, 0.2500000000000002220 ) ;
#25856=CYLINDRICAL_SURFACE ( 'NONE', #29662, 0.2500000000000002220 ) ;
#25868=CARTESIAN_POINT ( 'NONE',  ( 21.25000000000001066, 24.74999999999998224, 4.000000000000000000 ) ) ;
#25896=FACE_OUTER_BOUND ( 'NONE', #67149, .T. ) ;
#25904=VERTEX_POINT ( 'NONE', #65853 ) ;
#25914=ORIENTED_EDGE ( 'NONE', *, *, #21511, .T. ) ;
#25917=VECTOR ( 'NONE', #3425, 1000.000000000000000 ) ;
#25922=AXIS2_PLACEMENT_3D ( 'NONE', #27678, #17536, #54434 ) ;
#25934=CARTESIAN_POINT ( 'NONE',  ( 69.99999999999998579, 8.572527594031471415E-15, 4.000000000000000000 ) ) ;
#25950=EDGE_CURVE ( 'NONE', #22828, #51066, #17686, .T. ) ;
#25972=ORIENTED_EDGE ( 'NONE', *, *, #10731, .F. ) ;
#26002=VECTOR ( 'NONE', #68753, 1000.000000000000000 ) ;
#26024=CARTESIAN_POINT ( 'NONE',  ( 57.49999999999999289, 27.99999999999998934, 3.750000000000000000 ) ) ;
#26037=DIRECTION ( 'NONE',  ( 0.000000000000000000, -1.000000000000000000, 0.000000000000000000 ) ) ;
#26045=DIRECTION ( 'NONE',  ( 0.000000000000000000, 0.000000000000000000, -1.000000000000000000 ) ) ;
#26046=CARTESIAN_POINT ( 'NONE',  ( 59.00000000000000000, 11.99999999999999822, 4.000000000000000000 ) ) ;
#26050=CARTESIAN_POINT ( 'NONE',  ( 1.000000000000000000, 36.74999999999999289, -4.000000000000000000 ) ) ;
#26067=AXIS2_PLACEMENT_3D ( 'NONE', #5085, #3663, #52947 ) ;
#26072=AXIS2_PLACEMENT_3D ( 'NONE', #11316, #6720, #12009 ) ;
#26082=DIRECTION ( 'NONE',  ( -1.000000000000000000, 0.000000000000000000, 0.000000000000000000 ) ) ;
#26086=CYLINDRICAL_SURFACE ( 'NONE', #68048, 0.2500000000000002220 ) ;
#26096=ORIENTED_EDGE ( 'NONE', *, *, #334, .F. ) ;
#26102=ORIENTED_EDGE ( 'NONE', *, *, #36879, .F. ) ;
#26106=ORIENTED_EDGE ( 'NONE', *, *, #37229, .T. ) ;
#26119=EDGE_CURVE ( 'NONE', #64812, #57523, #28385, .T. ) ;
#26127=ADVANCED_FACE ( 'NONE', ( #68984 ), #64023, .T. ) ;
#26151=DIRECTION ( 'NONE',  ( 0.000000000000000000, -1.000000000000000000, 0.000000000000000000 ) ) ;
#26163=DIRECTION ( 'NONE',  ( -0.000000000000000000, -0.000000000000000000, -1.000000000000000000 ) ) ;
#26179=DIRECTION ( 'NONE',  ( 0.000000000000000000, 0.000000000000000000, -1.000000000000000000 ) ) ;
#26210=EDGE_CURVE ( 'NONE', #67943, #49467, #27746, .T. ) ;
#26238=ADVANCED_FACE ( 'NONE', ( #10577 ), #53488, .T. ) ;
#26241=AXIS2_PLACEMENT_3D ( 'NONE', #35733, #50867, #2965 ) ;
#26258=ORIENTED_EDGE ( 'NONE', *, *, #44149, .T. ) ;
#26289=ORIENTED_EDGE ( 'NONE', *, *, #68333, .T. ) ;
#26298=DIRECTION ( 'NONE',  ( -1.000000000000000000, 0.000000000000000000, 0.000000000000000000 ) ) ;
#26336=CARTESIAN_POINT ( 'NONE',  ( 66.74999999999998579, 36.75000000000000000, -4.000000000000000000 ) ) ;
#26346=EDGE_LOOP ( 'NONE', ( #24882, #45365, #26289, #41794 ) ) ;
#26349=DIRECTION ( 'NONE',  ( 0.000000000000000000, -0.000000000000000000, -1.000000000000000000 ) ) ;
#26351=EDGE_LOOP ( 'NONE', ( #58266, #53891, #38385 ) ) ;
#26361=CYLINDRICAL_SURFACE ( 'NONE', #66956, 1.000000000000000000 ) ;
#26375=CARTESIAN_POINT ( 'NONE',  ( 3.749999999999999556, 33.99999999999998579, -3.750000000000000000 ) ) ;
#26382=VERTEX_POINT ( 'NONE', #25268 ) ;
#26385=EDGE_CURVE ( 'NONE', #21325, #15190, #63255, .T. ) ;
#26389=ORIENTED_EDGE ( 'NONE', *, *, #61146, .T. ) ;
#26414=VECTOR ( 'NONE', #33258, 1000.000000000000000 ) ;
#26436=CARTESIAN_POINT ( 'NONE',  ( 48.49999999999999289, 24.74999999999998579, -3.750000000000000000 ) ) ;
#26452=CARTESIAN_POINT ( 'NONE',  ( 12.25000000000000355, 30.99999999999998579, 3.750000000000000000 ) ) ;
#26460=ORIENTED_EDGE ( 'NONE', *, *, #45415, .T. ) ;
#26463=SURFACE_SIDE_STYLE ('',( #69390 ) ) ;
#26467=DIRECTION ( 'NONE',  ( 1.000000000000000000, 7.709882115452469292E-16, 0.000000000000000000 ) ) ;
#26479=ORIENTED_EDGE ( 'NONE', *, *, #15850, .F. ) ;
#26488=EDGE_CURVE ( 'NONE', #7947, #27455, #21725, .T. ) ;
#26491=VERTEX_POINT ( 'NONE', #64284 ) ;
#26509=ORIENTED_EDGE ( 'NONE', *, *, #35664, .F. ) ;
#26511=DIRECTION ( 'NONE',  ( -1.000000000000000000, 0.000000000000000000, 0.000000000000000000 ) ) ;
#26524=ORIENTED_EDGE ( 'NONE', *, *, #9812, .T. ) ;
#26536=SURFACE_SIDE_STYLE ('',( #20218 ) ) ;
#26539=EDGE_CURVE ( 'NONE', #823, #37329, #31929, .T. ) ;
#26540=VERTEX_POINT ( 'NONE', #22413 ) ;
#26545=VERTEX_POINT ( 'NONE', #27664 ) ;
#26563=ORIENTED_EDGE ( 'NONE', *, *, #59471, .F. ) ;
#26564=EDGE_CURVE ( 'NONE', #38988, #31454, #11510, .T. ) ;
#26566=DIRECTION ( 'NONE',  ( 0.000000000000000000, 1.000000000000000000, -0.000000000000000000 ) ) ;
#26586=CARTESIAN_POINT ( 'NONE',  ( 3.749999999999999556, 34.24999999999998579, 3.750000000000000000 ) ) ;
#26589=EDGE_LOOP ( 'NONE', ( #19444, #32779, #46029, #56820 ) ) ;
#26599=CARTESIAN_POINT ( 'NONE',  ( 68.99999999999998579, 8.572527594031471415E-15, -3.000000000000000000 ) ) ;
#26610=VECTOR ( 'NONE', #16290, 1000.000000000000000 ) ;
#26618=CARTESIAN_POINT ( 'NONE',  ( 17.25000000000000711, 24.74999999999997868, 4.000000000000000000 ) ) ;
#26635=EDGE_CURVE ( 'NONE', #25571, #16642, #13868, .T. ) ;
#26650=EDGE_LOOP ( 'NONE', ( #11728, #9670, #3229, #35176 ) ) ;
#26667=DIRECTION ( 'NONE',  ( -1.000000000000000000, 0.000000000000000000, 0.000000000000000000 ) ) ;
#26680=DIRECTION ( 'NONE',  ( -1.000000000000000000, 0.000000000000000000, 0.000000000000000000 ) ) ;
#26705=DIRECTION ( 'NONE',  ( -0.000000000000000000, 1.000000000000000000, -0.000000000000000000 ) ) ;
#26707=DIRECTION ( 'NONE',  ( -0.000000000000000000, 0.000000000000000000, -1.000000000000000000 ) ) ;
#26709=CIRCLE ( 'NONE', #66033, 0.5000000000000004441 ) ;
#26773=SURFACE_STYLE_FILL_AREA ( #58137 ) ;
#26786=ORIENTED_EDGE ( 'NONE', *, *, #6524, .F. ) ;
#26804=ADVANCED_FACE ( 'NONE', ( #18536 ), #22771, .T. ) ;
#26827=CARTESIAN_POINT ( 'NONE',  ( 39.74999999999999289, 18.74999999999997868, 3.750000000000000000 ) ) ;
#26854=ORIENTED_EDGE ( 'NONE', *, *, #3541, .T. ) ;
#26870=AXIS2_PLACEMENT_3D ( 'NONE', #18773, #36394, #52203 ) ;
#26872=CIRCLE ( 'NONE', #60573, 0.2500000000000002220 ) ;
#26950=DIRECTION ( 'NONE',  ( -0.000000000000000000, -0.000000000000000000, 1.000000000000000000 ) ) ;
#26975=VECTOR ( 'NONE', #47410, 1000.000000000000000 ) ;
#26979=LINE ( 'NONE', #27333, #10168 ) ;
#27009=VERTEX_POINT ( 'NONE', #42454 ) ;
#27023=ORIENTED_EDGE ( 'NONE', *, *, #6351, .F. ) ;
#27029=CARTESIAN_POINT ( 'NONE',  ( 57.74999999999998579, 30.74999999999999289, 3.750000000000000000 ) ) ;
#27055=CARTESIAN_POINT ( 'NONE',  ( 48.74999999999999289, 24.99999999999998579, 4.000000000000000000 ) ) ;
#27059=VECTOR ( 'NONE', #22439, 1000.000000000000114 ) ;
#27066=AXIS2_PLACEMENT_3D ( 'NONE', #47394, #26566, #20617 ) ;
#27075=AXIS2_PLACEMENT_3D ( 'NONE', #67891, #61527, #3822 ) ;
#27108=ORIENTED_EDGE ( 'NONE', *, *, #66472, .T. ) ;
#27124=EDGE_CURVE ( 'NONE', #39296, #34249, #22961, .T. ) ;
#27125=DIRECTION ( 'NONE',  ( 1.156482317317870344E-15, 1.000000000000000000, 0.000000000000000000 ) ) ;
#27128=FACE_OUTER_BOUND ( 'NONE', #60886, .T. ) ;
#27145=ORIENTED_EDGE ( 'NONE', *, *, #58223, .T. ) ;
#27173=ADVANCED_FACE ( 'NONE', ( #33578 ), #33243, .T. ) ;
#27185=DIRECTION ( 'NONE',  ( -0.000000000000000000, 0.000000000000000000, -1.000000000000000000 ) ) ;
#27212=EDGE_CURVE ( 'NONE', #43779, #69071, #8403, .T. ) ;
#27231=AXIS2_PLACEMENT_3D ( 'NONE', #1213, #11828, #27976 ) ;
#27236=DIRECTION ( 'NONE',  ( 0.000000000000000000, -1.000000000000000000, 0.000000000000000000 ) ) ;
#27237=DIRECTION ( 'NONE',  ( 0.000000000000000000, 0.000000000000000000, 1.000000000000000000 ) ) ;
#27263=CIRCLE ( 'NONE', #14978, 0.2500000000000002220 ) ;
#27271=DIRECTION ( 'NONE',  ( 0.000000000000000000, 0.000000000000000000, -1.000000000000000000 ) ) ;
#27283=EDGE_CURVE ( 'NONE', #29672, #44704, #19740, .T. ) ;
#27287=CARTESIAN_POINT ( 'NONE',  ( 12.75000000000000533, 27.99999999999998224, -3.750000000000000000 ) ) ;
#27297=ADVANCED_FACE ( 'NONE', ( #65428 ), #11261, .F. ) ;
#27302=DIRECTION ( 'NONE',  ( 0.000000000000000000, 1.000000000000000000, 0.000000000000000000 ) ) ;
#27312=FACE_OUTER_BOUND ( 'NONE', #56853, .T. ) ;
#27318=DIRECTION ( 'NONE',  ( 0.000000000000000000, 0.000000000000000000, -1.000000000000000000 ) ) ;
#27333=CARTESIAN_POINT ( 'NONE',  ( 62.24999999999998579, 33.74999999999999289, -4.000000000000000000 ) ) ;
#27350=ORIENTED_EDGE ( 'NONE', *, *, #65266, .F. ) ;
#27359=VERTEX_POINT ( 'NONE', #59799 ) ;
#27380=VECTOR ( 'NONE', #9908, 1000.000000000000000 ) ;
#27410=DIRECTION ( 'NONE',  ( 0.000000000000000000, 1.000000000000000000, 0.000000000000000000 ) ) ;
#27414=FACE_OUTER_BOUND ( 'NONE', #16963, .T. ) ;
#27418=DIRECTION ( 'NONE',  ( 0.000000000000000000, 1.000000000000000000, 0.000000000000000000 ) ) ;
#27426=VECTOR ( 'NONE', #43697, 1000.000000000000000 ) ;
#27442=DIRECTION ( 'NONE',  ( -0.000000000000000000, 0.000000000000000000, -1.000000000000000000 ) ) ;
#27451=ORIENTED_EDGE ( 'NONE', *, *, #19785, .F. ) ;
#27455=VERTEX_POINT ( 'NONE', #29863 ) ;
#27458=ORIENTED_EDGE ( 'NONE', *, *, #47327, .T. ) ;
#27481=CARTESIAN_POINT ( 'NONE',  ( 12.75000000000000533, 27.99999999999998224, 3.750000000000000000 ) ) ;
#27509=AXIS2_PLACEMENT_3D ( 'NONE', #28757, #22817, #54790 ) ;
#27532=DIRECTION ( 'NONE',  ( 0.7071067811865398012, 8.659560562354839181E-17, -0.7071067811865552333 ) ) ;
#27539=CARTESIAN_POINT ( 'NONE',  ( 10.99999999999999645, 11.99999999999999289, -4.000000000000000000 ) ) ;
#27550=ADVANCED_FACE ( 'NONE', ( #42900 ), #6176, .T. ) ;
#27582=AXIS2_PLACEMENT_3D ( 'NONE', #7129, #28555, #23305 ) ;
#27636=DIRECTION ( 'NONE',  ( -1.000000000000000000, 0.000000000000000000, 0.000000000000000000 ) ) ;
#27638=FACE_OUTER_BOUND ( 'NONE', #68, .T. ) ;
#27660=DIRECTION ( 'NONE',  ( 1.000000000000000000, 0.000000000000000000, 0.000000000000000000 ) ) ;
#27661=EDGE_LOOP ( 'NONE', ( #37074, #12564, #39805 ) ) ;
#27662=CARTESIAN_POINT ( 'NONE',  ( 21.25000000000001066, 24.74999999999998224, 3.750000000000000000 ) ) ;
#27664=CARTESIAN_POINT ( 'NONE',  ( 21.50000000000001066, 24.74999999999998224, -3.750000000000000000 ) ) ;
#27678=CARTESIAN_POINT ( 'NONE',  ( 52.75000000000000000, 24.74999999999998224, 3.750000000000000000 ) ) ;
#27693=EDGE_LOOP ( 'NONE', ( #63764, #12273, #59506, #18979 ) ) ;
#27720=ORIENTED_EDGE ( 'NONE', *, *, #15043, .T. ) ;
#27740=AXIS2_PLACEMENT_3D ( 'NONE', #69643, #69318, #11247 ) ;
#27746=LINE ( 'NONE', #22509, #11605 ) ;
#27747=AXIS2_PLACEMENT_3D ( 'NONE', #6625, #17247, #65740 ) ;
#27756=DIRECTION ( 'NONE',  ( -1.000000000000000000, 0.000000000000000000, 0.000000000000000000 ) ) ;
#27758=ADVANCED_FACE ( 'NONE', ( #36732 ), #31046, .T. ) ;
#27763=CARTESIAN_POINT ( 'NONE',  ( 12.25000000000000355, 30.74999999999998579, -3.750000000000000000 ) ) ;
#27779=DIRECTION ( 'NONE',  ( -1.000000000000000000, 0.000000000000000000, 0.000000000000000000 ) ) ;
#27824=ORIENTED_EDGE ( 'NONE', *, *, #26635, .F. ) ;
#27851=LINE ( 'NONE', #60248, #44528 ) ;
#27861=CARTESIAN_POINT ( 'NONE',  ( 14.09999999999999609, 11.99999999999999289, -3.499999999999991118 ) ) ;
#27862=CARTESIAN_POINT ( 'NONE',  ( 62.24999999999998579, 31.24999999999999289, -3.750000000000000000 ) ) ;
#27888=CIRCLE ( 'NONE', #62704, 0.2500000000000002220 ) ;
#27898=VERTEX_POINT ( 'NONE', #12023 ) ;
#27926=CARTESIAN_POINT ( 'NONE',  ( 26.25000000000001066, 18.99999999999997868, 3.750000000000000000 ) ) ;
#27934=EDGE_CURVE ( 'NONE', #42659, #67453, #23275, .T. ) ;
#27951=DIRECTION ( 'NONE',  ( 1.000000000000000000, 2.168404344971008868E-16, -0.000000000000000000 ) ) ;
#27966=DIRECTION ( 'NONE',  ( 0.000000000000000000, 0.000000000000000000, -1.000000000000000000 ) ) ;
#27974=AXIS2_PLACEMENT_3D ( 'NONE', #4337, #16005, #4716 ) ;
#27976=DIRECTION ( 'NONE',  ( -1.000000000000000000, 0.000000000000000000, 0.000000000000000000 ) ) ;
#27992=CARTESIAN_POINT ( 'NONE',  ( 16.75000000000000711, 27.74999999999998224, -4.000000000000000000 ) ) ;
#28010=AXIS2_PLACEMENT_3D ( 'NONE', #20804, #38045, #5987 ) ;
#28011=FACE_OUTER_BOUND ( 'NONE', #10706, .T. ) ;
#28025=VERTEX_POINT ( 'NONE', #30252 ) ;
#28029=DIRECTION ( 'NONE',  ( 1.156482317317870344E-15, -1.000000000000000000, 0.000000000000000000 ) ) ;
#28045=ORIENTED_EDGE ( 'NONE', *, *, #436, .F. ) ;
#28051=DIRECTION ( 'NONE',  ( -0.000000000000000000, 0.000000000000000000, -1.000000000000000000 ) ) ;
#28073=VERTEX_POINT ( 'NONE', #25678 ) ;
#28078=VECTOR ( 'NONE', #65958, 1000.000000000000000 ) ;
#28086=( LENGTH_UNIT ( ) NAMED_UNIT ( * ) SI_UNIT ( .MILLI., .METRE. ) );
#28107=CARTESIAN_POINT ( 'NONE',  ( 52.99999999999999289, 27.74999999999998579, 3.750000000000000000 ) ) ;
#28109=CYLINDRICAL_SURFACE ( 'NONE', #23819, 0.2500000000000002220 ) ;
#28115=AXIS2_PLACEMENT_3D ( 'NONE', #8870, #51795, #63019 ) ;
#28122=DIRECTION ( 'NONE',  ( 0.000000000000000000, 0.000000000000000000, -1.000000000000000000 ) ) ;
#28127=VERTEX_POINT ( 'NONE', #23516 ) ;
#28134=STYLED_ITEM ( 'NONE', ( #40100 ), #17696 ) ;
#28150=ORIENTED_EDGE ( 'NONE', *, *, #50513, .T. ) ;
#28229=AXIS2_PLACEMENT_3D ( 'NONE', #40175, #50362, #7456 ) ;
#28233=ORIENTED_EDGE ( 'NONE', *, *, #7948, .F. ) ;
#28237=ORIENTED_EDGE ( 'NONE', *, *, #15052, .F. ) ;
#28240=ORIENTED_EDGE ( 'NONE', *, *, #34867, .T. ) ;
#28241=AXIS2_PLACEMENT_3D ( 'NONE', #36077, #9345, #14260 ) ;
#28245=DIRECTION ( 'NONE',  ( 0.000000000000000000, -0.000000000000000000, -1.000000000000000000 ) ) ;
#28307=EDGE_CURVE ( 'NONE', #27455, #35469, #14837, .T. ) ;
#28315=ADVANCED_FACE ( 'NONE', ( #68526 ), #4120, .T. ) ;
#28338=LINE ( 'NONE', #1580, #36444 ) ;
#28382=VERTEX_POINT ( 'NONE', #2721 ) ;
#28385=CIRCLE ( 'NONE', #4817, 0.2500000000000002220 ) ;
#28417=ORIENTED_EDGE ( 'NONE', *, *, #15295, .F. ) ;
#28425=ORIENTED_EDGE ( 'NONE', *, *, #69346, .T. ) ;
#28440=DIRECTION ( 'NONE',  ( 0.000000000000000000, 1.000000000000000000, 0.000000000000000000 ) ) ;
#28457=VECTOR ( 'NONE', #58267, 1000.000000000000114 ) ;
#28481=DIRECTION ( 'NONE',  ( 0.000000000000000000, 0.000000000000000000, -1.000000000000000000 ) ) ;
#28513=EDGE_CURVE ( 'NONE', #19343, #24476, #42515, .T. ) ;
#28555=DIRECTION ( 'NONE',  ( 0.000000000000000000, 1.000000000000000000, 0.000000000000000000 ) ) ;
#28556=ADVANCED_FACE ( 'NONE', ( #48141 ), #125, .T. ) ;
#28564=ADVANCED_FACE ( 'NONE', ( #20686 ), #42195, .T. ) ;
#28565=ADVANCED_FACE ( 'NONE', ( #63587 ), #15430, .T. ) ;
#28573=CIRCLE ( 'NONE', #32016, 0.2500000000000002220 ) ;
#28597=LINE ( 'NONE', #44160, #24935 ) ;
#28613=ORIENTED_EDGE ( 'NONE', *, *, #46520, .T. ) ;
#28627=VERTEX_POINT ( 'NONE', #46244 ) ;
#28650=LINE ( 'NONE', #44885, #21182 ) ;
#28682=ORIENTED_EDGE ( 'NONE', *, *, #39344, .F. ) ;
#28702=EDGE_CURVE ( 'NONE', #13649, #64044, #35047, .T. ) ;
#28746=CARTESIAN_POINT ( 'NONE',  ( 12.50000000000000533, 27.99999999999998224, 3.750000000000000000 ) ) ;
#28753=ORIENTED_EDGE ( 'NONE', *, *, #38726, .T. ) ;
#28757=CARTESIAN_POINT ( 'NONE',  ( 68.99999999999998579, 1.000000000000008438, -3.000000000000000000 ) ) ;
#28760=DIRECTION ( 'NONE',  ( -0.000000000000000000, 1.000000000000000000, -0.000000000000000000 ) ) ;
#28762=ADVANCED_BREP_SHAPE_REPRESENTATION ( '', ( #50950, #42840 ), #7944 ) ;
#28773=CARTESIAN_POINT ( 'NONE',  ( 62.60000000000000142, 11.99999999999999822, 4.000000000000000000 ) ) ;
#28774=CARTESIAN_POINT ( 'NONE',  ( 57.74999999999998579, 30.99999999999999289, -3.750000000000000000 ) ) ;
#28776=VECTOR ( 'NONE', #6974, 1000.000000000000000 ) ;
#28784=CARTESIAN_POINT ( 'NONE',  ( 7.750000000000000000, 33.74999999999998579, -3.750000000000000000 ) ) ;
#28793=VERTEX_POINT ( 'NONE', #52205 ) ;
#28795=CARTESIAN_POINT ( 'NONE',  ( 66.49999999999998579, 34.24999999999999289, 4.000000000000000000 ) ) ;
#28820=CIRCLE ( 'NONE', #29943, 0.2500000000000002220 ) ;
#28821=CARTESIAN_POINT ( 'NONE',  ( 3.249999999999998668, 36.74999999999999289, 3.750000000000000000 ) ) ;
#28823=CARTESIAN_POINT ( 'NONE',  ( 48.74999999999999289, 24.99999999999998579, -3.750000000000000000 ) ) ;
#28836=DIRECTION ( 'NONE',  ( -0.000000000000000000, -0.000000000000000000, 1.000000000000000000 ) ) ;
#28839=DIRECTION ( 'NONE',  ( 0.000000000000000000, -0.000000000000000000, -1.000000000000000000 ) ) ;
#28844=ADVANCED_FACE ( 'NONE', ( #48325 ), #38478, .T. ) ;
#28848=DIRECTION ( 'NONE',  ( 1.000000000000000000, 0.000000000000000000, 0.000000000000000000 ) ) ;
#28880=ORIENTED_EDGE ( 'NONE', *, *, #578, .T. ) ;
#28885=APPLICATION_CONTEXT ( 'automotive_design' ) ;
#28912=DIRECTION ( 'NONE',  ( -1.000000000000000000, 0.000000000000000000, 0.000000000000000000 ) ) ;
#28916=ORIENTED_EDGE ( 'NONE', *, *, #26488, .T. ) ;
#28928=SPHERICAL_SURFACE ( 'NONE', #50001, 0.2500000000000000000 ) ;
#28939=AXIS2_PLACEMENT_3D ( 'NONE', #36313, #4222, #36670 ) ;
#29009=ORIENTED_EDGE ( 'NONE', *, *, #7782, .T. ) ;
#29023=EDGE_LOOP ( 'NONE', ( #41247, #24504, #66007 ) ) ;
#29031=DIRECTION ( 'NONE',  ( 0.000000000000000000, 0.000000000000000000, 1.000000000000000000 ) ) ;
#29039=VERTEX_POINT ( 'NONE', #62630 ) ;
#29046=ORIENTED_EDGE ( 'NONE', *, *, #51088, .T. ) ;
#29059=CARTESIAN_POINT ( 'NONE',  ( 25.75000000000001066, 21.74999999999998224, -3.750000000000000000 ) ) ;
#29076=ORIENTED_EDGE ( 'NONE', *, *, #41261, .T. ) ;
#29083=VERTEX_POINT ( 'NONE', #5973 ) ;
#29088=DIRECTION ( 'NONE',  ( -1.000000000000000000, -7.709882115452469292E-16, 0.000000000000000000 ) ) ;
#29090=CARTESIAN_POINT ( 'NONE',  ( 3.749999999999999556, 34.24999999999998579, 4.000000000000000000 ) ) ;
#29102=AXIS2_PLACEMENT_3D ( 'NONE', #24068, #19827, #13861 ) ;
#29105=ADVANCED_FACE ( 'NONE', ( #27414 ), #640, .T. ) ;
#29117=ORIENTED_EDGE ( 'NONE', *, *, #65982, .T. ) ;
#29176=CARTESIAN_POINT ( 'NONE',  ( 48.25000000000000000, 21.74999999999998579, 4.000000000000000000 ) ) ;
#29179=ORIENTED_EDGE ( 'NONE', *, *, #35664, .T. ) ;
#29211=FACE_OUTER_BOUND ( 'NONE', #23907, .T. ) ;
#29226=CIRCLE ( 'NONE', #37169, 0.2500000000000002220 ) ;
#29227=VERTEX_POINT ( 'NONE', #13317 ) ;
#29230=CARTESIAN_POINT ( 'NONE',  ( 8.000000000000000000, 33.74999999999998579, -3.750000000000000000 ) ) ;
#29240=EDGE_LOOP ( 'NONE', ( #38080, #56897, #39555, #41637 ) ) ;
#29246=CARTESIAN_POINT ( 'NONE',  ( 68.99999999999998579, 36.75000000000000000, 3.000000000000000000 ) ) ;
#29250=DIRECTION ( 'NONE',  ( -0.000000000000000000, 0.000000000000000000, -1.000000000000000000 ) ) ;
#29262=AXIS2_PLACEMENT_3D ( 'NONE', #14053, #46088, #30197 ) ;
#29274=CARTESIAN_POINT ( 'NONE',  ( 53.24999999999999289, 27.74999999999998579, 3.750000000000000000 ) ) ;
#29281=ADVANCED_FACE ( 'NONE', ( #11950 ), #66449, .T. ) ;
#29299=ORIENTED_EDGE ( 'NONE', *, *, #37055, .T. ) ;
#29304=ORIENTED_EDGE ( 'NONE', *, *, #16502, .T. ) ;
#29314=DIRECTION ( 'NONE',  ( 0.000000000000000000, -1.000000000000000000, 0.000000000000000000 ) ) ;
#29343=DIRECTION ( 'NONE',  ( -1.000000000000000000, 0.000000000000000000, 0.000000000000000000 ) ) ;
#29354=AXIS2_PLACEMENT_3D ( 'NONE', #67696, #14572, #3993 ) ;
#29388=AXIS2_PLACEMENT_3D ( 'NONE', #27662, #16489, #65325 ) ;
#29425=CIRCLE ( 'NONE', #37326, 0.2500000000000002220 ) ;
#29433=CARTESIAN_POINT ( 'NONE',  ( 55.40000000000000568, 11.99999999999999822, -4.000000000000000000 ) ) ;
#29450=DIRECTION ( 'NONE',  ( 0.000000000000000000, 1.000000000000000000, 0.000000000000000000 ) ) ;
#29451=EDGE_CURVE ( 'NONE', #40838, #5687, #68911, .T. ) ;
#29523=CIRCLE ( 'NONE', #50866, 0.2500000000000002220 ) ;
#29540=ADVANCED_FACE ( 'NONE', ( #24949 ), #3814, .T. ) ;
#29545=DIRECTION ( 'NONE',  ( -1.000000000000000000, 0.000000000000000000, 0.000000000000000000 ) ) ;
#29546=ORIENTED_EDGE ( 'NONE', *, *, #46520, .F. ) ;
#29548=EDGE_LOOP ( 'NONE', ( #21186, #39817, #11942, #62591 ) ) ;
#29552=DIRECTION ( 'NONE',  ( -0.000000000000000000, -0.000000000000000000, 1.000000000000000000 ) ) ;
#29554=EDGE_LOOP ( 'NONE', ( #50616, #1805, #10202, #45839 ) ) ;
#29619=EDGE_CURVE ( 'NONE', #45200, #59828, #56582, .T. ) ;
#29630=VECTOR ( 'NONE', #63598, 1000.000000000000000 ) ;
#29634=DIRECTION ( 'NONE',  ( 0.000000000000000000, -1.000000000000000000, 0.000000000000000000 ) ) ;
#29636=EDGE_CURVE ( 'NONE', #4102, #13223, #3775, .T. ) ;
#29641=ORIENTED_EDGE ( 'NONE', *, *, #13369, .T. ) ;
#29651=CARTESIAN_POINT ( 'NONE',  ( 61.74999999999998579, 30.74999999999999289, -3.750000000000000000 ) ) ;
#29662=AXIS2_PLACEMENT_3D ( 'NONE', #67743, #14273, #63503 ) ;
#29672=VERTEX_POINT ( 'NONE', #63960 ) ;
#29690=DIRECTION ( 'NONE',  ( 0.000000000000000000, 0.000000000000000000, -1.000000000000000000 ) ) ;
#29691=CARTESIAN_POINT ( 'NONE',  ( 30.25000000000000711, 18.74999999999997868, 3.750000000000000000 ) ) ;
#29704=DIRECTION ( 'NONE',  ( 0.000000000000000000, -1.000000000000000000, 0.000000000000000000 ) ) ;
#29709=AXIS2_PLACEMENT_3D ( 'NONE', #38889, #29314, #33901 ) ;
#29746=CARTESIAN_POINT ( 'NONE',  ( 68.99999999999998579, 8.450062914116736267E-15, 4.000000000000000000 ) ) ;
#29752=( GEOMETRIC_REPRESENTATION_CONTEXT ( 3 ) GLOBAL_UNCERTAINTY_ASSIGNED_CONTEXT ( ( #46132 ) ) GLOBAL_UNIT_ASSIGNED_CONTEXT ( ( #54284, #31432, #64842 ) ) REPRESENTATION_CONTEXT ( 'NONE', 'WORKASPACE' ) );
#29788=CARTESIAN_POINT ( 'NONE',  ( 26.00000000000001066, 18.99999999999997868, 3.750000000000000000 ) ) ;
#29801=CARTESIAN_POINT ( 'NONE',  ( 68.99999999999998579, 36.75000000000000000, -4.000000000000000000 ) ) ;
#29806=AXIS2_PLACEMENT_3D ( 'NONE', #23730, #17455, #39254 ) ;
#29810=ORIENTED_EDGE ( 'NONE', *, *, #57066, .T. ) ;
#29813=ORIENTED_EDGE ( 'NONE', *, *, #12382, .F. ) ;
#29815=DIRECTION ( 'NONE',  ( 2.312964634635740689E-15, -1.000000000000000000, 0.000000000000000000 ) ) ;
#29837=SURFACE_STYLE_USAGE ( .BOTH. , #56215 ) ;
#29846=VECTOR ( 'NONE', #35183, 1000.000000000000000 ) ;
#29854=VECTOR ( 'NONE', #51058, 1000.000000000000000 ) ;
#29863=CARTESIAN_POINT ( 'NONE',  ( 61.99999999999998579, 31.24999999999999289, -3.750000000000000000 ) ) ;
#29865=CARTESIAN_POINT ( 'NONE',  ( 57.49999999999998579, 30.99999999999999289, 4.000000000000000000 ) ) ;
#29878=ORIENTED_EDGE ( 'NONE', *, *, #57066, .F. ) ;
#29884=CARTESIAN_POINT ( 'NONE',  ( 0.000000000000000000, 21.74999999999998224, 4.000000000000000000 ) ) ;
#29897=CARTESIAN_POINT ( 'NONE',  ( 3.249999999999999112, 34.24999999999998579, 4.000000000000000000 ) ) ;
#29898=ORIENTED_EDGE ( 'NONE', *, *, #44133, .F. ) ;
#29902=CIRCLE ( 'NONE', #61324, 0.2500000000000002220 ) ;
#29936=CARTESIAN_POINT ( 'NONE',  ( 52.75000000000000000, 25.24999999999998579, 4.000000000000000000 ) ) ;
#29943=AXIS2_PLACEMENT_3D ( 'NONE', #1399, #16626, #65114 ) ;
#29951=AXIS2_PLACEMENT_3D ( 'NONE', #6889, #44234, #37919 ) ;
#29994=AXIS2_PLACEMENT_3D ( 'NONE', #22926, #12686, #7438 ) ;
#30002=CARTESIAN_POINT ( 'NONE',  ( 68.99999999999998579, 37.00000000000000000, -3.750000000000000000 ) ) ;
#30009=ADVANCED_FACE ( 'NONE', ( #36514 ), #40730, .T. ) ;
#30013=ADVANCED_FACE ( 'NONE', ( #8362 ), #54313, .T. ) ;
#30026=AXIS2_PLACEMENT_3D ( 'NONE', #6310, #1682, #66089 ) ;
#30035=ORIENTED_EDGE ( 'NONE', *, *, #42320, .T. ) ;
#30040=SURFACE_SIDE_STYLE ('',( #56429 ) ) ;
#30042=VECTOR ( 'NONE', #31989, 1000.000000000000000 ) ;
#30059=EDGE_CURVE ( 'NONE', #61571, #18083, #63542, .T. ) ;
#30080=FACE_OUTER_BOUND ( 'NONE', #57217, .T. ) ;
#30083=EDGE_CURVE ( 'NONE', #42973, #57523, #25213, .T. ) ;
#30084=DIRECTION ( 'NONE',  ( -1.000000000000000000, 0.000000000000000000, 0.000000000000000000 ) ) ;
#30099=DIRECTION ( 'NONE',  ( -0.000000000000000000, 0.000000000000000000, -1.000000000000000000 ) ) ;
#30106=DIRECTION ( 'NONE',  ( -1.000000000000000000, 0.000000000000000000, 0.000000000000000000 ) ) ;
#30123=ORIENTED_EDGE ( 'NONE', *, *, #33620, .T. ) ;
#30157=ORIENTED_EDGE ( 'NONE', *, *, #47574, .T. ) ;
#30159=DIRECTION ( 'NONE',  ( 0.000000000000000000, 0.000000000000000000, -1.000000000000000000 ) ) ;
#30165=CARTESIAN_POINT ( 'NONE',  ( 39.24999999999999289, 15.74999999999997513, -3.750000000000000000 ) ) ;
#30195=EDGE_CURVE ( 'NONE', #7926, #66803, #54624, .T. ) ;
#30197=DIRECTION ( 'NONE',  ( 0.000000000000000000, 0.000000000000000000, -1.000000000000000000 ) ) ;
#30205=DIRECTION ( 'NONE',  ( -1.156482317317870344E-15, -1.000000000000000000, -0.000000000000000000 ) ) ;
#30214=DIRECTION ( 'NONE',  ( 0.000000000000000000, -1.000000000000000000, 0.000000000000000000 ) ) ;
#30246=ORIENTED_EDGE ( 'NONE', *, *, #69649, .F. ) ;
#30252=CARTESIAN_POINT ( 'NONE',  ( 57.49999999999998579, 30.74999999999999289, -3.750000000000000000 ) ) ;
#30266=SPHERICAL_SURFACE ( 'NONE', #35324, 1.000000000000000000 ) ;
#30292=CARTESIAN_POINT ( 'NONE',  ( 66.24999999999998579, 34.24999999999999289, 3.750000000000000000 ) ) ;
#30293=DIRECTION ( 'NONE',  ( 0.000000000000000000, 0.000000000000000000, -1.000000000000000000 ) ) ;
#30300=ORIENTED_EDGE ( 'NONE', *, *, #56652, .T. ) ;
#30309=ORIENTED_EDGE ( 'NONE', *, *, #11826, .T. ) ;
#30317=ADVANCED_FACE ( 'NONE', ( #61979 ), #40210, .T. ) ;
#30331=ADVANCED_FACE ( 'NONE', ( #45518 ), #66579, .T. ) ;
#30369=CONICAL_SURFACE ( 'NONE', #59560, 3.100000000000000533, 0.7853981633974447263 ) ;
#30410=VERTEX_POINT ( 'NONE', #32061 ) ;
#30448=CARTESIAN_POINT ( 'NONE',  ( 57.24999999999999289, 28.24999999999998934, 3.750000000000000000 ) ) ;
#30477=VECTOR ( 'NONE', #24150, 1000.000000000000000 ) ;
#30483=ORIENTED_EDGE ( 'NONE', *, *, #2861, .T. ) ;
#30538=CIRCLE ( 'NONE', #45211, 3.600000000000005862 ) ;
#30556=DIRECTION ( 'NONE',  ( 0.000000000000000000, 0.000000000000000000, -1.000000000000000000 ) ) ;
#30573=CARTESIAN_POINT ( 'NONE',  ( 21.25000000000001066, 24.74999999999998224, 4.000000000000000000 ) ) ;
#30584=CYLINDRICAL_SURFACE ( 'NONE', #44086, 1.000000000000000000 ) ;
#30596=CIRCLE ( 'NONE', #12626, 0.5000000000000004441 ) ;
#30603=ORIENTED_EDGE ( 'NONE', *, *, #25023, .T. ) ;
#30604=EDGE_CURVE ( 'NONE', #27455, #5374, #2406, .T. ) ;
#30607=AXIS2_PLACEMENT_3D ( 'NONE', #38096, #64789, #64088 ) ;
#30617=ORIENTED_EDGE ( 'NONE', *, *, #59722, .F. ) ;
#30622=AXIS2_PLACEMENT_3D ( 'NONE', #65495, #64465, #33486 ) ;
#30656=AXIS2_PLACEMENT_3D ( 'NONE', #6898, #65299, #38266 ) ;
#30664=ORIENTED_EDGE ( 'NONE', *, *, #54408, .F. ) ;
#30679=ORIENTED_EDGE ( 'NONE', *, *, #50513, .F. ) ;
#30680=CIRCLE ( 'NONE', #305, 0.2500000000000002220 ) ;
#30689=EDGE_LOOP ( 'NONE', ( #46368, #2214, #54553, #66451 ) ) ;
#30694=ORIENTED_EDGE ( 'NONE', *, *, #1860, .T. ) ;
#30696=CARTESIAN_POINT ( 'NONE',  ( 57.75000000000005684, 1.335737076502141715E-13, 3.750000000000000000 ) ) ;
#30703=EDGE_LOOP ( 'NONE', ( #27824, #19842, #23929 ) ) ;
#30709=AXIS2_PLACEMENT_3D ( 'NONE', #15133, #59725, #21756 ) ;
#30715=EDGE_LOOP ( 'NONE', ( #57890, #43327, #53480, #11919 ) ) ;
#30716=EDGE_CURVE ( 'NONE', #7659, #38142, #6119, .T. ) ;
#30720=EDGE_CURVE ( 'NONE', #41886, #21325, #34477, .T. ) ;
#30749=AXIS2_PLACEMENT_3D ( 'NONE', #68107, #51920, #3676 ) ;
#30799=EDGE_CURVE ( 'NONE', #57684, #19536, #11587, .T. ) ;
#30803=AXIS2_PLACEMENT_3D ( 'NONE', #60174, #48977, #58797 ) ;
#30828=DIRECTION ( 'NONE',  ( 1.000000000000000000, 0.000000000000000000, -0.000000000000000000 ) ) ;
#30831=ORIENTED_EDGE ( 'NONE', *, *, #68089, .T. ) ;
#30842=FACE_OUTER_BOUND ( 'NONE', #49807, .T. ) ;
#30851=ORIENTED_EDGE ( 'NONE', *, *, #7635, .T. ) ;
#30871=DIRECTION ( 'NONE',  ( 0.000000000000000000, 0.000000000000000000, -1.000000000000000000 ) ) ;
#30875=DIRECTION ( 'NONE',  ( -1.000000000000000000, 0.000000000000000000, 0.000000000000000000 ) ) ;
#30893=EDGE_CURVE ( 'NONE', #49467, #14037, #1277, .T. ) ;
#30912=ADVANCED_FACE ( 'NONE', ( #31967 ), #37300, .T. ) ;
#30935=AXIS2_PLACEMENT_3D ( 'NONE', #38945, #6518, #65284 ) ;
#30949=DIRECTION ( 'NONE',  ( 0.000000000000000000, 0.000000000000000000, -1.000000000000000000 ) ) ;
#30974=CARTESIAN_POINT ( 'NONE',  ( 12.75000000000000533, 27.74999999999998224, 4.000000000000000000 ) ) ;
#30986=ADVANCED_FACE ( 'NONE', ( #60413 ), #49814, .T. ) ;
#31036=ORIENTED_EDGE ( 'NONE', *, *, #14891, .F. ) ;
#31041=ORIENTED_EDGE ( 'NONE', *, *, #66811, .T. ) ;
#31043=ADVANCED_FACE ( 'NONE', ( #55498 ), #3907, .F. ) ;
#31046=CYLINDRICAL_SURFACE ( 'NONE', #35415, 0.2500000000000002220 ) ;
#31071=DIRECTION ( 'NONE',  ( -1.000000000000000000, 0.000000000000000000, 0.000000000000000000 ) ) ;
#31117=VECTOR ( 'NONE', #54669, 1000.000000000000000 ) ;
#31120=EDGE_CURVE ( 'NONE', #20333, #4257, #33038, .T. ) ;
#31121=ORIENTED_EDGE ( 'NONE', *, *, #16402, .F. ) ;
#31133=ADVANCED_FACE ( 'NONE', ( #44195 ), #16194, .T. ) ;
#31173=ORIENTED_EDGE ( 'NONE', *, *, #46362, .F. ) ;
#31181=DIRECTION ( 'NONE',  ( -0.000000000000000000, -0.000000000000000000, 1.000000000000000000 ) ) ;
#31185=VERTEX_POINT ( 'NONE', #27926 ) ;
#31192=CARTESIAN_POINT ( 'NONE',  ( 52.75000000000000000, 24.74999999999998224, 4.000000000000000000 ) ) ;
#31196=ADVANCED_FACE ( 'NONE', ( #23983 ), #17448, .F. ) ;
#31204=DIRECTION ( 'NONE',  ( 0.000000000000000000, 0.000000000000000000, 1.000000000000000000 ) ) ;
#31245=VERTEX_POINT ( 'NONE', #61590 ) ;
#31250=CIRCLE ( 'NONE', #44821, 1.000000000000000888 ) ;
#31259=ORIENTED_EDGE ( 'NONE', *, *, #51267, .F. ) ;
#31269=DIRECTION ( 'NONE',  ( 1.000000000000000000, -0.000000000000000000, -0.000000000000000000 ) ) ;
#31286=ORIENTED_EDGE ( 'NONE', *, *, #29636, .T. ) ;
#31306=CARTESIAN_POINT ( 'NONE',  ( 53.24999999999999289, 27.74999999999998579, -3.750000000000000000 ) ) ;
#31309=DIRECTION ( 'NONE',  ( -1.000000000000000000, 0.000000000000000000, 0.000000000000000000 ) ) ;
#31314=CIRCLE ( 'NONE', #40331, 3.100000000000000533 ) ;
#31328=ADVANCED_FACE ( 'NONE', ( #25026 ), #36676, .T. ) ;
#31329=ORIENTED_EDGE ( 'NONE', *, *, #50065, .T. ) ;
#31348=EDGE_CURVE ( 'NONE', #19536, #7659, #4226, .T. ) ;
#31359=VERTEX_POINT ( 'NONE', #68293 ) ;
#31370=( NAMED_UNIT ( * ) PLANE_ANGLE_UNIT ( ) SI_UNIT ( $, .RADIAN. ) );
#31375=EDGE_LOOP ( 'NONE', ( #32180, #6384, #20664, #17560 ) ) ;
#31378=FILL_AREA_STYLE_COLOUR ( '', #69448 ) ;
#31388=DIRECTION ( 'NONE',  ( 1.000000000000000000, 0.000000000000000000, 0.000000000000000000 ) ) ;
#31397=ORIENTED_EDGE ( 'NONE', *, *, #69121, .F. ) ;
#31398=FACE_OUTER_BOUND ( 'NONE', #29548, .T. ) ;
#31403=CARTESIAN_POINT ( 'NONE',  ( 69.74999999999998579, 37.00000000000000000, -3.000000000000000000 ) ) ;
#31410=DIRECTION ( 'NONE',  ( 0.000000000000000000, 0.000000000000000000, -1.000000000000000000 ) ) ;
#31411=ORIENTED_EDGE ( 'NONE', *, *, #19047, .T. ) ;
#31417=DIRECTION ( 'NONE',  ( 1.000000000000000000, 0.000000000000000000, -0.000000000000000000 ) ) ;
#31432=( NAMED_UNIT ( * ) PLANE_ANGLE_UNIT ( ) SI_UNIT ( $, .RADIAN. ) );
#31436=AXIS2_PLACEMENT_3D ( 'NONE', #16719, #22663, #59225 ) ;
#31437=VECTOR ( 'NONE', #19371, 1000.000000000000000 ) ;
#31450=DIRECTION ( 'NONE',  ( 1.000000000000000000, 0.000000000000000000, 0.000000000000000000 ) ) ;
#31452=CIRCLE ( 'NONE', #1065, 1.000000000000000000 ) ;
#31454=VERTEX_POINT ( 'NONE', #28107 ) ;
#31463=CARTESIAN_POINT ( 'NONE',  ( 48.74999999999999289, 24.99999999999998579, -3.750000000000000000 ) ) ;
#31502=ADVANCED_FACE ( 'NONE', ( #22525 ), #44024, .T. ) ;
#31508=DIRECTION ( 'NONE',  ( -1.000000000000000000, 0.000000000000000000, 0.000000000000000000 ) ) ;
#31522=LINE ( 'NONE', #53356, #28457 ) ;
#31529=( GEOMETRIC_REPRESENTATION_CONTEXT ( 3 ) GLOBAL_UNCERTAINTY_ASSIGNED_CONTEXT ( ( #61428 ) ) GLOBAL_UNIT_ASSIGNED_CONTEXT ( ( #35686, #63095, #62406 ) ) REPRESENTATION_CONTEXT ( 'NONE', 'WORKASPACE' ) );
#31536=ORIENTED_EDGE ( 'NONE', *, *, #25693, .F. ) ;
#31547=ORIENTED_EDGE ( 'NONE', *, *, #25950, .F. ) ;
#31555=VERTEX_POINT ( 'NONE', #2020 ) ;
#31563=CARTESIAN_POINT ( 'NONE',  ( 7.750000000000019540, 4.481368979606759023E-15, 3.750000000000000000 ) ) ;
#31565=DIRECTION ( 'NONE',  ( -0.000000000000000000, 0.000000000000000000, -1.000000000000000000 ) ) ;
#31575=CYLINDRICAL_SURFACE ( 'NONE', #13357, 0.2500000000000002220 ) ;
#31593=ADVANCED_FACE ( 'NONE', ( #2753 ), #55207, .T. ) ;
#31645=DIRECTION ( 'NONE',  ( 0.000000000000000000, 0.000000000000000000, -1.000000000000000000 ) ) ;
#31661=EDGE_LOOP ( 'NONE', ( #16717, #68789, #11282, #69601 ) ) ;
#31665=AXIS2_PLACEMENT_3D ( 'NONE', #9978, #21916, #58163 ) ;
#31674=FACE_OUTER_BOUND ( 'NONE', #66771, .T. ) ;
#31675=ORIENTED_EDGE ( 'NONE', *, *, #16761, .T. ) ;
#31676=CARTESIAN_POINT ( 'NONE',  ( 12.25000000000000355, 30.74999999999998579, 4.000000000000000000 ) ) ;
#31677=DIRECTION ( 'NONE',  ( -1.000000000000000000, 0.000000000000000000, 0.000000000000000000 ) ) ;
#31680=LINE ( 'NONE', #55200, #44937 ) ;
#31687=FACE_OUTER_BOUND ( 'NONE', #63061, .T. ) ;
#31689=VECTOR ( 'NONE', #63428, 1000.000000000000000 ) ;
#31693=DIRECTION ( 'NONE',  ( -1.000000000000000000, 0.000000000000000000, 0.000000000000000000 ) ) ;
#31699=EDGE_LOOP ( 'NONE', ( #13371, #63311, #14065, #54311 ) ) ;
#31734=DIRECTION ( 'NONE',  ( 0.000000000000000000, 0.000000000000000000, 1.000000000000000000 ) ) ;
#31758=CLOSED_SHELL ( 'NONE', ( #59640, #47581, #24240, #2964, #3225, #47716, #4762, #2480, #7089, #62650, #47566, #7154, #6421, #27297, #8044, #15558, #53148, #44541, #18597, #21435, #52130, #14752, #5378, #12550, #22808, #53749, #67584, #62498, #20672, #44415, #42931, #37413, #20512, #61608, #46195, #10910, #61514, #31043, #25449, #41324, #17674, #12127, #30912, #31593, #23119, #63843, #45420, #64739, #58940, #20431, #36016, #31196, #45667, #6184, #18491, #6414, #34795, #2463, #7064, #4045, #22178, #44706, #20093, #67605, #13341, #68306, #53785, #48812, #63694, #43412, #29540, #10169, #46002, #17696, #38867, #23504, #54436, #68714, #72, #21601, #63612, #38738, #54250, #49057, #63453, #55835, #720, #9444, #30986, #49531, #45724, #58229, #48658, #50025, #22212, #5787, #55304, #38081, #54141, #8439, #44623, #35933, #40218, #33502, #48901, #1538, #41180, #31328, #7310, #44546, #63301, #69428, #30013, #34634, #28315, #10505, #15056, #54087, #9147, #15674, #15144, #27758, #66071, #37469, #30009, #63284, #51705, #3548, #6028, #43745, #741, #49421, #65523, #26238, #65920, #13675, #32908, #27173, #28556, #24811, #39769, #58871, #44672, #29281, #48027, #28844, #10974, #27550, #63553, #26804, #28564, #22246, #23957, #1393, #28565, #21931, #52674, #29105, #47558, #22893, #30331, #58111, #62091, #51871, #30317, #8450, #66154, #51170, #26127, #3278, #11265, #53423, #43136, #60902, #37834, #40985, #36915, #11835, #56733, #64886, #39855, #44899, #46338, #61006, #7094, #2012, #20629, #69023, #31502, #13347, #1401, #64405, #38430, #69536, #4849, #40937, #15414, #39181, #56528, #22317, #16883, #21407, #53251, #47794, #37296, #31133 ) ) ;
#31766=VECTOR ( 'NONE', #27125, 1000.000000000000000 ) ;
#31772=DIRECTION ( 'NONE',  ( 0.000000000000000000, -0.000000000000000000, 1.000000000000000000 ) ) ;
#31778=DIRECTION ( 'NONE',  ( 0.000000000000000000, 1.000000000000000000, -0.000000000000000000 ) ) ;
#31790=CARTESIAN_POINT ( 'NONE',  ( 3.249999999999998668, 36.74999999999999289, 4.000000000000000000 ) ) ;
#31792=VERTEX_POINT ( 'NONE', #65341 ) ;
#31798=AXIS2_PLACEMENT_3D ( 'NONE', #67457, #40761, #67120 ) ;
#31811=ORIENTED_EDGE ( 'NONE', *, *, #54927, .T. ) ;
#31817=DIRECTION ( 'NONE',  ( -0.000000000000000000, -0.000000000000000000, -1.000000000000000000 ) ) ;
#31851=UNCERTAINTY_MEASURE_WITH_UNIT (LENGTH_MEASURE( 1.000000000000000082E-05 ), #24899, 'distance_accuracy_value', 'NONE');
#31856=DIRECTION ( 'NONE',  ( -1.000000000000000000, 0.000000000000000000, 0.000000000000000000 ) ) ;
#31863=DIRECTION ( 'NONE',  ( -0.000000000000000000, 0.000000000000000000, -1.000000000000000000 ) ) ;
#31868=EDGE_CURVE ( 'NONE', #54091, #33883, #52243, .T. ) ;
#31870=FACE_OUTER_BOUND ( 'NONE', #9162, .T. ) ;
#31871=VERTEX_POINT ( 'NONE', #13247 ) ;
#31880=ORIENTED_EDGE ( 'NONE', *, *, #28702, .T. ) ;
#31917=CARTESIAN_POINT ( 'NONE',  ( 43.75000000000000000, 18.74999999999998224, 3.750000000000000000 ) ) ;
#31929=LINE ( 'NONE', #64968, #39759 ) ;
#31932=AXIS2_PLACEMENT_3D ( 'NONE', #56369, #2865, #24354 ) ;
#31950=FACE_OUTER_BOUND ( 'NONE', #12706, .T. ) ;
#31967=FACE_OUTER_BOUND ( 'NONE', #22918, .T. ) ;
#31980=FACE_OUTER_BOUND ( 'NONE', #17355, .T. ) ;
#31983=AXIS2_PLACEMENT_3D ( 'NONE', #10341, #31772, #37107 ) ;
#31989=DIRECTION ( 'NONE',  ( -0.000000000000000000, -0.000000000000000000, 1.000000000000000000 ) ) ;
#31995=EDGE_CURVE ( 'NONE', #24250, #11473, #2663, .T. ) ;
#32016=AXIS2_PLACEMENT_3D ( 'NONE', #2215, #34639, #56099 ) ;
#32022=DIRECTION ( 'NONE',  ( 0.000000000000000000, 1.000000000000000000, -0.000000000000000000 ) ) ;
#32029=EDGE_LOOP ( 'NONE', ( #31411, #1186, #26096, #22732 ) ) ;
#32056=CARTESIAN_POINT ( 'NONE',  ( 3.499999999999999112, 34.24999999999998579, -3.750000000000000000 ) ) ;
#32061=CARTESIAN_POINT ( 'NONE',  ( 7.750000000000000000, 33.74999999999998579, -4.000000000000000000 ) ) ;
#32074=DIRECTION ( 'NONE',  ( 0.000000000000000000, 0.000000000000000000, 1.000000000000000000 ) ) ;
#32084=LINE ( 'NONE', #32406, #69332 ) ;
#32102=ORIENTED_EDGE ( 'NONE', *, *, #39837, .T. ) ;
#32111=AXIS2_PLACEMENT_3D ( 'NONE', #39626, #3296, #44911 ) ;
#32124=AXIS2_PLACEMENT_3D ( 'NONE', #57013, #46871, #8828 ) ;
#32134=DIRECTION ( 'NONE',  ( 0.000000000000000000, 0.000000000000000000, -1.000000000000000000 ) ) ;
#32141=CARTESIAN_POINT ( 'NONE',  ( 3.249999999999998668, 36.74999999999999289, 3.750000000000000000 ) ) ;
#32144=AXIS2_PLACEMENT_3D ( 'NONE', #57257, #45371, #40770 ) ;
#32165=LINE ( 'NONE', #11041, #69298 ) ;
#32166=AXIS2_PLACEMENT_3D ( 'NONE', #51836, #26467, #25088 ) ;
#32180=ORIENTED_EDGE ( 'NONE', *, *, #35177, .T. ) ;
#32200=DIRECTION ( 'NONE',  ( 0.000000000000000000, -1.000000000000000000, 0.000000000000000000 ) ) ;
#32228=EDGE_CURVE ( 'NONE', #835, #28025, #9565, .T. ) ;
#32231=VERTEX_POINT ( 'NONE', #15031 ) ;
#32233=CIRCLE ( 'NONE', #27740, 0.2500000000000002220 ) ;
#32260=CARTESIAN_POINT ( 'NONE',  ( 61.99999999999998579, 33.74999999999999289, -3.750000000000000000 ) ) ;
#32291=DIRECTION ( 'NONE',  ( -2.312964634635740689E-15, 1.000000000000000000, 0.000000000000000000 ) ) ;
#32297=AXIS2_PLACEMENT_3D ( 'NONE', #53780, #47539, #47182 ) ;
#32322=SURFACE_STYLE_FILL_AREA ( #6285 ) ;
#32331=EDGE_CURVE ( 'NONE', #5648, #68323, #34289, .T. ) ;
#32355=CARTESIAN_POINT ( 'NONE',  ( 0.000000000000000000, 36.74999999999999289, 3.750000000000000000 ) ) ;
#32392=EDGE_CURVE ( 'NONE', #69157, #7947, #23096, .T. ) ;
#32406=CARTESIAN_POINT ( 'NONE',  ( 21.25000000000000711, 22.24999999999998224, -4.000000000000000000 ) ) ;
#32408=AXIS2_PLACEMENT_3D ( 'NONE', #68887, #31565, #21024 ) ;
#32415=VECTOR ( 'NONE', #1650, 1000.000000000000000 ) ;
#32429=ORIENTED_EDGE ( 'NONE', *, *, #64087, .T. ) ;
#32445=AXIS2_PLACEMENT_3D ( 'NONE', #45221, #54078, #13501 ) ;
#32451=VECTOR ( 'NONE', #49486, 1000.000000000000000 ) ;
#32470=SURFACE_SIDE_STYLE ('',( #36779 ) ) ;
#32490=AXIS2_PLACEMENT_3D ( 'NONE', #13557, #4035, #46680 ) ;
#32494=LINE ( 'NONE', #4362, #25160 ) ;
#32504=EDGE_LOOP ( 'NONE', ( #64634, #64778, #48897, #49073 ) ) ;
#32505=AXIS2_PLACEMENT_3D ( 'NONE', #15699, #37181, #15378 ) ;
#32520=DIRECTION ( 'NONE',  ( -1.000000000000000000, 0.000000000000000000, 0.000000000000000000 ) ) ;
#32526=AXIS2_PLACEMENT_3D ( 'NONE', #52484, #35235, #66910 ) ;
#32543=CIRCLE ( 'NONE', #61756, 0.2500000000000002220 ) ;
#32548=CARTESIAN_POINT ( 'NONE',  ( 61.74999999999998579, 30.99999999999999289, 3.750000000000000000 ) ) ;
#32577=CARTESIAN_POINT ( 'NONE',  ( 59.00000000000000000, 11.99999999999999822, 4.000000000000000000 ) ) ;
#32579=ORIENTED_EDGE ( 'NONE', *, *, #53238, .F. ) ;
#32599=LINE ( 'NONE', #59324, #38827 ) ;
#32600=ORIENTED_EDGE ( 'NONE', *, *, #48169, .F. ) ;
#32601=DIRECTION ( 'NONE',  ( -1.000000000000000000, 0.000000000000000000, 0.000000000000000000 ) ) ;
#32604=DIRECTION ( 'NONE',  ( 1.000000000000000000, 0.000000000000000000, 0.000000000000000000 ) ) ;
#32614=FACE_OUTER_BOUND ( 'NONE', #69001, .T. ) ;
#32625=CIRCLE ( 'NONE', #15848, 0.5000000000000004441 ) ;
#32633=ORIENTED_EDGE ( 'NONE', *, *, #59155, .T. ) ;
#32642=ORIENTED_EDGE ( 'NONE', *, *, #62582, .T. ) ;
#32645=CIRCLE ( 'NONE', #13565, 0.2500000000000000000 ) ;
#32655=VERTEX_POINT ( 'NONE', #58873 ) ;
#32660=CARTESIAN_POINT ( 'NONE',  ( 57.24999999999999289, 28.24999999999998934, 3.750000000000000000 ) ) ;
#32664=ORIENTED_EDGE ( 'NONE', *, *, #65348, .T. ) ;
#32673=CARTESIAN_POINT ( 'NONE',  ( 30.75000000000001066, 16.24999999999997513, 3.750000000000000000 ) ) ;
#32676=ORIENTED_EDGE ( 'NONE', *, *, #52474, .T. ) ;
#32682=CARTESIAN_POINT ( 'NONE',  ( 44.25000000000000000, 21.74999999999998579, -4.000000000000000000 ) ) ;
#32699=DIRECTION ( 'NONE',  ( -1.000000000000000000, 0.000000000000000000, 0.000000000000000000 ) ) ;
#32704=DIRECTION ( 'NONE',  ( -1.000000000000000000, 0.000000000000000000, 0.000000000000000000 ) ) ;
#32706=CIRCLE ( 'NONE', #58524, 0.2500000000000002220 ) ;
#32720=VECTOR ( 'NONE', #33104, 1000.000000000000000 ) ;
#32736=VERTEX_POINT ( 'NONE', #45147 ) ;
#32739=DIRECTION ( 'NONE',  ( -1.000000000000000000, -5.782411586589351722E-16, 0.000000000000000000 ) ) ;
#32750=EDGE_CURVE ( 'NONE', #60504, #64131, #6423, .T. ) ;
#32753=DIRECTION ( 'NONE',  ( -0.000000000000000000, 0.000000000000000000, -1.000000000000000000 ) ) ;
#32774=CIRCLE ( 'NONE', #29388, 0.2500000000000002220 ) ;
#32775=FACE_OUTER_BOUND ( 'NONE', #19516, .T. ) ;
#32779=ORIENTED_EDGE ( 'NONE', *, *, #10095, .T. ) ;
#32810=LINE ( 'NONE', #53245, #69545 ) ;
#32812=EDGE_CURVE ( 'NONE', #25904, #29039, #27851, .T. ) ;
#32850=VERTEX_POINT ( 'NONE', #55305 ) ;
#32871=EDGE_LOOP ( 'NONE', ( #63934, #7056, #62364, #54269 ) ) ;
#32908=ADVANCED_FACE ( 'NONE', ( #65872 ), #39170, .T. ) ;
#32927=CARTESIAN_POINT ( 'NONE',  ( 30.50000000000001066, 15.74999999999997513, -3.750000000000000000 ) ) ;
#32930=DIRECTION ( 'NONE',  ( 0.000000000000000000, 0.000000000000000000, -1.000000000000000000 ) ) ;
#32956=CARTESIAN_POINT ( 'NONE',  ( 61.74999999999998579, 30.99999999999999289, -4.000000000000000000 ) ) ;
#32969=LINE ( 'NONE', #63913, #33103 ) ;
#33001=ORIENTED_EDGE ( 'NONE', *, *, #31868, .T. ) ;
#33004=AXIS2_PLACEMENT_3D ( 'NONE', #43906, #6543, #7274 ) ;
#33033=ORIENTED_EDGE ( 'NONE', *, *, #8144, .T. ) ;
#33038=CIRCLE ( 'NONE', #38701, 0.2500000000000002220 ) ;
#33072=CIRCLE ( 'NONE', #51047, 3.600000000000005862 ) ;
#33079=CARTESIAN_POINT ( 'NONE',  ( 48.74999999999999289, 24.74999999999998579, 3.750000000000000000 ) ) ;
#33098=ORIENTED_EDGE ( 'NONE', *, *, #30716, .F. ) ;
#33103=VECTOR ( 'NONE', #37244, 1000.000000000000000 ) ;
#33104=DIRECTION ( 'NONE',  ( -1.445602896647337931E-16, 1.000000000000000000, 0.000000000000000000 ) ) ;
#33132=TOROIDAL_SURFACE ( 'NONE', #46633, 0.5000000000000000000, 0.2500000000000000000 ) ;
#33135=STYLED_ITEM ( 'NONE', ( #10011 ), #38867 ) ;
#33147=EDGE_CURVE ( 'NONE', #26491, #2459, #59532, .T. ) ;
#33152=EDGE_LOOP ( 'NONE', ( #25668, #21612, #58462, #178 ) ) ;
#33179=AXIS2_PLACEMENT_3D ( 'NONE', #54572, #692, #16968 ) ;
#33202=ORIENTED_EDGE ( 'NONE', *, *, #51876, .F. ) ;
#33211=ORIENTED_EDGE ( 'NONE', *, *, #36584, .F. ) ;
#33227=DIRECTION ( 'NONE',  ( 0.000000000000000000, -1.000000000000000000, 0.000000000000000000 ) ) ;
#33235=VECTOR ( 'NONE', #23995, 1000.000000000000000 ) ;
#33237=VERTEX_POINT ( 'NONE', #45326 ) ;
#33240=LINE ( 'NONE', #36022, #25757 ) ;
#33243=CYLINDRICAL_SURFACE ( 'NONE', #4972, 0.2500000000000002220 ) ;
#33258=DIRECTION ( 'NONE',  ( -1.000000000000000000, 0.000000000000000000, 0.000000000000000000 ) ) ;
#33259=CARTESIAN_POINT ( 'NONE',  ( 21.75000000000001066, 22.24999999999998224, 3.750000000000000000 ) ) ;
#33273=EDGE_CURVE ( 'NONE', #28793, #47709, #47295, .T. ) ;
#33274=SPHERICAL_SURFACE ( 'NONE', #59821, 0.2500000000000000000 ) ;
#33291=EDGE_CURVE ( 'NONE', #57684, #16642, #15389, .T. ) ;
#33347=CARTESIAN_POINT ( 'NONE',  ( 30.50000000000000711, 18.99999999999997868, 4.000000000000000000 ) ) ;
#33354=LINE ( 'NONE', #28746, #48773 ) ;
#33363=AXIS2_PLACEMENT_3D ( 'NONE', #1398, #1750, #60517 ) ;
#33373=ORIENTED_EDGE ( 'NONE', *, *, #65990, .F. ) ;
#33375=PRESENTATION_STYLE_ASSIGNMENT (( #64701 ) ) ;
#33388=CARTESIAN_POINT ( 'NONE',  ( 12.75000000000000533, 27.74999999999998224, 3.750000000000000000 ) ) ;
#33410=EDGE_CURVE ( 'NONE', #6607, #44763, #15040, .T. ) ;
#33414=SPHERICAL_SURFACE ( 'NONE', #53836, 0.2500000000000000000 ) ;
#33420=FACE_OUTER_BOUND ( 'NONE', #54113, .T. ) ;
#33433=ORIENTED_EDGE ( 'NONE', *, *, #58464, .T. ) ;
#33434=DIRECTION ( 'NONE',  ( 0.000000000000000000, 0.000000000000000000, -1.000000000000000000 ) ) ;
#33458=ORIENTED_EDGE ( 'NONE', *, *, #69336, .T. ) ;
#33470=AXIS2_PLACEMENT_3D ( 'NONE', #23387, #815, #43853 ) ;
#33486=DIRECTION ( 'NONE',  ( 1.000000000000000000, 0.000000000000000000, 0.000000000000000000 ) ) ;
#33494=DIRECTION ( 'NONE',  ( -1.000000000000000000, 0.000000000000000000, 0.000000000000000000 ) ) ;
#33502=ADVANCED_FACE ( 'NONE', ( #16076 ), #59989, .T. ) ;
#33563=CARTESIAN_POINT ( 'NONE',  ( 21.50000000000000711, 22.24999999999998224, -3.750000000000000000 ) ) ;
#33572=EDGE_LOOP ( 'NONE', ( #24290, #38688, #22108, #69196 ) ) ;
#33578=FACE_OUTER_BOUND ( 'NONE', #45182, .T. ) ;
#33620=EDGE_CURVE ( 'NONE', #23940, #50938, #8961, .T. ) ;
#33622=AXIS2_PLACEMENT_3D ( 'NONE', #25194, #63857, #20255 ) ;
#33627=VECTOR ( 'NONE', #55318, 1000.000000000000000 ) ;
#33628=EDGE_LOOP ( 'NONE', ( #26460, #16471, #40494, #29878 ) ) ;
#33654=DIRECTION ( 'NONE',  ( 1.000000000000000000, 0.000000000000000000, 0.000000000000000000 ) ) ;
#33669=CARTESIAN_POINT ( 'NONE',  ( 39.74999999999999289, 18.99999999999997868, -3.750000000000000000 ) ) ;
#33674=EDGE_CURVE ( 'NONE', #11473, #26491, #20902, .T. ) ;
#33684=FACE_OUTER_BOUND ( 'NONE', #17916, .T. ) ;
#33696=ORIENTED_EDGE ( 'NONE', *, *, #68101, .T. ) ;
#33716=CARTESIAN_POINT ( 'NONE',  ( 62.24999999999998579, 33.74999999999999289, 4.000000000000000000 ) ) ;
#33727=ORIENTED_EDGE ( 'NONE', *, *, #57431, .F. ) ;
#33732=DIRECTION ( 'NONE',  ( 1.000000000000000000, 0.000000000000000000, 0.000000000000000000 ) ) ;
#33737=AXIS2_PLACEMENT_3D ( 'NONE', #66460, #27756, #49260 ) ;
#33744=CARTESIAN_POINT ( 'NONE',  ( 57.74999999999998579, 30.74999999999999289, 3.750000000000000000 ) ) ;
#33748=CIRCLE ( 'NONE', #51758, 0.2500000000000002220 ) ;
#33775=CARTESIAN_POINT ( 'NONE',  ( 30.75000000000001066, 16.24999999999997513, -3.750000000000000000 ) ) ;
#33793=EDGE_CURVE ( 'NONE', #11461, #27455, #66205, .T. ) ;
#33800=VERTEX_POINT ( 'NONE', #31790 ) ;
#33820=CIRCLE ( 'NONE', #25922, 0.2500000000000002220 ) ;
#33831=DIRECTION ( 'NONE',  ( 1.000000000000000000, 0.000000000000000000, -0.000000000000000000 ) ) ;
#33836=EDGE_CURVE ( 'NONE', #2790, #44704, #34778, .T. ) ;
#33844=VERTEX_POINT ( 'NONE', #2496 ) ;
#33847=AXIS2_PLACEMENT_3D ( 'NONE', #21140, #42645, #14149 ) ;
#33865=EDGE_CURVE ( 'NONE', #37744, #17986, #44809, .T. ) ;
#33883=VERTEX_POINT ( 'NONE', #60255 ) ;
#33893=AXIS2_PLACEMENT_3D ( 'NONE', #28821, #38044, #43675 ) ;
#33898=EDGE_CURVE ( 'NONE', #61448, #33800, #7485, .T. ) ;
#33901=DIRECTION ( 'NONE',  ( 0.000000000000000000, 0.000000000000000000, -1.000000000000000000 ) ) ;
#33905=CARTESIAN_POINT ( 'NONE',  ( 48.75000000000000000, 22.24999999999998579, 3.750000000000000000 ) ) ;
#33909=EDGE_CURVE ( 'NONE', #29083, #9427, #24008, .T. ) ;
#33921=EDGE_CURVE ( 'NONE', #22828, #64131, #11180, .T. ) ;
#33924=CARTESIAN_POINT ( 'NONE',  ( 66.24999999999998579, 34.24999999999999289, 4.000000000000000000 ) ) ;
#33926=DIRECTION ( 'NONE',  ( 0.000000000000000000, -1.000000000000000000, 0.000000000000000000 ) ) ;
#33928=EDGE_CURVE ( 'NONE', #42069, #31871, #18395, .T. ) ;
#33943=CARTESIAN_POINT ( 'NONE',  ( 59.00000000000000000, 11.99999999999999822, 3.499999999999992895 ) ) ;
#33962=CARTESIAN_POINT ( 'NONE',  ( 53.00000000000000000, 24.99999999999998579, 3.750000000000000000 ) ) ;
#33994=AXIS2_PLACEMENT_3D ( 'NONE', #49473, #16456, #27966 ) ;
#34026=VECTOR ( 'NONE', #11665, 1000.000000000000000 ) ;
#34028=DIRECTION ( 'NONE',  ( -0.000000000000000000, 0.000000000000000000, -1.000000000000000000 ) ) ;
#34037=EDGE_LOOP ( 'NONE', ( #66399, #24343, #18235, #52247 ) ) ;
#34057=EDGE_LOOP ( 'NONE', ( #28150, #53898, #7145 ) ) ;
#34058=AXIS2_PLACEMENT_3D ( 'NONE', #42363, #6, #63418 ) ;
#34062=EDGE_CURVE ( 'NONE', #6066, #37003, #1010, .T. ) ;
#34071=VECTOR ( 'NONE', #48709, 1000.000000000000000 ) ;
#34072=ORIENTED_EDGE ( 'NONE', *, *, #8515, .F. ) ;
#34081=FILL_AREA_STYLE_COLOUR ( '', #18308 ) ;
#34089=AXIS2_PLACEMENT_3D ( 'NONE', #18270, #28440, #34095 ) ;
#34095=DIRECTION ( 'NONE',  ( 0.000000000000000000, 0.000000000000000000, 1.000000000000000000 ) ) ;
#34133=DIRECTION ( 'NONE',  ( 0.000000000000000000, -0.000000000000000000, 1.000000000000000000 ) ) ;
#34144=CYLINDRICAL_SURFACE ( 'NONE', #36097, 0.2500000000000002220 ) ;
#34145=DIRECTION ( 'NONE',  ( 0.000000000000000000, -1.000000000000000000, 0.000000000000000000 ) ) ;
#34155=EDGE_LOOP ( 'NONE', ( #3843, #54943, #61616, #62511 ) ) ;
#34170=AXIS2_PLACEMENT_3D ( 'NONE', #2221, #35361, #45930 ) ;
#34173=DIRECTION ( 'NONE',  ( 1.000000000000000000, 0.000000000000000000, 0.000000000000000000 ) ) ;
#34182=CARTESIAN_POINT ( 'NONE',  ( 57.74999999999998579, 30.74999999999999289, -4.000000000000000000 ) ) ;
#34195=CIRCLE ( 'NONE', #12837, 0.2500000000000002220 ) ;
#34196=ORIENTED_EDGE ( 'NONE', *, *, #3147, .F. ) ;
#34198=DIRECTION ( 'NONE',  ( 0.000000000000000000, -1.000000000000000000, 0.000000000000000000 ) ) ;
#34206=AXIS2_PLACEMENT_3D ( 'NONE', #66793, #50268, #65745 ) ;
#34209=CIRCLE ( 'NONE', #40975, 0.2500000000000002220 ) ;
#34249=VERTEX_POINT ( 'NONE', #29176 ) ;
#34282=ORIENTED_EDGE ( 'NONE', *, *, #21255, .F. ) ;
#34289=CIRCLE ( 'NONE', #29806, 0.5000000000000004441 ) ;
#34308=DIRECTION ( 'NONE',  ( -0.000000000000000000, -0.000000000000000000, 1.000000000000000000 ) ) ;
#34320=DIRECTION ( 'NONE',  ( 0.000000000000000000, 1.000000000000000000, 0.000000000000000000 ) ) ;
#34358=EDGE_LOOP ( 'NONE', ( #60498, #60013, #43135, #26102 ) ) ;
#34378=AXIS2_PLACEMENT_3D ( 'NONE', #54796, #22824, #65720 ) ;
#34403=LINE ( 'NONE', #35794, #147 ) ;
#34416=VERTEX_POINT ( 'NONE', #62245 ) ;
#34438=SURFACE_STYLE_FILL_AREA ( #55894 ) ;
#34458=FACE_OUTER_BOUND ( 'NONE', #69057, .T. ) ;
#34466=EDGE_CURVE ( 'NONE', #40838, #61112, #6758, .T. ) ;
#34472=DIRECTION ( 'NONE',  ( 0.000000000000000000, -1.000000000000000000, 0.000000000000000000 ) ) ;
#34474=AXIS2_PLACEMENT_3D ( 'NONE', #26599, #48121, #10794 ) ;
#34477=LINE ( 'NONE', #50663, #54412 ) ;
#34487=DIRECTION ( 'NONE',  ( 0.000000000000000000, 0.000000000000000000, -1.000000000000000000 ) ) ;
#34491=ORIENTED_EDGE ( 'NONE', *, *, #45078, .T. ) ;
#34529=CARTESIAN_POINT ( 'NONE',  ( 30.75000000000001066, 16.24999999999997513, -3.750000000000000000 ) ) ;
#34540=TOROIDAL_SURFACE ( 'NONE', #53628, 0.5000000000000000000, 0.2500000000000000000 ) ;
#34547=VERTEX_POINT ( 'NONE', #20374 ) ;
#34583=CARTESIAN_POINT ( 'NONE',  ( 16.75000000000000711, 27.99999999999998224, 4.000000000000000000 ) ) ;
#34633=DIRECTION ( 'NONE',  ( 1.000000000000000000, -0.000000000000000000, 0.000000000000000000 ) ) ;
#34634=ADVANCED_FACE ( 'NONE', ( #3647 ), #10019, .T. ) ;
#34636=CIRCLE ( 'NONE', #42519, 0.5000000000000004441 ) ;
#34639=DIRECTION ( 'NONE',  ( 1.000000000000000000, -0.000000000000000000, 0.000000000000000000 ) ) ;
#34647=DIRECTION ( 'NONE',  ( 1.000000000000000000, -0.000000000000000000, 0.000000000000000000 ) ) ;
#34667=ORIENTED_EDGE ( 'NONE', *, *, #21544, .T. ) ;
#34684=DIRECTION ( 'NONE',  ( 0.000000000000000000, 1.000000000000000000, 0.000000000000000000 ) ) ;
#34694=CARTESIAN_POINT ( 'NONE',  ( 48.74999999999999289, 24.74999999999998579, 4.000000000000000000 ) ) ;
#34709=DIRECTION ( 'NONE',  ( 0.000000000000000000, 0.000000000000000000, -1.000000000000000000 ) ) ;
#34710=AXIS2_PLACEMENT_3D ( 'NONE', #34694, #18542, #30106 ) ;
#34714=ORIENTED_EDGE ( 'NONE', *, *, #61104, .T. ) ;
#34723=CYLINDRICAL_SURFACE ( 'NONE', #55601, 0.2500000000000002220 ) ;
#34727=AXIS2_PLACEMENT_3D ( 'NONE', #29691, #3975, #67672 ) ;
#34747=VERTEX_POINT ( 'NONE', #37208 ) ;
#34750=DIRECTION ( 'NONE',  ( 0.000000000000000000, 0.000000000000000000, -1.000000000000000000 ) ) ;
#34760=FACE_OUTER_BOUND ( 'NONE', #17895, .T. ) ;
#34772=( NAMED_UNIT ( * ) SI_UNIT ( $, .STERADIAN. ) SOLID_ANGLE_UNIT ( ) );
#34778=CIRCLE ( 'NONE', #4426, 0.2500000000000002220 ) ;
#34795=ADVANCED_FACE ( 'NONE', ( #20647 ), #39275, .F. ) ;
#34797=AXIS2_PLACEMENT_3D ( 'NONE', #60832, #45059, #66474 ) ;
#34818=ORIENTED_EDGE ( 'NONE', *, *, #51951, .F. ) ;
#34838=VERTEX_POINT ( 'NONE', #65629 ) ;
#34851=DIRECTION ( 'NONE',  ( -1.000000000000000000, 0.000000000000000000, 0.000000000000000000 ) ) ;
#34865=DIRECTION ( 'NONE',  ( 0.000000000000000000, 0.000000000000000000, 1.000000000000000000 ) ) ;
#34867=EDGE_CURVE ( 'NONE', #64812, #31792, #55416, .T. ) ;
#34870=CARTESIAN_POINT ( 'NONE',  ( 39.49999999999999289, 18.74999999999997868, 4.000000000000000000 ) ) ;
#34883=AXIS2_PLACEMENT_3D ( 'NONE', #43096, #16684, #16351 ) ;
#34900=ORIENTED_EDGE ( 'NONE', *, *, #30083, .F. ) ;
#34905=DIRECTION ( 'NONE',  ( -1.000000000000000000, 0.000000000000000000, 0.000000000000000000 ) ) ;
#34906=DIRECTION ( 'NONE',  ( -5.782411586589351722E-16, 1.000000000000000000, 0.000000000000000000 ) ) ;
#34921=DIRECTION ( 'NONE',  ( 0.000000000000000000, 0.000000000000000000, -1.000000000000000000 ) ) ;
#34975=DIRECTION ( 'NONE',  ( 2.312964634635740689E-15, -1.000000000000000000, 0.000000000000000000 ) ) ;
#34980=FILL_AREA_STYLE ('',( #41682 ) ) ;
#34986=FACE_OUTER_BOUND ( 'NONE', #31375, .T. ) ;
#35010=CARTESIAN_POINT ( 'NONE',  ( 68.99999999999998579, 1.000000000000008438, -4.000000000000000000 ) ) ;
#35028=AXIS2_PLACEMENT_3D ( 'NONE', #26586, #41791, #16089 ) ;
#35030=ORIENTED_EDGE ( 'NONE', *, *, #11599, .T. ) ;
#35033=DIRECTION ( 'NONE',  ( -1.000000000000000000, 0.000000000000000000, 0.000000000000000000 ) ) ;
#35035=EDGE_CURVE ( 'NONE', #59308, #58413, #68699, .T. ) ;
#35046=DIRECTION ( 'NONE',  ( -1.000000000000000000, 0.000000000000000000, 0.000000000000000000 ) ) ;
#35047=CIRCLE ( 'NONE', #24947, 0.2500000000000002220 ) ;
#35060=DIRECTION ( 'NONE',  ( 1.000000000000000000, -0.000000000000000000, -0.000000000000000000 ) ) ;
#35105=VECTOR ( 'NONE', #10983, 1000.000000000000000 ) ;
#35158=DIRECTION ( 'NONE',  ( 1.000000000000000000, 0.000000000000000000, 0.000000000000000000 ) ) ;
#35163=DIRECTION ( 'NONE',  ( -1.000000000000000000, 0.000000000000000000, 0.000000000000000000 ) ) ;
#35167=VERTEX_POINT ( 'NONE', #53609 ) ;
#35176=ORIENTED_EDGE ( 'NONE', *, *, #67691, .F. ) ;
#35177=EDGE_CURVE ( 'NONE', #67453, #32736, #14967, .T. ) ;
#35182=CYLINDRICAL_SURFACE ( 'NONE', #12215, 0.2500000000000002220 ) ;
#35183=DIRECTION ( 'NONE',  ( 1.000000000000000000, 7.709882115452468306E-16, -0.000000000000000000 ) ) ;
#35185=CIRCLE ( 'NONE', #48690, 0.2500000000000002220 ) ;
#35220=ORIENTED_EDGE ( 'NONE', *, *, #48408, .F. ) ;
#35235=DIRECTION ( 'NONE',  ( 1.000000000000000000, 0.000000000000000000, 0.000000000000000000 ) ) ;
#35252=ORIENTED_EDGE ( 'NONE', *, *, #40775, .F. ) ;
#35282=ORIENTED_EDGE ( 'NONE', *, *, #33410, .F. ) ;
#35324=AXIS2_PLACEMENT_3D ( 'NONE', #47925, #19736, #69326 ) ;
#35332=ORIENTED_EDGE ( 'NONE', *, *, #22847, .F. ) ;
#35358=DIRECTION ( 'NONE',  ( -1.000000000000000000, 7.709882115452468306E-16, 0.000000000000000000 ) ) ;
#35361=DIRECTION ( 'NONE',  ( 1.000000000000000000, 0.000000000000000000, 0.000000000000000000 ) ) ;
#35371=ORIENTED_EDGE ( 'NONE', *, *, #66901, .F. ) ;
#35373=EDGE_CURVE ( 'NONE', #68534, #69071, #60944, .T. ) ;
#35374=CYLINDRICAL_SURFACE ( 'NONE', #22625, 0.2500000000000002220 ) ;
#35382=CARTESIAN_POINT ( 'NONE',  ( 57.49999999999998579, 30.99999999999999289, 3.750000000000000000 ) ) ;
#35406=LINE ( 'NONE', #51932, #51193 ) ;
#35415=AXIS2_PLACEMENT_3D ( 'NONE', #36000, #24716, #42365 ) ;
#35418=CARTESIAN_POINT ( 'NONE',  ( 26.00000000000001066, 21.99999999999998224, 3.750000000000000000 ) ) ;
#35421=DIRECTION ( 'NONE',  ( 1.000000000000000000, -0.000000000000000000, 0.000000000000000000 ) ) ;
#35429=CIRCLE ( 'NONE', #55654, 0.5000000000000004441 ) ;
#35449=SPHERICAL_SURFACE ( 'NONE', #60880, 0.2500000000000000000 ) ;
#35451=ORIENTED_EDGE ( 'NONE', *, *, #25327, .T. ) ;
#35459=DIRECTION ( 'NONE',  ( 0.000000000000000000, 0.000000000000000000, 1.000000000000000000 ) ) ;
#35469=VERTEX_POINT ( 'NONE', #23493 ) ;
#35472=CARTESIAN_POINT ( 'NONE',  ( 57.74999999999998579, 30.74999999999999289, -4.000000000000000000 ) ) ;
#35476=CARTESIAN_POINT ( 'NONE',  ( 30.25000000000000711, 18.99999999999997868, -3.750000000000000000 ) ) ;
#35523=CARTESIAN_POINT ( 'NONE',  ( 21.50000000000001066, 24.99999999999998579, 3.750000000000000000 ) ) ;
#35543=ORIENTED_EDGE ( 'NONE', *, *, #39352, .F. ) ;
#35550=CARTESIAN_POINT ( 'NONE',  ( 57.24999999999999289, 28.24999999999998934, -4.000000000000000000 ) ) ;
#35586=SPHERICAL_SURFACE ( 'NONE', #43252, 0.2500000000000000000 ) ;
#35597=DIRECTION ( 'NONE',  ( 1.000000000000000000, 0.000000000000000000, 0.000000000000000000 ) ) ;
#35608=CARTESIAN_POINT ( 'NONE',  ( 48.49999999999999289, 24.74999999999998579, 3.750000000000000000 ) ) ;
#35618=DIRECTION ( 'NONE',  ( -1.000000000000000000, -7.709882115452469292E-16, 0.000000000000000000 ) ) ;
#35664=EDGE_CURVE ( 'NONE', #7106, #37864, #28597, .T. ) ;
#35667=ORIENTED_EDGE ( 'NONE', *, *, #23047, .T. ) ;
#35686=( LENGTH_UNIT ( ) NAMED_UNIT ( * ) SI_UNIT ( .MILLI., .METRE. ) );
#35705=EDGE_LOOP ( 'NONE', ( #31329, #36033, #35252, #28233 ) ) ;
#35717=AXIS2_PLACEMENT_3D ( 'NONE', #69149, #47753, #52969 ) ;
#35733=CARTESIAN_POINT ( 'NONE',  ( 68.99999999999998579, 1.000000000000008438, 4.000000000000000000 ) ) ;
#35737=DIRECTION ( 'NONE',  ( 0.000000000000000000, 0.000000000000000000, -1.000000000000000000 ) ) ;
#35742=EDGE_CURVE ( 'NONE', #33844, #17336, #18209, .T. ) ;
#35745=ORIENTED_EDGE ( 'NONE', *, *, #3691, .T. ) ;
#35774=CARTESIAN_POINT ( 'NONE',  ( 44.25000000000000000, 21.74999999999998579, -3.750000000000000000 ) ) ;
#35777=EDGE_LOOP ( 'NONE', ( #7267, #46065, #10090, #33001 ) ) ;
#35794=CARTESIAN_POINT ( 'NONE',  ( 53.25000000000005684, 1.231653667943533289E-13, 4.000000000000000000 ) ) ;
#35798=DIRECTION ( 'NONE',  ( 1.000000000000000000, 0.000000000000000000, -0.000000000000000000 ) ) ;
#35813=CYLINDRICAL_SURFACE ( 'NONE', #32144, 0.2500000000000002220 ) ;
#35816=DIRECTION ( 'NONE',  ( 1.000000000000000000, -0.000000000000000000, 0.000000000000000000 ) ) ;
#35819=DIRECTION ( 'NONE',  ( -1.000000000000000000, 0.000000000000000000, 0.000000000000000000 ) ) ;
#35822=CIRCLE ( 'NONE', #3230, 0.2500000000000002220 ) ;
#35824=DIRECTION ( 'NONE',  ( 0.000000000000000000, 0.000000000000000000, -1.000000000000000000 ) ) ;
#35906=ORIENTED_EDGE ( 'NONE', *, *, #41649, .T. ) ;
#35909=AXIS2_PLACEMENT_3D ( 'NONE', #30696, #8581, #3965 ) ;
#35915=LINE ( 'NONE', #57717, #31437 ) ;
#35933=ADVANCED_FACE ( 'NONE', ( #27128 ), #7092, .T. ) ;
#35934=CARTESIAN_POINT ( 'NONE',  ( 39.74999999999999289, 0.000000000000000000, 4.000000000000000000 ) ) ;
#35945=VECTOR ( 'NONE', #58423, 1000.000000000000000 ) ;
#35946=ORIENTED_EDGE ( 'NONE', *, *, #11505, .T. ) ;
#35957=AXIS2_PLACEMENT_3D ( 'NONE', #57053, #63020, #30293 ) ;
#35981=CARTESIAN_POINT ( 'NONE',  ( 48.25000000000000000, 22.24999999999998579, 4.000000000000000000 ) ) ;
#36000=CARTESIAN_POINT ( 'NONE',  ( 44.00000000000000000, 18.74999999999998224, -3.750000000000000000 ) ) ;
#36006=CARTESIAN_POINT ( 'NONE',  ( 53.00000000000000000, 25.24999999999998579, 4.000000000000000000 ) ) ;
#36016=ADVANCED_FACE ( 'NONE', ( #3490 ), #45794, .F. ) ;
#36017=DIRECTION ( 'NONE',  ( 7.709882115452468306E-16, -1.000000000000000000, 0.000000000000000000 ) ) ;
#36022=CARTESIAN_POINT ( 'NONE',  ( 3.249999999999998668, 36.99999999999999289, 4.000000000000000000 ) ) ;
#36033=ORIENTED_EDGE ( 'NONE', *, *, #5520, .F. ) ;
#36054=DIRECTION ( 'NONE',  ( -1.000000000000000000, -1.224646799147353207E-16, 0.000000000000000000 ) ) ;
#36061=AXIS2_PLACEMENT_3D ( 'NONE', #23467, #57938, #4076 ) ;
#36067=EDGE_CURVE ( 'NONE', #28627, #26545, #27263, .T. ) ;
#36072=COLOUR_RGB ( '', 0.09019608, 0.27058824, 0.51372549) ;
#36073=ORIENTED_EDGE ( 'NONE', *, *, #58691, .F. ) ;
#36077=CARTESIAN_POINT ( 'NONE',  ( 59.00000000000000000, 11.99999999999999822, 3.499999999999992895 ) ) ;
#36079=EDGE_CURVE ( 'NONE', #57523, #7926, #5951, .T. ) ;
#36097=AXIS2_PLACEMENT_3D ( 'NONE', #66505, #18325, #44746 ) ;
#36107=CIRCLE ( 'NONE', #64143, 0.5000000000000004441 ) ;
#36112=AXIS2_PLACEMENT_3D ( 'NONE', #56269, #8095, #24591 ) ;
#36154=EDGE_CURVE ( 'NONE', #22530, #7454, #40865, .T. ) ;
#36165=CARTESIAN_POINT ( 'NONE',  ( 66.74999999999998579, 36.75000000000000000, -3.750000000000000000 ) ) ;
#36179=AXIS2_PLACEMENT_3D ( 'NONE', #6771, #17707, #18030 ) ;
#36180=EDGE_CURVE ( 'NONE', #65996, #20493, #63259, .T. ) ;
#36198=ORIENTED_EDGE ( 'NONE', *, *, #59030, .F. ) ;
#36313=CARTESIAN_POINT ( 'NONE',  ( 10.99999999999999645, 11.99999999999999289, -3.499999999999991118 ) ) ;
#36317=CONICAL_SURFACE ( 'NONE', #46405, 3.600000000000005862, 0.7853981633974447263 ) ;
#36318=CIRCLE ( 'NONE', #10430, 0.5000000000000004441 ) ;
#36322=VERTEX_POINT ( 'NONE', #60117 ) ;
#36337=TOROIDAL_SURFACE ( 'NONE', #10497, 0.5000000000000000000, 0.2500000000000000000 ) ;
#36354=ORIENTED_EDGE ( 'NONE', *, *, #61433, .T. ) ;
#36356=EDGE_CURVE ( 'NONE', #3561, #11185, #35185, .T. ) ;
#36357=FACE_OUTER_BOUND ( 'NONE', #31661, .T. ) ;
#36373=VECTOR ( 'NONE', #41047, 1000.000000000000000 ) ;
#36374=AXIS2_PLACEMENT_3D ( 'NONE', #13022, #6105, #19330 ) ;
#36377=FACE_OUTER_BOUND ( 'NONE', #37500, .T. ) ;
#36379=VERTEX_POINT ( 'NONE', #32682 ) ;
#36382=FILL_AREA_STYLE ('',( #31378 ) ) ;
#36386=CARTESIAN_POINT ( 'NONE',  ( 66.74999999999998579, 36.75000000000000000, 3.750000000000000000 ) ) ;
#36394=DIRECTION ( 'NONE',  ( 0.000000000000000000, 0.000000000000000000, -1.000000000000000000 ) ) ;
#36402=AXIS2_PLACEMENT_3D ( 'NONE', #49898, #17551, #1642 ) ;
#36415=CYLINDRICAL_SURFACE ( 'NONE', #49242, 0.2500000000000002220 ) ;
#36438=ORIENTED_EDGE ( 'NONE', *, *, #37788, .T. ) ;
#36442=ORIENTED_EDGE ( 'NONE', *, *, #9246, .T. ) ;
#36444=VECTOR ( 'NONE', #7601, 1000.000000000000000 ) ;
#36457=CIRCLE ( 'NONE', #6075, 0.2500000000000002220 ) ;
#36465=CYLINDRICAL_SURFACE ( 'NONE', #46053, 0.2500000000000002220 ) ;
#36478=DIRECTION ( 'NONE',  ( 0.000000000000000000, 0.000000000000000000, -1.000000000000000000 ) ) ;
#36480=ORIENTED_EDGE ( 'NONE', *, *, #63216, .F. ) ;
#36514=FACE_OUTER_BOUND ( 'NONE', #34057, .T. ) ;
#36528=ORIENTED_EDGE ( 'NONE', *, *, #63368, .T. ) ;
#36556=DIRECTION ( 'NONE',  ( 0.000000000000000000, 0.000000000000000000, -1.000000000000000000 ) ) ;
#36584=EDGE_CURVE ( 'NONE', #30410, #57684, #59926, .T. ) ;
#36585=CARTESIAN_POINT ( 'NONE',  ( 57.49999999999999289, 28.24999999999998934, -3.750000000000000000 ) ) ;
#36604=ORIENTED_EDGE ( 'NONE', *, *, #64087, .F. ) ;
#36610=CARTESIAN_POINT ( 'NONE',  ( 68.99999999999998579, 1.000000000000008438, -3.000000000000000000 ) ) ;
#36611=DIRECTION ( 'NONE',  ( -1.000000000000000000, 0.000000000000000000, 0.000000000000000000 ) ) ;
#36614=ORIENTED_EDGE ( 'NONE', *, *, #67686, .T. ) ;
#36617=DIRECTION ( 'NONE',  ( 0.000000000000000000, 0.000000000000000000, -1.000000000000000000 ) ) ;
#36621=ORIENTED_EDGE ( 'NONE', *, *, #38732, .F. ) ;
#36624=ORIENTED_EDGE ( 'NONE', *, *, #19817, .T. ) ;
#36631=CARTESIAN_POINT ( 'NONE',  ( 1.000000000000000000, 0.000000000000000000, 4.000000000000000000 ) ) ;
#36649=AXIS2_PLACEMENT_3D ( 'NONE', #38692, #39368, #12940 ) ;
#36659=ORIENTED_EDGE ( 'NONE', *, *, #43649, .F. ) ;
#36668=DIRECTION ( 'NONE',  ( 5.782411586589351722E-16, -1.000000000000000000, -0.000000000000000000 ) ) ;
#36670=DIRECTION ( 'NONE',  ( -1.000000000000000000, 0.000000000000000000, 0.000000000000000000 ) ) ;
#36676=CYLINDRICAL_SURFACE ( 'NONE', #64474, 0.2500000000000002220 ) ;
#36684=CARTESIAN_POINT ( 'NONE',  ( 57.74999999999998579, 30.99999999999999289, -3.750000000000000000 ) ) ;
#36688=AXIS2_PLACEMENT_3D ( 'NONE', #53107, #4538, #14782 ) ;
#36732=FACE_OUTER_BOUND ( 'NONE', #20720, .T. ) ;
#36752=DIRECTION ( 'NONE',  ( -1.000000000000000000, 0.000000000000000000, 0.000000000000000000 ) ) ;
#36757=FACE_OUTER_BOUND ( 'NONE', #3363, .T. ) ;
#36758=EDGE_CURVE ( 'NONE', #46687, #3561, #49910, .T. ) ;
#36759=ORIENTED_EDGE ( 'NONE', *, *, #6486, .T. ) ;
#36764=VECTOR ( 'NONE', #14894, 1000.000000000000000 ) ;
#36767=LINE ( 'NONE', #20180, #58254 ) ;
#36768=CARTESIAN_POINT ( 'NONE',  ( 66.74999999999998579, 0.000000000000000000, 3.750000000000000000 ) ) ;
#36779=SURFACE_STYLE_FILL_AREA ( #49064 ) ;
#36802=DIRECTION ( 'NONE',  ( 0.000000000000000000, 0.000000000000000000, -1.000000000000000000 ) ) ;
#36804=CIRCLE ( 'NONE', #37914, 0.2500000000000002220 ) ;
#36822=AXIS2_PLACEMENT_3D ( 'NONE', #32673, #68953, #63994 ) ;
#36830=ORIENTED_EDGE ( 'NONE', *, *, #2415, .T. ) ;
#36831=DIRECTION ( 'NONE',  ( 0.000000000000000000, -0.000000000000000000, 1.000000000000000000 ) ) ;
#36869=CARTESIAN_POINT ( 'NONE',  ( 17.25000000000000711, 24.74999999999997868, 3.750000000000000000 ) ) ;
#36874=ORIENTED_EDGE ( 'NONE', *, *, #3213, .F. ) ;
#36877=CARTESIAN_POINT ( 'NONE',  ( 12.50000000000000533, 28.24999999999998224, 3.750000000000000000 ) ) ;
#36879=EDGE_CURVE ( 'NONE', #68764, #62693, #28338, .T. ) ;
#36881=ORIENTED_EDGE ( 'NONE', *, *, #23092, .T. ) ;
#36892=DIRECTION ( 'NONE',  ( -1.000000000000000000, -5.782411586589331015E-16, 0.000000000000000000 ) ) ;
#36907=CARTESIAN_POINT ( 'NONE',  ( 39.74999999999999289, 16.24999999999997513, 3.750000000000000000 ) ) ;
#36912=ORIENTED_EDGE ( 'NONE', *, *, #2824, .F. ) ;
#36915=ADVANCED_FACE ( 'NONE', ( #57894 ), #25856, .T. ) ;
#36933=EDGE_LOOP ( 'NONE', ( #68297, #27458, #28425, #42792, #60288, #7852 ) ) ;
#36947=ORIENTED_EDGE ( 'NONE', *, *, #21684, .T. ) ;
#36974=EDGE_CURVE ( 'NONE', #44704, #24621, #47366, .T. ) ;
#36975=ORIENTED_EDGE ( 'NONE', *, *, #42098, .T. ) ;
#36988=ORIENTED_EDGE ( 'NONE', *, *, #67147, .F. ) ;
#37003=VERTEX_POINT ( 'NONE', #47744 ) ;
#37017=FACE_OUTER_BOUND ( 'NONE', #1833, .T. ) ;
#37027=AXIS2_PLACEMENT_3D ( 'NONE', #12187, #22772, #18176 ) ;
#37029=EDGE_LOOP ( 'NONE', ( #50314, #2026, #1232, #13383 ) ) ;
#37031=FACE_OUTER_BOUND ( 'NONE', #52227, .T. ) ;
#37055=EDGE_CURVE ( 'NONE', #11185, #29083, #62242, .T. ) ;
#37058=DIRECTION ( 'NONE',  ( -1.000000000000000000, 0.000000000000000000, 0.000000000000000000 ) ) ;
#37074=ORIENTED_EDGE ( 'NONE', *, *, #20950, .T. ) ;
#37103=ORIENTED_EDGE ( 'NONE', *, *, #65982, .F. ) ;
#37107=DIRECTION ( 'NONE',  ( -1.000000000000000000, 0.000000000000000000, 0.000000000000000000 ) ) ;
#37113=DIRECTION ( 'NONE',  ( 0.000000000000000000, 0.000000000000000000, -1.000000000000000000 ) ) ;
#37117=FACE_OUTER_BOUND ( 'NONE', #57132, .T. ) ;
#37124=ORIENTED_EDGE ( 'NONE', *, *, #5192, .T. ) ;
#37141=DIRECTION ( 'NONE',  ( 0.000000000000000000, 0.000000000000000000, -1.000000000000000000 ) ) ;
#37153=DIRECTION ( 'NONE',  ( 1.000000000000000000, 0.000000000000000000, 0.000000000000000000 ) ) ;
#37168=ORIENTED_EDGE ( 'NONE', *, *, #69110, .F. ) ;
#37169=AXIS2_PLACEMENT_3D ( 'NONE', #29059, #18186, #61422 ) ;
#37176=CARTESIAN_POINT ( 'NONE',  ( 55.89999999999999147, 11.99999999999999822, -3.499999999999999556 ) ) ;
#37181=DIRECTION ( 'NONE',  ( -0.000000000000000000, -0.000000000000000000, -1.000000000000000000 ) ) ;
#37193=FACE_OUTER_BOUND ( 'NONE', #22204, .T. ) ;
#37202=CARTESIAN_POINT ( 'NONE',  ( 44.00000000000000000, 21.74999999999998579, 4.000000000000000000 ) ) ;
#37208=CARTESIAN_POINT ( 'NONE',  ( 66.74999999999998579, 34.24999999999999289, -4.000000000000000000 ) ) ;
#37225=ORIENTED_EDGE ( 'NONE', *, *, #10279, .T. ) ;
#37229=EDGE_CURVE ( 'NONE', #56118, #33883, #39927, .T. ) ;
#37230=FACE_OUTER_BOUND ( 'NONE', #57542, .T. ) ;
#37244=DIRECTION ( 'NONE',  ( 1.000000000000000000, 0.000000000000000000, -0.000000000000000000 ) ) ;
#37252=ORIENTED_EDGE ( 'NONE', *, *, #24081, .T. ) ;
#37256=DIRECTION ( 'NONE',  ( 5.782411586589351722E-16, -1.000000000000000000, 0.000000000000000000 ) ) ;
#37296=ADVANCED_FACE ( 'NONE', ( #45559 ), #49760, .T. ) ;
#37300=CYLINDRICAL_SURFACE ( 'NONE', #40851, 0.2500000000000002220 ) ;
#37326=AXIS2_PLACEMENT_3D ( 'NONE', #27763, #66468, #59807 ) ;
#37327=FACE_OUTER_BOUND ( 'NONE', #44092, .T. ) ;
#37329=VERTEX_POINT ( 'NONE', #23353 ) ;
#37347=SPHERICAL_SURFACE ( 'NONE', #63770, 0.2500000000000000000 ) ;
#37355=CYLINDRICAL_SURFACE ( 'NONE', #1610, 0.2500000000000002220 ) ;
#37357=EDGE_CURVE ( 'NONE', #31792, #42973, #10640, .T. ) ;
#37361=CARTESIAN_POINT ( 'NONE',  ( 61.99999999999998579, 33.99999999999999289, 4.000000000000000000 ) ) ;
#37375=SPHERICAL_SURFACE ( 'NONE', #68065, 0.2500000000000000000 ) ;
#37413=ADVANCED_FACE ( 'NONE', ( #56050 ), #50793, .F. ) ;
#37420=FILL_AREA_STYLE_COLOUR ( '', #42963 ) ;
#37460=CARTESIAN_POINT ( 'NONE',  ( 48.49999999999999289, 24.74999999999998579, 4.000000000000000000 ) ) ;
#37464=EDGE_CURVE ( 'NONE', #56343, #23940, #329, .T. ) ;
#37469=ADVANCED_FACE ( 'NONE', ( #22545 ), #11640, .T. ) ;
#37500=EDGE_LOOP ( 'NONE', ( #49389, #10349, #36438, #31397 ) ) ;
#37511=VECTOR ( 'NONE', #25067, 1000.000000000000000 ) ;
#37535=FACE_OUTER_BOUND ( 'NONE', #12343, .T. ) ;
#37543=DIRECTION ( 'NONE',  ( 1.000000000000000000, 0.000000000000000000, 0.000000000000000000 ) ) ;
#37577=ORIENTED_EDGE ( 'NONE', *, *, #40930, .F. ) ;
#37610=ORIENTED_EDGE ( 'NONE', *, *, #30716, .T. ) ;
#37639=VECTOR ( 'NONE', #62458, 1000.000000000000000 ) ;
#37654=LINE ( 'NONE', #69600, #44253 ) ;
#37668=( NAMED_UNIT ( * ) PLANE_ANGLE_UNIT ( ) SI_UNIT ( $, .RADIAN. ) );
#37719=EDGE_CURVE ( 'NONE', #47990, #49817, #20543, .T. ) ;
#37720=CARTESIAN_POINT ( 'NONE',  ( 1.908195823574488119E-14, 24.75000000000002487, 3.750000000000000000 ) ) ;
#37721=CYLINDRICAL_SURFACE ( 'NONE', #52826, 0.2500000000000002220 ) ;
#37744=VERTEX_POINT ( 'NONE', #52914 ) ;
#37764=EDGE_LOOP ( 'NONE', ( #55520, #34196, #62622, #54420 ) ) ;
#37788=EDGE_CURVE ( 'NONE', #2804, #65448, #5997, .T. ) ;
#37797=LINE ( 'NONE', #43072, #63914 ) ;
#37831=FACE_OUTER_BOUND ( 'NONE', #466, .T. ) ;
#37834=ADVANCED_FACE ( 'NONE', ( #37117 ), #47691, .T. ) ;
#37864=VERTEX_POINT ( 'NONE', #7482 ) ;
#37874=EDGE_LOOP ( 'NONE', ( #3220, #10102, #41357, #64331, #41812, #44780 ) ) ;
#37882=CONICAL_SURFACE ( 'NONE', #59146, 3.599999999999992095, 0.7853981633974375098 ) ;
#37894=CARTESIAN_POINT ( 'NONE',  ( 26.00000000000001066, 19.24999999999997868, -4.000000000000000000 ) ) ;
#37906=ORIENTED_EDGE ( 'NONE', *, *, #54926, .F. ) ;
#37914=AXIS2_PLACEMENT_3D ( 'NONE', #47918, #21457, #21113 ) ;
#37919=DIRECTION ( 'NONE',  ( -1.000000000000000000, 0.000000000000000000, 0.000000000000000000 ) ) ;
#37929=LINE ( 'NONE', #32956, #32451 ) ;
#37945=DIRECTION ( 'NONE',  ( 1.000000000000000000, 0.000000000000000000, 0.000000000000000000 ) ) ;
#37989=VERTEX_POINT ( 'NONE', #51433 ) ;
#37995=EDGE_LOOP ( 'NONE', ( #42448, #12865, #192, #69515 ) ) ;
#38009=EDGE_LOOP ( 'NONE', ( #50489, #10125, #37168, #35667 ) ) ;
#38010=LINE ( 'NONE', #4195, #48693 ) ;
#38033=SPHERICAL_SURFACE ( 'NONE', #63439, 1.000000000000000000 ) ;
#38044=DIRECTION ( 'NONE',  ( 0.000000000000000000, -1.000000000000000000, 0.000000000000000000 ) ) ;
#38045=DIRECTION ( 'NONE',  ( -0.000000000000000000, 0.000000000000000000, -1.000000000000000000 ) ) ;
#38063=LINE ( 'NONE', #22904, #32720 ) ;
#38080=ORIENTED_EDGE ( 'NONE', *, *, #24228, .F. ) ;
#38081=ADVANCED_FACE ( 'NONE', ( #37031 ), #52841, .T. ) ;
#38087=LINE ( 'NONE', #5324, #39746 ) ;
#38096=CARTESIAN_POINT ( 'NONE',  ( 48.74999999999999289, 24.74999999999998579, 3.750000000000000000 ) ) ;
#38116=VERTEX_POINT ( 'NONE', #15559 ) ;
#38120=DIRECTION ( 'NONE',  ( 0.000000000000000000, 0.000000000000000000, -1.000000000000000000 ) ) ;
#38142=VERTEX_POINT ( 'NONE', #32056 ) ;
#38157=DIRECTION ( 'NONE',  ( 0.000000000000000000, 0.000000000000000000, 1.000000000000000000 ) ) ;
#38162=ORIENTED_EDGE ( 'NONE', *, *, #26119, .F. ) ;
#38177=ORIENTED_EDGE ( 'NONE', *, *, #65202, .T. ) ;
#38209=VECTOR ( 'NONE', #34198, 1000.000000000000000 ) ;
#38245=DIRECTION ( 'NONE',  ( 0.000000000000000000, 0.000000000000000000, 1.000000000000000000 ) ) ;
#38251=EDGE_LOOP ( 'NONE', ( #12581, #11625 ) ) ;
#38254=LINE ( 'NONE', #22039, #40627 ) ;
#38266=DIRECTION ( 'NONE',  ( -1.000000000000000000, -1.224646799147353207E-16, 0.000000000000000000 ) ) ;
#38267=EDGE_CURVE ( 'NONE', #32231, #41879, #49906, .T. ) ;
#38293=CARTESIAN_POINT ( 'NONE',  ( 30.25000000000001066, 16.24999999999997513, 4.000000000000000000 ) ) ;
#38297=ORIENTED_EDGE ( 'NONE', *, *, #40417, .F. ) ;
#38304=CIRCLE ( 'NONE', #40550, 0.2500000000000002220 ) ;
#38311=CIRCLE ( 'NONE', #24743, 0.2500000000000002220 ) ;
#38319=EDGE_CURVE ( 'NONE', #65448, #61448, #54394, .T. ) ;
#38338=DIRECTION ( 'NONE',  ( 0.000000000000000000, 0.000000000000000000, 1.000000000000000000 ) ) ;
#38339=ORIENTED_EDGE ( 'NONE', *, *, #8515, .T. ) ;
#38340=CARTESIAN_POINT ( 'NONE',  ( 26.25000000000001066, 18.74999999999997868, 3.750000000000000000 ) ) ;
#38349=AXIS2_PLACEMENT_3D ( 'NONE', #33347, #2673, #28029 ) ;
#38358=DIRECTION ( 'NONE',  ( -0.000000000000000000, 0.000000000000000000, -1.000000000000000000 ) ) ;
#38365=ORIENTED_EDGE ( 'NONE', *, *, #5886, .T. ) ;
#38381=EDGE_LOOP ( 'NONE', ( #58827, #8725, #57039, #18159 ) ) ;
#38382=CARTESIAN_POINT ( 'NONE',  ( 44.00000000000000000, 19.24999999999998224, -3.750000000000000000 ) ) ;
#38385=ORIENTED_EDGE ( 'NONE', *, *, #61308, .F. ) ;
#38388=DIRECTION ( 'NONE',  ( 1.000000000000000000, 7.709882115452469292E-16, 0.000000000000000000 ) ) ;
#38392=DIRECTION ( 'NONE',  ( 0.000000000000000000, 0.000000000000000000, 1.000000000000000000 ) ) ;
#38406=CARTESIAN_POINT ( 'NONE',  ( 52.99999999999999289, 27.99999999999998579, 4.000000000000000000 ) ) ;
#38407=AXIS2_PLACEMENT_3D ( 'NONE', #24105, #67027, #18819 ) ;
#38416=CARTESIAN_POINT ( 'NONE',  ( 16.75000000000000711, 25.24999999999998224, -4.000000000000000000 ) ) ;
#38420=ORIENTED_EDGE ( 'NONE', *, *, #57205, .T. ) ;
#38421=ORIENTED_EDGE ( 'NONE', *, *, #48686, .F. ) ;
#38424=DIRECTION ( 'NONE',  ( -1.000000000000000000, 0.000000000000000000, 0.000000000000000000 ) ) ;
#38430=ADVANCED_FACE ( 'NONE', ( #7735 ), #56627, .T. ) ;
#38433=EDGE_LOOP ( 'NONE', ( #41730, #9691, #64759, #51244 ) ) ;
#38450=ORIENTED_EDGE ( 'NONE', *, *, #65668, .F. ) ;
#38460=CARTESIAN_POINT ( 'NONE',  ( 8.250000000000001776, 30.99999999999998579, 4.000000000000000000 ) ) ;
#38478=CYLINDRICAL_SURFACE ( 'NONE', #19379, 0.2500000000000002220 ) ;
#38504=ORIENTED_EDGE ( 'NONE', *, *, #52980, .F. ) ;
#38510=LINE ( 'NONE', #59903, #53960 ) ;
#38537=DIRECTION ( 'NONE',  ( 0.000000000000000000, 0.000000000000000000, -1.000000000000000000 ) ) ;
#38584=MECHANICAL_DESIGN_GEOMETRIC_PRESENTATION_REPRESENTATION('',(#3644),#16070);
#38601=CARTESIAN_POINT ( 'NONE',  ( 61.74999999999998579, 31.24999999999999289, 4.000000000000000000 ) ) ;
#38605=ORIENTED_EDGE ( 'NONE', *, *, #13785, .T. ) ;
#38607=DIRECTION ( 'NONE',  ( -0.000000000000000000, 1.000000000000000000, -0.000000000000000000 ) ) ;
#38613=ORIENTED_EDGE ( 'NONE', *, *, #29451, .F. ) ;
#38614=EDGE_CURVE ( 'NONE', #37329, #47990, #66760, .T. ) ;
#38615=VECTOR ( 'NONE', #54416, 1000.000000000000000 ) ;
#38618=DIRECTION ( 'NONE',  ( 0.000000000000000000, 0.000000000000000000, 1.000000000000000000 ) ) ;
#38633=DIRECTION ( 'NONE',  ( 0.000000000000000000, 1.000000000000000000, 0.000000000000000000 ) ) ;
#38646=CARTESIAN_POINT ( 'NONE',  ( 69.74999999999998579, 37.00000000000000000, 3.000000000000000000 ) ) ;
#38652=EDGE_CURVE ( 'NONE', #23317, #44704, #28573, .T. ) ;
#38659=CIRCLE ( 'NONE', #23993, 0.2500000000000002220 ) ;
#38688=ORIENTED_EDGE ( 'NONE', *, *, #49426, .F. ) ;
#38692=CARTESIAN_POINT ( 'NONE',  ( 57.74999999999998579, 30.74999999999999289, -3.750000000000000000 ) ) ;
#38698=ORIENTED_EDGE ( 'NONE', *, *, #15369, .T. ) ;
#38699=DIRECTION ( 'NONE',  ( -0.000000000000000000, -0.000000000000000000, -1.000000000000000000 ) ) ;
#38701=AXIS2_PLACEMENT_3D ( 'NONE', #9919, #67974, #41254 ) ;
#38726=EDGE_CURVE ( 'NONE', #46628, #69646, #3280, .T. ) ;
#38729=ORIENTED_EDGE ( 'NONE', *, *, #10104, .F. ) ;
#38732=EDGE_CURVE ( 'NONE', #59828, #21622, #51886, .T. ) ;
#38734=AXIS2_PLACEMENT_3D ( 'NONE', #13189, #34647, #56105 ) ;
#38737=ORIENTED_EDGE ( 'NONE', *, *, #25650, .F. ) ;
#38738=ADVANCED_FACE ( 'NONE', ( #4338 ), #24768, .T. ) ;
#38759=EDGE_CURVE ( 'NONE', #28382, #51968, #25819, .T. ) ;
#38772=TOROIDAL_SURFACE ( 'NONE', #8419, 0.5000000000000000000, 0.2500000000000000000 ) ;
#38787=PLANE ( 'NONE',  #26072 ) ;
#38794=CYLINDRICAL_SURFACE ( 'NONE', #41268, 0.2500000000000002220 ) ;
#38797=ORIENTED_EDGE ( 'NONE', *, *, #59817, .T. ) ;
#38827=VECTOR ( 'NONE', #64637, 1000.000000000000000 ) ;
#38849=ORIENTED_EDGE ( 'NONE', *, *, #43649, .T. ) ;
#38867=ADVANCED_FACE ( 'NONE', ( #21954 ), #69088, .F. ) ;
#38889=CARTESIAN_POINT ( 'NONE',  ( 30.25000000000001066, 16.24999999999997513, -3.750000000000000000 ) ) ;
#38910=DIRECTION ( 'NONE',  ( 0.000000000000000000, 0.000000000000000000, 1.000000000000000000 ) ) ;
#38945=CARTESIAN_POINT ( 'NONE',  ( 53.24999999999999289, 27.99999999999998579, -3.750000000000000000 ) ) ;
#38955=EDGE_CURVE ( 'NONE', #31454, #55156, #7313, .T. ) ;
#38967=VECTOR ( 'NONE', #35798, 1000.000000000000000 ) ;
#38986=CARTESIAN_POINT ( 'NONE',  ( 68.99999999999998579, 1.000000000000008438, -3.000000000000000000 ) ) ;
#38988=VERTEX_POINT ( 'NONE', #24682 ) ;
#38996=DIRECTION ( 'NONE',  ( 1.000000000000000000, 0.000000000000000000, -0.000000000000000000 ) ) ;
#39000=VECTOR ( 'NONE', #16022, 1000.000000000000000 ) ;
#39010=VECTOR ( 'NONE', #57722, 1000.000000000000114 ) ;
#39013=ORIENTED_EDGE ( 'NONE', *, *, #4094, .T. ) ;
#39026=CARTESIAN_POINT ( 'NONE',  ( 44.00000000000000000, 21.99999999999998579, 3.750000000000000000 ) ) ;
#39033=ORIENTED_EDGE ( 'NONE', *, *, #15385, .F. ) ;
#39047=ORIENTED_EDGE ( 'NONE', *, *, #42157, .T. ) ;
#39061=AXIS2_PLACEMENT_3D ( 'NONE', #21341, #66334, #11834 ) ;
#39067=DIRECTION ( 'NONE',  ( 0.000000000000000000, 0.000000000000000000, 1.000000000000000000 ) ) ;
#39137=DIRECTION ( 'NONE',  ( -2.312964634635740689E-15, 1.000000000000000000, 0.000000000000000000 ) ) ;
#39141=CARTESIAN_POINT ( 'NONE',  ( 61.99999999999998579, 33.74999999999999289, 3.750000000000000000 ) ) ;
#39170=SPHERICAL_SURFACE ( 'NONE', #27582, 0.2500000000000000000 ) ;
#39181=ADVANCED_FACE ( 'NONE', ( #69364 ), #7370, .T. ) ;
#39209=ORIENTED_EDGE ( 'NONE', *, *, #17180, .F. ) ;
#39216=ORIENTED_EDGE ( 'NONE', *, *, #55269, .F. ) ;
#39217=AXIS2_PLACEMENT_3D ( 'NONE', #14031, #19646, #68538 ) ;
#39254=DIRECTION ( 'NONE',  ( -1.000000000000000000, 0.000000000000000000, 0.000000000000000000 ) ) ;
#39269=EDGE_LOOP ( 'NONE', ( #30694, #62016, #62758 ) ) ;
#39275=CYLINDRICAL_SURFACE ( 'NONE', #65258, 0.2500000000000002220 ) ;
#39296=VERTEX_POINT ( 'NONE', #39804 ) ;
#39314=DIRECTION ( 'NONE',  ( 0.000000000000000000, 0.000000000000000000, -1.000000000000000000 ) ) ;
#39315=CARTESIAN_POINT ( 'NONE',  ( 21.25000000000001066, 24.74999999999998224, 3.750000000000000000 ) ) ;
#39322=CIRCLE ( 'NONE', #48323, 0.2500000000000002220 ) ;
#39344=EDGE_CURVE ( 'NONE', #57903, #35167, #54880, .T. ) ;
#39352=EDGE_CURVE ( 'NONE', #59935, #22202, #9161, .T. ) ;
#39368=DIRECTION ( 'NONE',  ( 0.000000000000000000, 1.000000000000000000, 0.000000000000000000 ) ) ;
#39375=EDGE_LOOP ( 'NONE', ( #52949, #14002, #20091, #47357, #26524, #14104, #13746, #32429, #42502, #26389, #46572, #36881, #8700, #28753, #58974, #30483, #47427, #64896, #5920, #63632, #19269, #30157, #47433, #989, #51096, #43388, #51368, #69595, #288, #18029, #21802, #12671, #60455, #68421, #9143, #29299, #48053, #34491, #14080, #15924, #7546, #22458, #52451, #56107, #1951, #32676 ) ) ;
#39377=SPHERICAL_SURFACE ( 'NONE', #46974, 0.2500000000000000000 ) ;
#39408=AXIS2_PLACEMENT_3D ( 'NONE', #11251, #54504, #32699 ) ;
#39425=EDGE_CURVE ( 'NONE', #33800, #51729, #3107, .T. ) ;
#39437=AXIS2_PLACEMENT_3D ( 'NONE', #26827, #21584, #42060 ) ;
#39438=EDGE_CURVE ( 'NONE', #18810, #26382, #46476, .T. ) ;
#39444=FACE_OUTER_BOUND ( 'NONE', #51778, .T. ) ;
#39446=FACE_OUTER_BOUND ( 'NONE', #54375, .T. ) ;
#39469=DIRECTION ( 'NONE',  ( 1.000000000000000000, -0.000000000000000000, 0.000000000000000000 ) ) ;
#39481=ORIENTED_EDGE ( 'NONE', *, *, #24081, .F. ) ;
#39482=EDGE_CURVE ( 'NONE', #7454, #13649, #24602, .T. ) ;
#39483=AXIS2_PLACEMENT_3D ( 'NONE', #643, #60815, #22169 ) ;
#39486=ORIENTED_EDGE ( 'NONE', *, *, #55440, .F. ) ;
#39495=CIRCLE ( 'NONE', #15889, 0.2500000000000002220 ) ;
#39500=SPHERICAL_SURFACE ( 'NONE', #41566, 0.2500000000000000000 ) ;
#39546=AXIS2_PLACEMENT_3D ( 'NONE', #48488, #187, #5173 ) ;
#39555=ORIENTED_EDGE ( 'NONE', *, *, #62572, .T. ) ;
#39586=DIRECTION ( 'NONE',  ( 0.000000000000000000, 0.000000000000000000, -1.000000000000000000 ) ) ;
#39626=CARTESIAN_POINT ( 'NONE',  ( 0.000000000000000000, 36.74999999999999289, -3.750000000000000000 ) ) ;
#39629=FILL_AREA_STYLE_COLOUR ( '', #47486 ) ;
#39634=PLANE ( 'NONE',  #3671 ) ;
#39642=EDGE_CURVE ( 'NONE', #14417, #42069, #63646, .T. ) ;
#39645=CARTESIAN_POINT ( 'NONE',  ( 66.74999999999998579, 36.75000000000000000, -3.750000000000000000 ) ) ;
#39656=DIRECTION ( 'NONE',  ( 0.000000000000000000, 1.000000000000000000, -0.000000000000000000 ) ) ;
#39658=EDGE_CURVE ( 'NONE', #11473, #68610, #64709, .T. ) ;
#39674=CARTESIAN_POINT ( 'NONE',  ( 21.75000000000001066, 21.74999999999998224, -3.750000000000000000 ) ) ;
#39685=CARTESIAN_POINT ( 'NONE',  ( 0.2500000000000000000, 36.99999999999999289, 3.000000000000000000 ) ) ;
#39686=DIRECTION ( 'NONE',  ( 0.000000000000000000, -1.000000000000000000, 0.000000000000000000 ) ) ;
#39701=VERTEX_POINT ( 'NONE', #6604 ) ;
#39703=DIRECTION ( 'NONE',  ( 1.000000000000000000, 0.000000000000000000, 0.000000000000000000 ) ) ;
#39704=ORIENTED_EDGE ( 'NONE', *, *, #12694, .F. ) ;
#39710=AXIS2_PLACEMENT_3D ( 'NONE', #62953, #57340, #52446 ) ;
#39722=CARTESIAN_POINT ( 'NONE',  ( 52.75000000000000000, 25.24999999999998579, -3.750000000000000000 ) ) ;
#39732=DIRECTION ( 'NONE',  ( 0.000000000000000000, -1.000000000000000000, 0.000000000000000000 ) ) ;
#39738=ORIENTED_EDGE ( 'NONE', *, *, #52310, .F. ) ;
#39740=CARTESIAN_POINT ( 'NONE',  ( 10.99999999999999645, 11.99999999999999289, -4.000000000000000000 ) ) ;
#39746=VECTOR ( 'NONE', #53869, 1000.000000000000000 ) ;
#39753=EDGE_CURVE ( 'NONE', #34416, #48755, #1651, .T. ) ;
#39759=VECTOR ( 'NONE', #11159, 1000.000000000000000 ) ;
#39769=ADVANCED_FACE ( 'NONE', ( #598 ), #22464, .T. ) ;
#39797=PLANE ( 'NONE',  #25122 ) ;
#39803=DIRECTION ( 'NONE',  ( 0.000000000000000000, 0.000000000000000000, -1.000000000000000000 ) ) ;
#39804=CARTESIAN_POINT ( 'NONE',  ( 48.25000000000000000, 21.99999999999998579, 3.750000000000000000 ) ) ;
#39805=ORIENTED_EDGE ( 'NONE', *, *, #65686, .F. ) ;
#39817=ORIENTED_EDGE ( 'NONE', *, *, #47574, .F. ) ;
#39837=EDGE_CURVE ( 'NONE', #26382, #31359, #54794, .T. ) ;
#39855=ADVANCED_FACE ( 'NONE', ( #59745 ), #11554, .T. ) ;
#39884=DIRECTION ( 'NONE',  ( 0.000000000000000000, 0.000000000000000000, 1.000000000000000000 ) ) ;
#39920=EDGE_LOOP ( 'NONE', ( #54199, #25719, #64063, #25145 ) ) ;
#39927=LINE ( 'NONE', #44856, #25231 ) ;
#39981=CYLINDRICAL_SURFACE ( 'NONE', #32111, 0.2500000000000002220 ) ;
#39996=EDGE_LOOP ( 'NONE', ( #22191, #14795, #22249, #55936 ) ) ;
#40000=ORIENTED_EDGE ( 'NONE', *, *, #47980, .T. ) ;
#40017=CARTESIAN_POINT ( 'NONE',  ( 39.49999999999999289, 16.24999999999997513, -3.750000000000000000 ) ) ;
#40044=PLANE ( 'NONE',  #38349 ) ;
#40053=FACE_OUTER_BOUND ( 'NONE', #6950, .T. ) ;
#40055=EDGE_CURVE ( 'NONE', #41886, #4261, #29902, .T. ) ;
#40056=ORIENTED_EDGE ( 'NONE', *, *, #38267, .F. ) ;
#40063=DIRECTION ( 'NONE',  ( 7.709882115452441682E-16, -1.000000000000000000, 0.000000000000000000 ) ) ;
#40064=VECTOR ( 'NONE', #23175, 1000.000000000000000 ) ;
#40079=LINE ( 'NONE', #56197, #22173 ) ;
#40092=ORIENTED_EDGE ( 'NONE', *, *, #33291, .F. ) ;
#40096=LINE ( 'NONE', #57630, #55888 ) ;
#40100=PRESENTATION_STYLE_ASSIGNMENT (( #60136 ) ) ;
#40124=EDGE_LOOP ( 'NONE', ( #4386, #62142, #39216, #16454 ) ) ;
#40132=ORIENTED_EDGE ( 'NONE', *, *, #1504, .F. ) ;
#40155=DIRECTION ( 'NONE',  ( 0.000000000000000000, -0.000000000000000000, -1.000000000000000000 ) ) ;
#40175=CARTESIAN_POINT ( 'NONE',  ( 48.74999999999999289, 24.74999999999998579, 3.750000000000000000 ) ) ;
#40195=VECTOR ( 'NONE', #24218, 1000.000000000000000 ) ;
#40202=VERTEX_POINT ( 'NONE', #59294 ) ;
#40204=EDGE_CURVE ( 'NONE', #12261, #50231, #51292, .T. ) ;
#40207=DIRECTION ( 'NONE',  ( -1.445602896647337931E-16, 1.000000000000000000, 0.000000000000000000 ) ) ;
#40210=CYLINDRICAL_SURFACE ( 'NONE', #59990, 0.2500000000000002220 ) ;
#40218=ADVANCED_FACE ( 'NONE', ( #60347 ), #12154, .T. ) ;
#40227=DIRECTION ( 'NONE',  ( 0.000000000000000000, 1.000000000000000000, 0.000000000000000000 ) ) ;
#40241=ORIENTED_EDGE ( 'NONE', *, *, #65758, .F. ) ;
#40273=SHAPE_REPRESENTATION_RELATIONSHIP ( 'NONE' , 'NONE' ,  #21315, #28762 ) ;
#40274=FACE_OUTER_BOUND ( 'NONE', #9893, .T. ) ;
#40281=VERTEX_POINT ( 'NONE', #35010 ) ;
#40295=ORIENTED_EDGE ( 'NONE', *, *, #1464, .T. ) ;
#40309=SURFACE_SIDE_STYLE ('',( #13546 ) ) ;
#40315=CIRCLE ( 'NONE', #32445, 0.2500000000000002220 ) ;
#40320=AXIS2_PLACEMENT_3D ( 'NONE', #31917, #37945, #5175 ) ;
#40321=CYLINDRICAL_SURFACE ( 'NONE', #32490, 0.2500000000000002220 ) ;
#40331=AXIS2_PLACEMENT_3D ( 'NONE', #1579, #49495, #1224 ) ;
#40361=DIRECTION ( 'NONE',  ( 1.000000000000000000, 1.224646799147353207E-16, 0.000000000000000000 ) ) ;
#40372=ORIENTED_EDGE ( 'NONE', *, *, #58166, .T. ) ;
#40373=CIRCLE ( 'NONE', #52731, 1.000000000000000000 ) ;
#40386=DIRECTION ( 'NONE',  ( 1.000000000000000000, 0.000000000000000000, 0.000000000000000000 ) ) ;
#40387=EDGE_LOOP ( 'NONE', ( #49198, #51051, #59218, #69639 ) ) ;
#40403=AXIS2_PLACEMENT_3D ( 'NONE', #42812, #20962, #16055 ) ;
#40407=EDGE_LOOP ( 'NONE', ( #24274, #28916, #66087, #30851 ) ) ;
#40415=EDGE_LOOP ( 'NONE', ( #36830, #4520, #54710, #43954 ) ) ;
#40417=EDGE_CURVE ( 'NONE', #49817, #11185, #49000, .T. ) ;
#40419=( NAMED_UNIT ( * ) PLANE_ANGLE_UNIT ( ) SI_UNIT ( $, .RADIAN. ) );
#40424=DIRECTION ( 'NONE',  ( -0.000000000000000000, -0.000000000000000000, 1.000000000000000000 ) ) ;
#40462=VECTOR ( 'NONE', #36752, 1000.000000000000000 ) ;
#40463=EDGE_CURVE ( 'NONE', #28627, #2770, #32084, .T. ) ;
#40464=CARTESIAN_POINT ( 'NONE',  ( 16.75000000000000711, 27.74999999999998224, -3.750000000000000000 ) ) ;
#40466=CARTESIAN_POINT ( 'NONE',  ( 39.74999999999999289, 18.99999999999997868, -3.750000000000000000 ) ) ;
#40467=ORIENTED_EDGE ( 'NONE', *, *, #33410, .T. ) ;
#40476=CARTESIAN_POINT ( 'NONE',  ( 43.75000000000000000, 19.24999999999998224, 3.750000000000000000 ) ) ;
#40494=ORIENTED_EDGE ( 'NONE', *, *, #68046, .F. ) ;
#40498=EDGE_LOOP ( 'NONE', ( #31036, #54116, #37225, #48894 ) ) ;
#40502=AXIS2_PLACEMENT_3D ( 'NONE', #16762, #49453, #1880 ) ;
#40505=DIRECTION ( 'NONE',  ( -1.000000000000000000, 0.000000000000000000, 0.000000000000000000 ) ) ;
#40513=ORIENTED_EDGE ( 'NONE', *, *, #66901, .T. ) ;
#40526=ORIENTED_EDGE ( 'NONE', *, *, #39658, .T. ) ;
#40531=DIRECTION ( 'NONE',  ( 0.000000000000000000, 0.000000000000000000, -1.000000000000000000 ) ) ;
#40550=AXIS2_PLACEMENT_3D ( 'NONE', #32141, #25813, #58526 ) ;
#40607=VECTOR ( 'NONE', #45916, 1000.000000000000000 ) ;
#40627=VECTOR ( 'NONE', #9768, 1000.000000000000000 ) ;
#40628=EDGE_CURVE ( 'NONE', #30410, #19536, #45753, .T. ) ;
#40656=CIRCLE ( 'NONE', #65335, 0.2500000000000002220 ) ;
#40660=AXIS2_PLACEMENT_3D ( 'NONE', #4651, #47275, #63053 ) ;
#40667=( LENGTH_UNIT ( ) NAMED_UNIT ( * ) SI_UNIT ( .MILLI., .METRE. ) );
#40674=ORIENTED_EDGE ( 'NONE', *, *, #56795, .T. ) ;
#40679=AXIS2_PLACEMENT_3D ( 'NONE', #9762, #4431, #63554 ) ;
#40680=LINE ( 'NONE', #51218, #44326 ) ;
#40681=EDGE_CURVE ( 'NONE', #51630, #33237, #25521, .T. ) ;
#40730=SPHERICAL_SURFACE ( 'NONE', #53247, 0.2500000000000000000 ) ;
#40761=DIRECTION ( 'NONE',  ( 0.000000000000000000, 1.000000000000000000, 0.000000000000000000 ) ) ;
#40770=DIRECTION ( 'NONE',  ( 1.000000000000000000, 0.000000000000000000, 0.000000000000000000 ) ) ;
#40775=EDGE_CURVE ( 'NONE', #51660, #41879, #18751, .T. ) ;
#40776=VECTOR ( 'NONE', #67922, 1000.000000000000000 ) ;
#40814=ORIENTED_EDGE ( 'NONE', *, *, #68246, .T. ) ;
#40818=DIRECTION ( 'NONE',  ( -1.000000000000000000, 0.000000000000000000, 0.000000000000000000 ) ) ;
#40836=DIRECTION ( 'NONE',  ( 1.000000000000000000, 0.000000000000000000, 0.000000000000000000 ) ) ;
#40838=VERTEX_POINT ( 'NONE', #9172 ) ;
#40851=AXIS2_PLACEMENT_3D ( 'NONE', #53440, #5222, #26667 ) ;
#40858=CARTESIAN_POINT ( 'NONE',  ( 69.74999999999998579, 36.75000000000000000, 3.000000000000000000 ) ) ;
#40865=LINE ( 'NONE', #55961, #25098 ) ;
#40880=DIRECTION ( 'NONE',  ( -0.000000000000000000, 0.000000000000000000, -1.000000000000000000 ) ) ;
#40896=EDGE_CURVE ( 'NONE', #29039, #24476, #60363, .T. ) ;
#40921=EDGE_LOOP ( 'NONE', ( #5473, #36604, #41471, #6811 ) ) ;
#40926=LINE ( 'NONE', #66944, #68578 ) ;
#40927=DIRECTION ( 'NONE',  ( 0.000000000000000000, -1.000000000000000000, 0.000000000000000000 ) ) ;
#40930=EDGE_CURVE ( 'NONE', #48045, #42659, #63658, .T. ) ;
#40936=FACE_OUTER_BOUND ( 'NONE', #34037, .T. ) ;
#40937=ADVANCED_FACE ( 'NONE', ( #259 ), #64350, .T. ) ;
#40942=ORIENTED_EDGE ( 'NONE', *, *, #14891, .T. ) ;
#40947=ORIENTED_EDGE ( 'NONE', *, *, #69423, .F. ) ;
#40972=CARTESIAN_POINT ( 'NONE',  ( 43.75000000000000000, 19.24999999999998224, -4.000000000000000000 ) ) ;
#40975=AXIS2_PLACEMENT_3D ( 'NONE', #2823, #12719, #40531 ) ;
#40985=ADVANCED_FACE ( 'NONE', ( #10204 ), #18796, .T. ) ;
#40997=SHAPE_DEFINITION_REPRESENTATION ( #63040, #21315 ) ;
#41039=VECTOR ( 'NONE', #46932, 1000.000000000000000 ) ;
#41047=DIRECTION ( 'NONE',  ( 5.782411586589351722E-16, -1.000000000000000000, -0.000000000000000000 ) ) ;
#41058=CARTESIAN_POINT ( 'NONE',  ( 8.250000000000001776, 30.99999999999998579, 3.750000000000000000 ) ) ;
#41076=DIRECTION ( 'NONE',  ( -1.000000000000000000, 0.000000000000000000, 0.000000000000000000 ) ) ;
#41130=CARTESIAN_POINT ( 'NONE',  ( 61.74999999999998579, 31.24999999999999289, -3.750000000000000000 ) ) ;
#41132=EDGE_LOOP ( 'NONE', ( #5603, #33696, #10496, #7188 ) ) ;
#41146=FACE_OUTER_BOUND ( 'NONE', #10959, .T. ) ;
#41177=VERTEX_POINT ( 'NONE', #28773 ) ;
#41180=ADVANCED_FACE ( 'NONE', ( #7346 ), #39377, .T. ) ;
#41181=DIRECTION ( 'NONE',  ( 0.000000000000000000, 0.000000000000000000, -1.000000000000000000 ) ) ;
#41182=DIRECTION ( 'NONE',  ( -0.000000000000000000, -0.000000000000000000, 1.000000000000000000 ) ) ;
#41208=DIRECTION ( 'NONE',  ( -1.000000000000000000, -7.709882115452468306E-16, 0.000000000000000000 ) ) ;
#41243=CARTESIAN_POINT ( 'NONE',  ( 39.74999999999999289, 16.24999999999997513, 4.000000000000000000 ) ) ;
#41247=ORIENTED_EDGE ( 'NONE', *, *, #32392, .T. ) ;
#41254=DIRECTION ( 'NONE',  ( 0.000000000000000000, 0.000000000000000000, -1.000000000000000000 ) ) ;
#41261=EDGE_CURVE ( 'NONE', #25473, #50390, #40079, .T. ) ;
#41265=EDGE_CURVE ( 'NONE', #24621, #7947, #9831, .T. ) ;
#41268=AXIS2_PLACEMENT_3D ( 'NONE', #5677, #39137, #59151 ) ;
#41294=( NAMED_UNIT ( * ) PLANE_ANGLE_UNIT ( ) SI_UNIT ( $, .RADIAN. ) );
#41324=ADVANCED_FACE ( 'NONE', ( #22359 ), #2209, .F. ) ;
#41329=CIRCLE ( 'NONE', #63733, 0.2500000000000002220 ) ;
#41335=CARTESIAN_POINT ( 'NONE',  ( 21.25000000000001066, 24.99999999999998579, 3.750000000000000000 ) ) ;
#41357=ORIENTED_EDGE ( 'NONE', *, *, #59030, .T. ) ;
#41363=ORIENTED_EDGE ( 'NONE', *, *, #69346, .F. ) ;
#41419=CARTESIAN_POINT ( 'NONE',  ( 48.74999999999999289, 24.74999999999998579, -3.750000000000000000 ) ) ;
#41434=ORIENTED_EDGE ( 'NONE', *, *, #68629, .F. ) ;
#41457=ORIENTED_EDGE ( 'NONE', *, *, #63605, .T. ) ;
#41465=ORIENTED_EDGE ( 'NONE', *, *, #46983, .F. ) ;
#41471=ORIENTED_EDGE ( 'NONE', *, *, #57421, .F. ) ;
#41493=VECTOR ( 'NONE', #17147, 1000.000000000000000 ) ;
#41502=EDGE_CURVE ( 'NONE', #61490, #12327, #50345, .T. ) ;
#41558=ORIENTED_EDGE ( 'NONE', *, *, #10336, .T. ) ;
#41564=ORIENTED_EDGE ( 'NONE', *, *, #3460, .F. ) ;
#41566=AXIS2_PLACEMENT_3D ( 'NONE', #22605, #65505, #33494 ) ;
#41568=DIRECTION ( 'NONE',  ( 0.000000000000000000, 1.000000000000000000, 0.000000000000000000 ) ) ;
#41592=DIRECTION ( 'NONE',  ( 1.445602896647337931E-16, -1.000000000000000000, 0.000000000000000000 ) ) ;
#41597=ORIENTED_EDGE ( 'NONE', *, *, #39753, .T. ) ;
#41623=ORIENTED_EDGE ( 'NONE', *, *, #3213, .T. ) ;
#41626=PLANE ( 'NONE',  #64444 ) ;
#41634=CARTESIAN_POINT ( 'NONE',  ( 39.74999999999999289, 18.74999999999997868, -4.000000000000000000 ) ) ;
#41637=ORIENTED_EDGE ( 'NONE', *, *, #11050, .F. ) ;
#41639=( LENGTH_UNIT ( ) NAMED_UNIT ( * ) SI_UNIT ( .MILLI., .METRE. ) );
#41649=EDGE_CURVE ( 'NONE', #66803, #61112, #20174, .T. ) ;
#41652=FACE_OUTER_BOUND ( 'NONE', #39375, .T. ) ;
#41676=PRODUCT_DEFINITION_FORMATION_WITH_SPECIFIED_SOURCE ( 'ANY', '', #4050, .NOT_KNOWN. ) ;
#41682=FILL_AREA_STYLE_COLOUR ( '', #43939 ) ;
#41696=CARTESIAN_POINT ( 'NONE',  ( 25.75000000000001066, 0.000000000000000000, 4.000000000000000000 ) ) ;
#41718=( NAMED_UNIT ( * ) SI_UNIT ( $, .STERADIAN. ) SOLID_ANGLE_UNIT ( ) );
#41730=ORIENTED_EDGE ( 'NONE', *, *, #61435, .T. ) ;
#41736=DIRECTION ( 'NONE',  ( -1.000000000000000000, 0.000000000000000000, 0.000000000000000000 ) ) ;
#41760=AXIS2_PLACEMENT_3D ( 'NONE', #62422, #19145, #8621 ) ;
#41765=DIRECTION ( 'NONE',  ( -1.000000000000000000, 0.000000000000000000, 0.000000000000000000 ) ) ;
#41769=DIRECTION ( 'NONE',  ( -1.000000000000000000, 0.000000000000000000, 0.000000000000000000 ) ) ;
#41782=DIRECTION ( 'NONE',  ( -0.000000000000000000, 0.000000000000000000, -1.000000000000000000 ) ) ;
#41791=DIRECTION ( 'NONE',  ( -0.000000000000000000, 0.000000000000000000, -1.000000000000000000 ) ) ;
#41794=ORIENTED_EDGE ( 'NONE', *, *, #43256, .F. ) ;
#41812=ORIENTED_EDGE ( 'NONE', *, *, #11779, .T. ) ;
#41817=AXIS2_PLACEMENT_3D ( 'NONE', #31563, #21713, #36892 ) ;
#41820=EDGE_LOOP ( 'NONE', ( #63591, #27720, #31547, #66215 ) ) ;
#41827=DIRECTION ( 'NONE',  ( -0.000000000000000000, -0.000000000000000000, -1.000000000000000000 ) ) ;
#41835=DIRECTION ( 'NONE',  ( -0.000000000000000000, 0.000000000000000000, -1.000000000000000000 ) ) ;
#41879=VERTEX_POINT ( 'NONE', #10314 ) ;
#41886=VERTEX_POINT ( 'NONE', #63425 ) ;
#41889=AXIS2_PLACEMENT_3D ( 'NONE', #4797, #43188, #825 ) ;
#41912=CARTESIAN_POINT ( 'NONE',  ( 21.75000000000001066, 21.74999999999998224, -4.000000000000000000 ) ) ;
#41927=PLANE ( 'NONE',  #63176 ) ;
#41945=LINE ( 'NONE', #26050, #17935 ) ;
#41949=AXIS2_PLACEMENT_3D ( 'NONE', #1185, #27951, #22719 ) ;
#41956=LINE ( 'NONE', #36684, #24253 ) ;
#41962=ORIENTED_EDGE ( 'NONE', *, *, #61941, .F. ) ;
#41968=DIRECTION ( 'NONE',  ( 0.000000000000000000, 0.000000000000000000, 1.000000000000000000 ) ) ;
#41971=AXIS2_PLACEMENT_3D ( 'NONE', #2428, #12002, #55250 ) ;
#41978=ORIENTED_EDGE ( 'NONE', *, *, #36758, .F. ) ;
#42002=AXIS2_PLACEMENT_3D ( 'NONE', #21955, #47334, #11381 ) ;
#42015=DIRECTION ( 'NONE',  ( -1.000000000000000000, 0.000000000000000000, 0.000000000000000000 ) ) ;
#42051=DIRECTION ( 'NONE',  ( 0.000000000000000000, 1.000000000000000000, 0.000000000000000000 ) ) ;
#42053=ORIENTED_EDGE ( 'NONE', *, *, #26635, .T. ) ;
#42060=DIRECTION ( 'NONE',  ( 0.000000000000000000, 0.000000000000000000, -1.000000000000000000 ) ) ;
#42067=DIRECTION ( 'NONE',  ( 1.000000000000000000, -0.000000000000000000, -0.000000000000000000 ) ) ;
#42069=VERTEX_POINT ( 'NONE', #9448 ) ;
#42098=EDGE_CURVE ( 'NONE', #44763, #57684, #42517, .T. ) ;
#42102=AXIS2_PLACEMENT_3D ( 'NONE', #21120, #15199, #52811 ) ;
#42109=AXIS2_PLACEMENT_3D ( 'NONE', #59283, #17132, #20990 ) ;
#42123=AXIS2_PLACEMENT_3D ( 'NONE', #66980, #44175, #43374 ) ;
#42125=ORIENTED_EDGE ( 'NONE', *, *, #18466, .T. ) ;
#42127=EDGE_CURVE ( 'NONE', #51712, #22240, #50400, .T. ) ;
#42144=CIRCLE ( 'NONE', #7299, 0.2499999999999997780 ) ;
#42148=DIRECTION ( 'NONE',  ( 0.000000000000000000, 1.000000000000000000, 0.000000000000000000 ) ) ;
#42157=EDGE_CURVE ( 'NONE', #8197, #40202, #4122, .T. ) ;
#42189=CARTESIAN_POINT ( 'NONE',  ( 30.25000000000000711, 18.74999999999997868, -4.000000000000000000 ) ) ;
#42191=FACE_OUTER_BOUND ( 'NONE', #37874, .T. ) ;
#42195=CYLINDRICAL_SURFACE ( 'NONE', #39546, 0.2500000000000002220 ) ;
#42214=ORIENTED_EDGE ( 'NONE', *, *, #21079, .T. ) ;
#42216=LINE ( 'NONE', #36585, #45949 ) ;
#42233=EDGE_CURVE ( 'NONE', #56118, #25430, #5430, .T. ) ;
#42241=ORIENTED_EDGE ( 'NONE', *, *, #10731, .T. ) ;
#42242=ORIENTED_EDGE ( 'NONE', *, *, #15659, .T. ) ;
#42271=DIRECTION ( 'NONE',  ( 1.000000000000000000, 1.224646799147353207E-16, 0.000000000000000000 ) ) ;
#42302=DIRECTION ( 'NONE',  ( -0.000000000000000000, -0.000000000000000000, -1.000000000000000000 ) ) ;
#42313=CARTESIAN_POINT ( 'NONE',  ( 44.25000000000000000, 21.99999999999998579, 4.000000000000000000 ) ) ;
#42320=EDGE_CURVE ( 'NONE', #28127, #50231, #11070, .T. ) ;
#42332=ORIENTED_EDGE ( 'NONE', *, *, #20283, .T. ) ;
#42334=ORIENTED_EDGE ( 'NONE', *, *, #20972, .F. ) ;
#42362=CARTESIAN_POINT ( 'NONE',  ( 17.25000000000000711, 25.24999999999998224, 4.000000000000000000 ) ) ;
#42363=CARTESIAN_POINT ( 'NONE',  ( 43.75000000000000000, 18.74999999999998224, -3.750000000000000000 ) ) ;
#42365=DIRECTION ( 'NONE',  ( 0.000000000000000000, 1.000000000000000000, 0.000000000000000000 ) ) ;
#42370=ORIENTED_EDGE ( 'NONE', *, *, #52123, .F. ) ;
#42406=EDGE_CURVE ( 'NONE', #29227, #56343, #17861, .T. ) ;
#42421=ORIENTED_EDGE ( 'NONE', *, *, #38955, .F. ) ;
#42424=DIRECTION ( 'NONE',  ( 0.7071067811865451302, 0.000000000000000000, 0.7071067811865500152 ) ) ;
#42427=LINE ( 'NONE', #63818, #68792 ) ;
#42448=ORIENTED_EDGE ( 'NONE', *, *, #12721, .F. ) ;
#42454=CARTESIAN_POINT ( 'NONE',  ( 57.49999999999999289, 28.24999999999998934, -3.750000000000000000 ) ) ;
#42459=ORIENTED_EDGE ( 'NONE', *, *, #33865, .F. ) ;
#42466=LINE ( 'NONE', #37894, #64639 ) ;
#42467=CARTESIAN_POINT ( 'NONE',  ( 17.25000000000000711, 25.24999999999998224, -4.000000000000000000 ) ) ;
#42493=DIRECTION ( 'NONE',  ( 0.000000000000000000, 0.000000000000000000, -1.000000000000000000 ) ) ;
#42502=ORIENTED_EDGE ( 'NONE', *, *, #14156, .T. ) ;
#42515=LINE ( 'NONE', #55001, #8085 ) ;
#42517=LINE ( 'NONE', #29230, #60473 ) ;
#42519=AXIS2_PLACEMENT_3D ( 'NONE', #42362, #5008, #52876 ) ;
#42521=DIRECTION ( 'NONE',  ( 0.000000000000000000, -1.000000000000000000, 0.000000000000000000 ) ) ;
#42527=EDGE_LOOP ( 'NONE', ( #16296, #53726, #9550, #38613 ) ) ;
#42542=CARTESIAN_POINT ( 'NONE',  ( 1.000000000000000000, 36.74999999999999289, -3.000000000000000000 ) ) ;
#42593=DIRECTION ( 'NONE',  ( 1.445602896647337931E-16, -1.000000000000000000, 0.000000000000000000 ) ) ;
#42610=AXIS2_PLACEMENT_3D ( 'NONE', #1589, #12888, #7605 ) ;
#42615=DIRECTION ( 'NONE',  ( -2.168404344971009361E-16, 1.000000000000000000, 0.000000000000000000 ) ) ;
#42619=CARTESIAN_POINT ( 'NONE',  ( 57.74999999999999289, 28.24999999999998934, 3.750000000000000000 ) ) ;
#42622=ORIENTED_EDGE ( 'NONE', *, *, #67026, .T. ) ;
#42634=AXIS2_PLACEMENT_3D ( 'NONE', #43428, #64815, #59522 ) ;
#42638=ORIENTED_EDGE ( 'NONE', *, *, #34062, .F. ) ;
#42645=DIRECTION ( 'NONE',  ( 1.000000000000000000, -0.000000000000000000, 0.000000000000000000 ) ) ;
#42659=VERTEX_POINT ( 'NONE', #10406 ) ;
#42661=CARTESIAN_POINT ( 'NONE',  ( 61.74999999999998579, 31.24999999999999289, 3.750000000000000000 ) ) ;
#42665=DIRECTION ( 'NONE',  ( 1.445602896647337931E-16, -1.000000000000000000, -0.000000000000000000 ) ) ;
#42666=VECTOR ( 'NONE', #27532, 1000.000000000000114 ) ;
#42688=CARTESIAN_POINT ( 'NONE',  ( 21.50000000000001066, 24.74999999999998224, -3.750000000000000000 ) ) ;
#42703=VECTOR ( 'NONE', #18100, 1000.000000000000000 ) ;
#42719=DIRECTION ( 'NONE',  ( 0.000000000000000000, 0.000000000000000000, -1.000000000000000000 ) ) ;
#42749=CARTESIAN_POINT ( 'NONE',  ( 66.24999999999998579, 34.24999999999999289, -3.750000000000000000 ) ) ;
#42753=SURFACE_STYLE_USAGE ( .BOTH. , #32470 ) ;
#42755=CARTESIAN_POINT ( 'NONE',  ( 52.75000000000000000, 24.99999999999998579, -3.750000000000000000 ) ) ;
#42766=ORIENTED_EDGE ( 'NONE', *, *, #5956, .F. ) ;
#42778=ORIENTED_EDGE ( 'NONE', *, *, #63905, .T. ) ;
#42782=ORIENTED_EDGE ( 'NONE', *, *, #23092, .F. ) ;
#42792=ORIENTED_EDGE ( 'NONE', *, *, #30720, .T. ) ;
#42805=ORIENTED_EDGE ( 'NONE', *, *, #18869, .T. ) ;
#42812=CARTESIAN_POINT ( 'NONE',  ( 48.75000000000000000, 22.24999999999998579, -3.750000000000000000 ) ) ;
#42813=CYLINDRICAL_SURFACE ( 'NONE', #43310, 0.2500000000000002220 ) ;
#42816=MECHANICAL_DESIGN_GEOMETRIC_PRESENTATION_REPRESENTATION('',(#48425),#16922);
#42817=ORIENTED_EDGE ( 'NONE', *, *, #33928, .T. ) ;
#42819=VECTOR ( 'NONE', #25399, 1000.000000000000000 ) ;
#42828=DIRECTION ( 'NONE',  ( 1.000000000000000000, 0.000000000000000000, 0.000000000000000000 ) ) ;
#42840=AXIS2_PLACEMENT_3D ( 'NONE', #59977, #7217, #49786 ) ;
#42877=CARTESIAN_POINT ( 'NONE',  ( 12.50000000000000533, 28.24999999999998224, -3.750000000000000000 ) ) ;
#42887=CYLINDRICAL_SURFACE ( 'NONE', #23112, 0.2500000000000002220 ) ;
#42888=ORIENTED_EDGE ( 'NONE', *, *, #20348, .F. ) ;
#42900=FACE_OUTER_BOUND ( 'NONE', #30689, .T. ) ;
#42920=LINE ( 'NONE', #16854, #20610 ) ;
#42931=ADVANCED_FACE ( 'NONE', ( #67668 ), #9283, .F. ) ;
#42946=ORIENTED_EDGE ( 'NONE', *, *, #42406, .F. ) ;
#42963=COLOUR_RGB ( '', 0.66274510, 0.83137255, 0.94901961) ;
#42971=CARTESIAN_POINT ( 'NONE',  ( 3.749999999999999556, 33.74999999999998579, 4.000000000000000000 ) ) ;
#42973=VERTEX_POINT ( 'NONE', #19105 ) ;
#42996=ORIENTED_EDGE ( 'NONE', *, *, #57178, .T. ) ;
#42999=LINE ( 'NONE', #38416, #65061 ) ;
#43015=CARTESIAN_POINT ( 'NONE',  ( 39.74999999999999289, 18.74999999999997868, -4.000000000000000000 ) ) ;
#43047=ORIENTED_EDGE ( 'NONE', *, *, #7557, .F. ) ;
#43072=CARTESIAN_POINT ( 'NONE',  ( 57.49999999999998579, 30.74999999999999289, 4.000000000000000000 ) ) ;
#43076=CIRCLE ( 'NONE', #52025, 0.2500000000000002220 ) ;
#43092=CARTESIAN_POINT ( 'NONE',  ( 3.749999999999999556, 33.74999999999998579, 3.750000000000000000 ) ) ;
#43096=CARTESIAN_POINT ( 'NONE',  ( 16.75000000000000711, 27.74999999999998224, -3.750000000000000000 ) ) ;
#43135=ORIENTED_EDGE ( 'NONE', *, *, #23282, .T. ) ;
#43136=ADVANCED_FACE ( 'NONE', ( #21 ), #55645, .T. ) ;
#43154=CIRCLE ( 'NONE', #53355, 0.2500000000000002220 ) ;
#43156=CARTESIAN_POINT ( 'NONE',  ( 39.49999999999999289, 16.24999999999997513, -3.750000000000000000 ) ) ;
#43172=AXIS2_PLACEMENT_3D ( 'NONE', #14856, #64054, #10608 ) ;
#43173=CARTESIAN_POINT ( 'NONE',  ( 39.49999999999999289, 18.74999999999997868, -3.750000000000000000 ) ) ;
#43176=LINE ( 'NONE', #65609, #55941 ) ;
#43181=CARTESIAN_POINT ( 'NONE',  ( 69.99999999999998579, 36.75000000000000000, 4.000000000000000000 ) ) ;
#43188=DIRECTION ( 'NONE',  ( 0.000000000000000000, 1.000000000000000000, 0.000000000000000000 ) ) ;
#43203=AXIS2_PLACEMENT_3D ( 'NONE', #25934, #69222, #31204 ) ;
#43222=CARTESIAN_POINT ( 'NONE',  ( 69.99999999999998579, 1.000000000000008438, 4.000000000000000000 ) ) ;
#43237=ORIENTED_EDGE ( 'NONE', *, *, #39352, .T. ) ;
#43240=FACE_OUTER_BOUND ( 'NONE', #10448, .T. ) ;
#43252=AXIS2_PLACEMENT_3D ( 'NONE', #51764, #41568, #47213 ) ;
#43256=EDGE_CURVE ( 'NONE', #65411, #44314, #14833, .T. ) ;
#43297=PLANE ( 'NONE',  #53127 ) ;
#43301=FILL_AREA_STYLE_COLOUR ( '', #47982 ) ;
#43310=AXIS2_PLACEMENT_3D ( 'NONE', #46796, #8756, #16057 ) ;
#43319=AXIS2_PLACEMENT_3D ( 'NONE', #18577, #14324, #8376 ) ;
#43327=ORIENTED_EDGE ( 'NONE', *, *, #15295, .T. ) ;
#43350=LINE ( 'NONE', #42313, #35945 ) ;
#43362=AXIS2_PLACEMENT_3D ( 'NONE', #53988, #66277, #27237 ) ;
#43366=EDGE_LOOP ( 'NONE', ( #5017, #65874, #43605, #22730 ) ) ;
#43368=AXIS2_PLACEMENT_3D ( 'NONE', #64962, #16485, #21358 ) ;
#43369=CARTESIAN_POINT ( 'NONE',  ( 30.25000000000000711, 18.74999999999997868, 3.750000000000000000 ) ) ;
#43374=DIRECTION ( 'NONE',  ( 0.000000000000000000, 0.000000000000000000, 1.000000000000000000 ) ) ;
#43381=EDGE_LOOP ( 'NONE', ( #44854, #55854, #10101, #63483 ) ) ;
#43388=ORIENTED_EDGE ( 'NONE', *, *, #57754, .T. ) ;
#43396=DIRECTION ( 'NONE',  ( -1.156482317317870344E-15, -1.000000000000000000, -0.000000000000000000 ) ) ;
#43401=ORIENTED_EDGE ( 'NONE', *, *, #23196, .F. ) ;
#43405=DIRECTION ( 'NONE',  ( -0.000000000000000000, 0.000000000000000000, -1.000000000000000000 ) ) ;
#43412=ADVANCED_FACE ( 'NONE', ( #9901 ), #58414, .T. ) ;
#43428=CARTESIAN_POINT ( 'NONE',  ( 39.74999999999999289, 18.74999999999997868, -3.750000000000000000 ) ) ;
#43437=LINE ( 'NONE', #17697, #53680 ) ;
#43444=EDGE_CURVE ( 'NONE', #60007, #7926, #55196, .T. ) ;
#43455=DIRECTION ( 'NONE',  ( -0.000000000000000000, 0.000000000000000000, -1.000000000000000000 ) ) ;
#43457=EDGE_LOOP ( 'NONE', ( #10867, #69030, #34282 ) ) ;
#43463=CARTESIAN_POINT ( 'NONE',  ( 69.99999999999998579, 1.000000000000008438, 3.000000000000000000 ) ) ;
#43464=CARTESIAN_POINT ( 'NONE',  ( 3.749999999999999556, 34.24999999999998579, -3.750000000000000000 ) ) ;
#43474=CARTESIAN_POINT ( 'NONE',  ( 30.50000000000000711, 18.74999999999997868, -3.750000000000000000 ) ) ;
#43475=LINE ( 'NONE', #48381, #39000 ) ;
#43485=DIRECTION ( 'NONE',  ( 1.000000000000000000, 0.000000000000000000, 0.000000000000000000 ) ) ;
#43500=AXIS2_PLACEMENT_3D ( 'NONE', #39645, #61062, #29031 ) ;
#43518=DIRECTION ( 'NONE',  ( 0.000000000000000000, 0.000000000000000000, -1.000000000000000000 ) ) ;
#43528=DIRECTION ( 'NONE',  ( 1.000000000000000000, 0.000000000000000000, 0.000000000000000000 ) ) ;
#43537=CARTESIAN_POINT ( 'NONE',  ( 10.99999999999999645, 11.99999999999999289, -4.000000000000000000 ) ) ;
#43538=EDGE_LOOP ( 'NONE', ( #41597, #29641, #8652, #22127 ) ) ;
#43588=AXIS2_PLACEMENT_3D ( 'NONE', #61468, #6293, #49225 ) ;
#43605=ORIENTED_EDGE ( 'NONE', *, *, #48109, .T. ) ;
#43621=EDGE_LOOP ( 'NONE', ( #6749, #53631, #13633, #69618 ) ) ;
#43629=DIRECTION ( 'NONE',  ( -1.000000000000000000, 0.000000000000000000, 0.000000000000000000 ) ) ;
#43631=AXIS2_PLACEMENT_3D ( 'NONE', #44612, #17836, #39314 ) ;
#43633=ORIENTED_EDGE ( 'NONE', *, *, #52474, .F. ) ;
#43643=EDGE_LOOP ( 'NONE', ( #65986, #40056, #67298 ) ) ;
#43649=EDGE_CURVE ( 'NONE', #28025, #27009, #42216, .T. ) ;
#43675=DIRECTION ( 'NONE',  ( 0.000000000000000000, 0.000000000000000000, -1.000000000000000000 ) ) ;
#43679=VECTOR ( 'NONE', #6538, 1000.000000000000000 ) ;
#43681=ORIENTED_EDGE ( 'NONE', *, *, #6203, .T. ) ;
#43697=DIRECTION ( 'NONE',  ( -0.000000000000000000, 1.000000000000000000, -0.000000000000000000 ) ) ;
#43705=FACE_OUTER_BOUND ( 'NONE', #26346, .T. ) ;
#43745=ADVANCED_FACE ( 'NONE', ( #32614 ), #61671, .T. ) ;
#43771=EDGE_CURVE ( 'NONE', #25571, #47549, #40315, .T. ) ;
#43779=VERTEX_POINT ( 'NONE', #24403 ) ;
#43792=EDGE_CURVE ( 'NONE', #19502, #14179, #49305, .T. ) ;
#43845=CARTESIAN_POINT ( 'NONE',  ( 0.000000000000000000, 30.74999999999999289, 4.000000000000000000 ) ) ;
#43853=DIRECTION ( 'NONE',  ( 0.000000000000000000, 0.000000000000000000, -1.000000000000000000 ) ) ;
#43862=SPHERICAL_SURFACE ( 'NONE', #41889, 0.2500000000000000000 ) ;
#43894=AXIS2_PLACEMENT_3D ( 'NONE', #30448, #19909, #41765 ) ;
#43906=CARTESIAN_POINT ( 'NONE',  ( 68.99999999999998579, 1.000000000000008438, 3.000000000000000000 ) ) ;
#43920=EDGE_CURVE ( 'NONE', #24250, #41177, #24073, .T. ) ;
#43936=CARTESIAN_POINT ( 'NONE',  ( 25.75000000000001066, 19.24999999999997868, 4.000000000000000000 ) ) ;
#43939=COLOUR_RGB ( '', 0.40784314, 0.44705882, 0.49803922) ;
#43954=ORIENTED_EDGE ( 'NONE', *, *, #17795, .F. ) ;
#43970=VERTEX_POINT ( 'NONE', #63089 ) ;
#44007=DIRECTION ( 'NONE',  ( 0.000000000000000000, 0.000000000000000000, -1.000000000000000000 ) ) ;
#44024=CYLINDRICAL_SURFACE ( 'NONE', #49977, 0.2500000000000002220 ) ;
#44073=VECTOR ( 'NONE', #36668, 1000.000000000000000 ) ;
#44086=AXIS2_PLACEMENT_3D ( 'NONE', #19346, #14093, #52091 ) ;
#44092=EDGE_LOOP ( 'NONE', ( #5484, #12575, #18528, #14775 ) ) ;
#44123=DIRECTION ( 'NONE',  ( 0.000000000000000000, 0.000000000000000000, -1.000000000000000000 ) ) ;
#44133=EDGE_CURVE ( 'NONE', #60291, #22530, #15977, .T. ) ;
#44149=EDGE_CURVE ( 'NONE', #31454, #42659, #22422, .T. ) ;
#44156=CARTESIAN_POINT ( 'NONE',  ( 3.499999999999999112, 33.99999999999998579, 3.750000000000000000 ) ) ;
#44160=CARTESIAN_POINT ( 'NONE',  ( 12.50000000000000355, 30.74999999999998579, 4.000000000000000000 ) ) ;
#44168=CARTESIAN_POINT ( 'NONE',  ( 53.25000000000005684, 1.231653667943533289E-13, 3.750000000000000000 ) ) ;
#44169=ORIENTED_EDGE ( 'NONE', *, *, #14469, .T. ) ;
#44175=DIRECTION ( 'NONE',  ( -1.000000000000000000, 0.000000000000000000, 0.000000000000000000 ) ) ;
#44195=FACE_OUTER_BOUND ( 'NONE', #46240, .T. ) ;
#44210=CARTESIAN_POINT ( 'NONE',  ( 44.25000000000000000, 21.99999999999998579, 3.750000000000000000 ) ) ;
#44211=CARTESIAN_POINT ( 'NONE',  ( 61.74999999999998579, 31.24999999999999289, 3.750000000000000000 ) ) ;
#44213=CARTESIAN_POINT ( 'NONE',  ( 39.74999999999999289, 18.74999999999997868, 3.750000000000000000 ) ) ;
#44224=DIRECTION ( 'NONE',  ( 1.000000000000000000, 0.000000000000000000, 0.000000000000000000 ) ) ;
#44234=DIRECTION ( 'NONE',  ( 0.000000000000000000, 1.000000000000000000, 0.000000000000000000 ) ) ;
#44245=FACE_OUTER_BOUND ( 'NONE', #47090, .T. ) ;
#44247=ORIENTED_EDGE ( 'NONE', *, *, #5192, .F. ) ;
#44253=VECTOR ( 'NONE', #589, 1000.000000000000000 ) ;
#44276=FACE_OUTER_BOUND ( 'NONE', #61522, .T. ) ;
#44314=VERTEX_POINT ( 'NONE', #41243 ) ;
#44319=DIRECTION ( 'NONE',  ( 0.000000000000000000, 1.000000000000000000, 0.000000000000000000 ) ) ;
#44326=VECTOR ( 'NONE', #30084, 1000.000000000000000 ) ;
#44337=ORIENTED_EDGE ( 'NONE', *, *, #38652, .T. ) ;
#44346=ORIENTED_EDGE ( 'NONE', *, *, #65686, .T. ) ;
#44347=AXIS2_PLACEMENT_3D ( 'NONE', #21125, #20798, #52482 ) ;
#44356=ORIENTED_EDGE ( 'NONE', *, *, #25023, .F. ) ;
#44357=CARTESIAN_POINT ( 'NONE',  ( 25.75000000000001066, 0.000000000000000000, 3.750000000000000000 ) ) ;
#44415=ADVANCED_FACE ( 'NONE', ( #51773 ), #24327, .F. ) ;
#44425=CARTESIAN_POINT ( 'NONE',  ( 7.750000000000000000, 33.74999999999998579, -3.750000000000000000 ) ) ;
#44441=ORIENTED_EDGE ( 'NONE', *, *, #12101, .T. ) ;
#44476=AXIS2_PLACEMENT_3D ( 'NONE', #65816, #34145, #61225 ) ;
#44515=VECTOR ( 'NONE', #18978, 1000.000000000000000 ) ;
#44519=PLANE ( 'NONE',  #13712 ) ;
#44528=VECTOR ( 'NONE', #45508, 1000.000000000000000 ) ;
#44541=ADVANCED_FACE ( 'NONE', ( #5284 ), #58776, .F. ) ;
#44546=ADVANCED_FACE ( 'NONE', ( #31687 ), #37721, .T. ) ;
#44561=CARTESIAN_POINT ( 'NONE',  ( 17.00000000000000711, 24.99999999999998224, 3.750000000000000000 ) ) ;
#44575=ORIENTED_EDGE ( 'NONE', *, *, #43792, .F. ) ;
#44589=AXIS2_PLACEMENT_3D ( 'NONE', #4043, #68437, #41736 ) ;
#44612=CARTESIAN_POINT ( 'NONE',  ( 7.750000000000001776, 31.24999999999998579, 3.750000000000000000 ) ) ;
#44613=FACE_OUTER_BOUND ( 'NONE', #63467, .T. ) ;
#44623=ADVANCED_FACE ( 'NONE', ( #37017 ), #6691, .T. ) ;
#44635=CARTESIAN_POINT ( 'NONE',  ( 59.00000000000000000, 11.99999999999999822, -4.000000000000000000 ) ) ;
#44661=DIRECTION ( 'NONE',  ( 0.000000000000000000, -0.000000000000000000, 1.000000000000000000 ) ) ;
#44672=ADVANCED_FACE ( 'NONE', ( #47592 ), #66248, .T. ) ;
#44675=EDGE_CURVE ( 'NONE', #59308, #52155, #43350, .T. ) ;
#44690=EDGE_LOOP ( 'NONE', ( #9695, #12601, #40526, #13934 ) ) ;
#44692=LINE ( 'NONE', #28795, #6976 ) ;
#44698=FILL_AREA_STYLE_COLOUR ( '', #36072 ) ;
#44704=VERTEX_POINT ( 'NONE', #7390 ) ;
#44706=ADVANCED_FACE ( 'NONE', ( #33420 ), #49970, .T. ) ;
#44710=FACE_OUTER_BOUND ( 'NONE', #40921, .T. ) ;
#44720=DIRECTION ( 'NONE',  ( 0.000000000000000000, 0.000000000000000000, 1.000000000000000000 ) ) ;
#44721=ORIENTED_EDGE ( 'NONE', *, *, #32228, .F. ) ;
#44736=DIRECTION ( 'NONE',  ( -0.000000000000000000, -0.000000000000000000, 1.000000000000000000 ) ) ;
#44740=ORIENTED_EDGE ( 'NONE', *, *, #12101, .F. ) ;
#44746=DIRECTION ( 'NONE',  ( 1.000000000000000000, 0.000000000000000000, 0.000000000000000000 ) ) ;
#44763=VERTEX_POINT ( 'NONE', #17937 ) ;
#44780=ORIENTED_EDGE ( 'NONE', *, *, #14885, .T. ) ;
#44801=VECTOR ( 'NONE', #59097, 1000.000000000000000 ) ;
#44805=ORIENTED_EDGE ( 'NONE', *, *, #15823, .T. ) ;
#44809=LINE ( 'NONE', #22982, #56113 ) ;
#44821=AXIS2_PLACEMENT_3D ( 'NONE', #64626, #60028, #5858 ) ;
#44822=ORIENTED_EDGE ( 'NONE', *, *, #36079, .F. ) ;
#44824=DIRECTION ( 'NONE',  ( -1.000000000000000000, 0.000000000000000000, 0.000000000000000000 ) ) ;
#44840=EDGE_LOOP ( 'NONE', ( #18158, #10278, #65272, #68176 ) ) ;
#44854=ORIENTED_EDGE ( 'NONE', *, *, #65348, .F. ) ;
#44856=CARTESIAN_POINT ( 'NONE',  ( 21.75000000000001066, 21.99999999999998224, 4.000000000000000000 ) ) ;
#44868=DIRECTION ( 'NONE',  ( 1.000000000000000000, 0.000000000000000000, 0.000000000000000000 ) ) ;
#44869=LINE ( 'NONE', #65588, #42703 ) ;
#44885=CARTESIAN_POINT ( 'NONE',  ( 52.75000000000000000, 24.74999999999998224, -4.000000000000000000 ) ) ;
#44894=DIRECTION ( 'NONE',  ( 1.000000000000000000, -0.000000000000000000, 0.000000000000000000 ) ) ;
#44899=ADVANCED_FACE ( 'NONE', ( #24574 ), #56193, .T. ) ;
#44908=CARTESIAN_POINT ( 'NONE',  ( 16.75000000000000711, 0.000000000000000000, 3.750000000000000000 ) ) ;
#44911=DIRECTION ( 'NONE',  ( 0.000000000000000000, 0.000000000000000000, -1.000000000000000000 ) ) ;
#44915=CIRCLE ( 'NONE', #957, 0.5000000000000004441 ) ;
#44920=VECTOR ( 'NONE', #34906, 1000.000000000000000 ) ;
#44926=CARTESIAN_POINT ( 'NONE',  ( 66.49999999999998579, 37.00000000000000000, 4.000000000000000000 ) ) ;
#44937=VECTOR ( 'NONE', #50295, 1000.000000000000000 ) ;
#44964=CARTESIAN_POINT ( 'NONE',  ( 21.75000000000001066, 22.24999999999998224, 3.750000000000000000 ) ) ;
#44970=CIRCLE ( 'NONE', #21379, 3.100000000000005418 ) ;
#44989=EDGE_LOOP ( 'NONE', ( #15412, #20092, #46831, #57796 ) ) ;
#45028=CARTESIAN_POINT ( 'NONE',  ( 69.99999999999998579, 37.00000000000000000, 4.000000000000000000 ) ) ;
#45030=DIRECTION ( 'NONE',  ( -0.000000000000000000, -0.000000000000000000, 1.000000000000000000 ) ) ;
#45041=AXIS2_PLACEMENT_3D ( 'NONE', #17529, #22785, #11872 ) ;
#45059=DIRECTION ( 'NONE',  ( 1.000000000000000000, -0.000000000000000000, 0.000000000000000000 ) ) ;
#45070=CIRCLE ( 'NONE', #57387, 0.2500000000000002220 ) ;
#45071=DIRECTION ( 'NONE',  ( 0.000000000000000000, -0.000000000000000000, 1.000000000000000000 ) ) ;
#45078=EDGE_CURVE ( 'NONE', #9427, #4257, #40926, .T. ) ;
#45147=CARTESIAN_POINT ( 'NONE',  ( 57.24999999999999289, 27.99999999999998934, -3.750000000000000000 ) ) ;
#45166=EDGE_CURVE ( 'NONE', #26540, #38142, #20106, .T. ) ;
#45173=CARTESIAN_POINT ( 'NONE',  ( 69.74999999999998579, 37.00000000000000000, 4.000000000000000000 ) ) ;
#45179=AXIS2_PLACEMENT_3D ( 'NONE', #6828, #68885, #5500 ) ;
#45182=EDGE_LOOP ( 'NONE', ( #41457, #2603, #25111, #55946 ) ) ;
#45197=COLOUR_RGB ( '', 0.08235294, 0.09019608, 0.10196078) ;
#45200=VERTEX_POINT ( 'NONE', #47257 ) ;
#45211=AXIS2_PLACEMENT_3D ( 'NONE', #58635, #21330, #15068 ) ;
#45221=CARTESIAN_POINT ( 'NONE',  ( 7.750000000000000000, 33.74999999999998579, 3.750000000000000000 ) ) ;
#45223=FACE_OUTER_BOUND ( 'NONE', #8832, .T. ) ;
#45242=CARTESIAN_POINT ( 'NONE',  ( 30.75000000000001066, 15.99999999999997691, 4.000000000000000000 ) ) ;
#45256=AXIS2_PLACEMENT_3D ( 'NONE', #57152, #55779, #45944 ) ;
#45266=( NAMED_UNIT ( * ) SI_UNIT ( $, .STERADIAN. ) SOLID_ANGLE_UNIT ( ) );
#45272=CARTESIAN_POINT ( 'NONE',  ( 12.50000000000000355, 30.74999999999998579, -3.750000000000000000 ) ) ;
#45296=DIRECTION ( 'NONE',  ( 0.000000000000000000, 0.000000000000000000, 1.000000000000000000 ) ) ;
#45326=CARTESIAN_POINT ( 'NONE',  ( 7.899999999999995914, 11.99999999999999289, 3.500000000000004885 ) ) ;
#45327=AXIS2_PLACEMENT_3D ( 'NONE', #1395, #18336, #40155 ) ;
#45360=DIRECTION ( 'NONE',  ( -0.000000000000000000, -0.000000000000000000, 1.000000000000000000 ) ) ;
#45365=ORIENTED_EDGE ( 'NONE', *, *, #17116, .F. ) ;
#45367=ORIENTED_EDGE ( 'NONE', *, *, #58931, .F. ) ;
#45371=DIRECTION ( 'NONE',  ( 0.000000000000000000, 0.000000000000000000, 1.000000000000000000 ) ) ;
#45377=FILL_AREA_STYLE ('',( #34081 ) ) ;
#45385=CARTESIAN_POINT ( 'NONE',  ( 16.75000000000000711, 27.74999999999998224, -3.750000000000000000 ) ) ;
#45415=EDGE_CURVE ( 'NONE', #67453, #43970, #32706, .T. ) ;
#45418=CARTESIAN_POINT ( 'NONE',  ( 66.74999999999998579, 36.75000000000000000, -4.000000000000000000 ) ) ;
#45420=ADVANCED_FACE ( 'NONE', ( #56282 ), #34144, .F. ) ;
#45438=ORIENTED_EDGE ( 'NONE', *, *, #173, .T. ) ;
#45463=ORIENTED_EDGE ( 'NONE', *, *, #69432, .T. ) ;
#45465=CIRCLE ( 'NONE', #34170, 0.2500000000000002220 ) ;
#45480=ORIENTED_EDGE ( 'NONE', *, *, #48504, .T. ) ;
#45487=EDGE_CURVE ( 'NONE', #32231, #34838, #2053, .T. ) ;
#45493=DIRECTION ( 'NONE',  ( 2.312964634635740689E-15, -1.000000000000000000, 0.000000000000000000 ) ) ;
#45494=AXIS2_PLACEMENT_3D ( 'NONE', #55931, #23241, #18315 ) ;
#45508=DIRECTION ( 'NONE',  ( 1.000000000000000000, -0.000000000000000000, -0.000000000000000000 ) ) ;
#45509=VECTOR ( 'NONE', #64844, 1000.000000000000000 ) ;
#45518=FACE_OUTER_BOUND ( 'NONE', #7455, .T. ) ;
#45528=EDGE_CURVE ( 'NONE', #57523, #67106, #48117, .T. ) ;
#45532=AXIS2_PLACEMENT_3D ( 'NONE', #57563, #20264, #41769 ) ;
#45552=EDGE_CURVE ( 'NONE', #34838, #26540, #38254, .T. ) ;
#45559=FACE_OUTER_BOUND ( 'NONE', #53515, .T. ) ;
#45579=DIRECTION ( 'NONE',  ( 0.000000000000000000, -0.000000000000000000, -1.000000000000000000 ) ) ;
#45584=( NAMED_UNIT ( * ) PLANE_ANGLE_UNIT ( ) SI_UNIT ( $, .RADIAN. ) );
#45595=CARTESIAN_POINT ( 'NONE',  ( 39.49999999999999289, 18.99999999999997868, 3.750000000000000000 ) ) ;
#45603=DIRECTION ( 'NONE',  ( 1.000000000000000000, 0.000000000000000000, -0.000000000000000000 ) ) ;
#45632=EDGE_CURVE ( 'NONE', #47340, #34416, #6196, .T. ) ;
#45667=ADVANCED_FACE ( 'NONE', ( #46665 ), #35374, .F. ) ;
#45669=DIRECTION ( 'NONE',  ( -1.000000000000000000, 0.000000000000000000, 0.000000000000000000 ) ) ;
#45672=DIRECTION ( 'NONE',  ( -1.000000000000000000, 0.000000000000000000, 0.000000000000000000 ) ) ;
#45687=VECTOR ( 'NONE', #3744, 1000.000000000000000 ) ;
#45702=DIRECTION ( 'NONE',  ( -1.000000000000000000, 0.000000000000000000, 0.000000000000000000 ) ) ;
#45717=CYLINDRICAL_SURFACE ( 'NONE', #59872, 0.2500000000000002220 ) ;
#45724=ADVANCED_FACE ( 'NONE', ( #51203 ), #14601, .T. ) ;
#45753=CIRCLE ( 'NONE', #46930, 0.2500000000000002220 ) ;
#45786=FACE_OUTER_BOUND ( 'NONE', #7489, .T. ) ;
#45794=CYLINDRICAL_SURFACE ( 'NONE', #50903, 0.2500000000000002220 ) ;
#45815=CARTESIAN_POINT ( 'NONE',  ( 26.25000000000001066, 18.99999999999997868, -3.750000000000000000 ) ) ;
#45839=ORIENTED_EDGE ( 'NONE', *, *, #16761, .F. ) ;
#45845=DIRECTION ( 'NONE',  ( 0.000000000000000000, 0.000000000000000000, -1.000000000000000000 ) ) ;
#45849=FACE_BOUND ( 'NONE', #38251, .T. ) ;
#45853=EDGE_LOOP ( 'NONE', ( #38339, #60135, #19891 ) ) ;
#45916=DIRECTION ( 'NONE',  ( -0.000000000000000000, 1.000000000000000000, -0.000000000000000000 ) ) ;
#45930=DIRECTION ( 'NONE',  ( 0.000000000000000000, 0.000000000000000000, -1.000000000000000000 ) ) ;
#45934=AXIS2_PLACEMENT_3D ( 'NONE', #16798, #22390, #65988 ) ;
#45944=DIRECTION ( 'NONE',  ( 1.000000000000000000, 0.000000000000000000, 0.000000000000000000 ) ) ;
#45949=VECTOR ( 'NONE', #20344, 1000.000000000000000 ) ;
#45961=VECTOR ( 'NONE', #13029, 1000.000000000000000 ) ;
#45987=FACE_OUTER_BOUND ( 'NONE', #33628, .T. ) ;
#45988=DIRECTION ( 'NONE',  ( 1.000000000000000000, -0.000000000000000000, 0.000000000000000000 ) ) ;
#45994=DIRECTION ( 'NONE',  ( -0.000000000000000000, -0.000000000000000000, 1.000000000000000000 ) ) ;
#46002=ADVANCED_FACE ( 'NONE', ( #68339 ), #20462, .F. ) ;
#46006=DIRECTION ( 'NONE',  ( -1.000000000000000000, 0.000000000000000000, 0.000000000000000000 ) ) ;
#46029=ORIENTED_EDGE ( 'NONE', *, *, #44675, .T. ) ;
#46038=ORIENTED_EDGE ( 'NONE', *, *, #30799, .T. ) ;
#46048=CYLINDRICAL_SURFACE ( 'NONE', #50370, 0.2500000000000002220 ) ;
#46053=AXIS2_PLACEMENT_3D ( 'NONE', #63153, #69466, #37153 ) ;
#46063=CARTESIAN_POINT ( 'NONE',  ( 7.750000000000000000, 33.99999999999998579, 4.000000000000000000 ) ) ;
#46065=ORIENTED_EDGE ( 'NONE', *, *, #42233, .T. ) ;
#46088=DIRECTION ( 'NONE',  ( 0.000000000000000000, -1.000000000000000000, 0.000000000000000000 ) ) ;
#46089=( LENGTH_UNIT ( ) NAMED_UNIT ( * ) SI_UNIT ( .MILLI., .METRE. ) );
#46094=CARTESIAN_POINT ( 'NONE',  ( 39.24999999999999289, 15.74999999999997513, 4.000000000000000000 ) ) ;
#46108=CARTESIAN_POINT ( 'NONE',  ( 3.499999999999999112, 33.99999999999998579, 4.000000000000000000 ) ) ;
#46132=UNCERTAINTY_MEASURE_WITH_UNIT (LENGTH_MEASURE( 1.000000000000000082E-05 ), #54284, 'distance_accuracy_value', 'NONE');
#46143=ORIENTED_EDGE ( 'NONE', *, *, #37788, .F. ) ;
#46195=ADVANCED_FACE ( 'NONE', ( #32775 ), #38787, .F. ) ;
#46223=CARTESIAN_POINT ( 'NONE',  ( 0.000000000000000000, 0.000000000000000000, 3.000000000000000000 ) ) ;
#46240=EDGE_LOOP ( 'NONE', ( #22746, #42766, #42242, #47920 ) ) ;
#46242=CARTESIAN_POINT ( 'NONE',  ( 30.75000000000001066, 15.74999999999997513, 3.750000000000000000 ) ) ;
#46244=CARTESIAN_POINT ( 'NONE',  ( 21.25000000000001066, 24.74999999999998224, -4.000000000000000000 ) ) ;
#46271=AXIS2_PLACEMENT_3D ( 'NONE', #48499, #5511, #32601 ) ;
#46272=EDGE_CURVE ( 'NONE', #59022, #47549, #13381, .T. ) ;
#46305=SURFACE_STYLE_USAGE ( .BOTH. , #40309 ) ;
#46324=CARTESIAN_POINT ( 'NONE',  ( 21.25000000000001066, 24.74999999999998224, 3.750000000000000000 ) ) ;
#46338=ADVANCED_FACE ( 'NONE', ( #37327 ), #47186, .T. ) ;
#46345=ORIENTED_EDGE ( 'NONE', *, *, #37357, .T. ) ;
#46351=DIRECTION ( 'NONE',  ( 0.000000000000000000, 0.000000000000000000, -1.000000000000000000 ) ) ;
#46360=LINE ( 'NONE', #9039, #2238 ) ;
#46362=EDGE_CURVE ( 'NONE', #50231, #65411, #48215, .T. ) ;
#46368=ORIENTED_EDGE ( 'NONE', *, *, #8749, .F. ) ;
#46382=ORIENTED_EDGE ( 'NONE', *, *, #11112, .F. ) ;
#46405=AXIS2_PLACEMENT_3D ( 'NONE', #39740, #14017, #3048 ) ;
#46412=( NAMED_UNIT ( * ) SI_UNIT ( $, .STERADIAN. ) SOLID_ANGLE_UNIT ( ) );
#46413=DIRECTION ( 'NONE',  ( 0.000000000000000000, 1.000000000000000000, 0.000000000000000000 ) ) ;
#46417=ORIENTED_EDGE ( 'NONE', *, *, #11517, .F. ) ;
#46419=LINE ( 'NONE', #13668, #40195 ) ;
#46456=CARTESIAN_POINT ( 'NONE',  ( 25.75000000000001066, 19.24999999999997868, 3.750000000000000000 ) ) ;
#46461=ORIENTED_EDGE ( 'NONE', *, *, #1281, .F. ) ;
#46476=LINE ( 'NONE', #3833, #25334 ) ;
#46477=ORIENTED_EDGE ( 'NONE', *, *, #25169, .F. ) ;
#46483=EDGE_LOOP ( 'NONE', ( #38737, #38797, #17494, #20997 ) ) ;
#46489=ORIENTED_EDGE ( 'NONE', *, *, #7233, .T. ) ;
#46498=ORIENTED_EDGE ( 'NONE', *, *, #54775, .T. ) ;
#46520=EDGE_CURVE ( 'NONE', #56343, #19343, #49796, .T. ) ;
#46525=EDGE_LOOP ( 'NONE', ( #12680, #28237, #66846, #27023 ) ) ;
#46572=ORIENTED_EDGE ( 'NONE', *, *, #62638, .T. ) ;
#46577=ORIENTED_EDGE ( 'NONE', *, *, #55505, .T. ) ;
#46598=ORIENTED_EDGE ( 'NONE', *, *, #27212, .F. ) ;
#46626=AXIS2_PLACEMENT_3D ( 'NONE', #30573, #2780, #51019 ) ;
#46628=VERTEX_POINT ( 'NONE', #31192 ) ;
#46633=AXIS2_PLACEMENT_3D ( 'NONE', #53479, #26707, #49845 ) ;
#46651=CARTESIAN_POINT ( 'NONE',  ( 61.99999999999998579, 30.99999999999999289, 3.750000000000000000 ) ) ;
#46665=FACE_OUTER_BOUND ( 'NONE', #10913, .T. ) ;
#46669=ORIENTED_EDGE ( 'NONE', *, *, #40896, .T. ) ;
#46670=CIRCLE ( 'NONE', #5039, 0.2500000000000002220 ) ;
#46680=DIRECTION ( 'NONE',  ( 0.000000000000000000, 0.000000000000000000, -1.000000000000000000 ) ) ;
#46687=VERTEX_POINT ( 'NONE', #36877 ) ;
#46695=FACE_OUTER_BOUND ( 'NONE', #66503, .T. ) ;
#46731=CARTESIAN_POINT ( 'NONE',  ( 3.249999999999999112, 34.24999999999998579, -3.750000000000000000 ) ) ;
#46733=CARTESIAN_POINT ( 'NONE',  ( 30.50000000000000711, 18.74999999999997868, -3.750000000000000000 ) ) ;
#46796=CARTESIAN_POINT ( 'NONE',  ( 8.250000000000001776, 31.24999999999998579, 4.000000000000000000 ) ) ;
#46814=AXIS2_PLACEMENT_3D ( 'NONE', #46731, #34472, #52652 ) ;
#46826=ORIENTED_EDGE ( 'NONE', *, *, #3878, .T. ) ;
#46831=ORIENTED_EDGE ( 'NONE', *, *, #61051, .F. ) ;
#46849=ORIENTED_EDGE ( 'NONE', *, *, #13589, .T. ) ;
#46859=ORIENTED_EDGE ( 'NONE', *, *, #59951, .T. ) ;
#46869=DIRECTION ( 'NONE',  ( 1.000000000000000000, 7.709882115452468306E-16, -0.000000000000000000 ) ) ;
#46871=DIRECTION ( 'NONE',  ( 0.000000000000000000, 1.000000000000000000, 0.000000000000000000 ) ) ;
#46904=EDGE_CURVE ( 'NONE', #17887, #51828, #3700, .T. ) ;
#46929=EDGE_CURVE ( 'NONE', #68782, #25473, #61645, .T. ) ;
#46930=AXIS2_PLACEMENT_3D ( 'NONE', #44425, #39469, #50688 ) ;
#46932=DIRECTION ( 'NONE',  ( -1.000000000000000000, 0.000000000000000000, 0.000000000000000000 ) ) ;
#46967=DIRECTION ( 'NONE',  ( 0.000000000000000000, -1.000000000000000000, 0.000000000000000000 ) ) ;
#46974=AXIS2_PLACEMENT_3D ( 'NONE', #22833, #49923, #61144 ) ;
#46977=CYLINDRICAL_SURFACE ( 'NONE', #18129, 0.2500000000000002220 ) ;
#46983=EDGE_CURVE ( 'NONE', #50938, #39701, #15020, .T. ) ;
#47000=ORIENTED_EDGE ( 'NONE', *, *, #54927, .F. ) ;
#47010=FILL_AREA_STYLE_COLOUR ( '', #45197 ) ;
#47017=AXIS2_PLACEMENT_3D ( 'NONE', #64544, #11407, #775 ) ;
#47019=ORIENTED_EDGE ( 'NONE', *, *, #4417, .F. ) ;
#47043=CARTESIAN_POINT ( 'NONE',  ( 66.74999999999998579, 34.24999999999999289, -3.750000000000000000 ) ) ;
#47068=ORIENTED_EDGE ( 'NONE', *, *, #24684, .F. ) ;
#47070=DIRECTION ( 'NONE',  ( -1.000000000000000000, 0.000000000000000000, 0.000000000000000000 ) ) ;
#47090=EDGE_LOOP ( 'NONE', ( #18256, #34900, #9100, #15901 ) ) ;
#47100=AXIS2_PLACEMENT_3D ( 'NONE', #33744, #42719, #64117 ) ;
#47106=CIRCLE ( 'NONE', #14474, 0.2500000000000002220 ) ;
#47115=DIRECTION ( 'NONE',  ( 1.000000000000000000, -0.000000000000000000, -0.000000000000000000 ) ) ;
#47119=EDGE_LOOP ( 'NONE', ( #42421, #62674, #29009, #42782 ) ) ;
#47179=CARTESIAN_POINT ( 'NONE',  ( 21.25000000000001066, 24.74999999999998224, -3.750000000000000000 ) ) ;
#47182=DIRECTION ( 'NONE',  ( -1.000000000000000000, 0.000000000000000000, 0.000000000000000000 ) ) ;
#47185=AXIS2_PLACEMENT_3D ( 'NONE', #60904, #66184, #60230 ) ;
#47186=CYLINDRICAL_SURFACE ( 'NONE', #54192, 0.2500000000000002220 ) ;
#47203=AXIS2_PLACEMENT_3D ( 'NONE', #61107, #55828, #41076 ) ;
#47213=DIRECTION ( 'NONE',  ( -1.000000000000000000, 0.000000000000000000, 0.000000000000000000 ) ) ;
#47214=ORIENTED_EDGE ( 'NONE', *, *, #69423, .T. ) ;
#47232=DIRECTION ( 'NONE',  ( 0.000000000000000000, 1.000000000000000000, 0.000000000000000000 ) ) ;
#47241=VERTEX_POINT ( 'NONE', #15515 ) ;
#47245=CARTESIAN_POINT ( 'NONE',  ( 0.000000000000000000, 30.74999999999998579, 3.750000000000000000 ) ) ;
#47257=CARTESIAN_POINT ( 'NONE',  ( 26.00000000000001066, 19.24999999999997868, 3.750000000000000000 ) ) ;
#47275=DIRECTION ( 'NONE',  ( -1.000000000000000000, 0.000000000000000000, 0.000000000000000000 ) ) ;
#47283=DIRECTION ( 'NONE',  ( 0.000000000000000000, 0.000000000000000000, -1.000000000000000000 ) ) ;
#47284=VERTEX_POINT ( 'NONE', #68619 ) ;
#47295=CIRCLE ( 'NONE', #13393, 0.2500000000000002220 ) ;
#47298=DIRECTION ( 'NONE',  ( -1.000000000000000000, 0.000000000000000000, 0.000000000000000000 ) ) ;
#47327=EDGE_CURVE ( 'NONE', #69071, #24587, #2473, .T. ) ;
#47333=CIRCLE ( 'NONE', #56260, 0.2500000000000002220 ) ;
#47334=DIRECTION ( 'NONE',  ( 1.000000000000000000, -0.000000000000000000, 0.000000000000000000 ) ) ;
#47340=VERTEX_POINT ( 'NONE', #69310 ) ;
#47349=ORIENTED_EDGE ( 'NONE', *, *, #22959, .F. ) ;
#47357=ORIENTED_EDGE ( 'NONE', *, *, #43792, .T. ) ;
#47366=LINE ( 'NONE', #51558, #11686 ) ;
#47394=CARTESIAN_POINT ( 'NONE',  ( 57.74999999999998579, 30.74999999999999289, 3.750000000000000000 ) ) ;
#47410=DIRECTION ( 'NONE',  ( 0.000000000000000000, 0.000000000000000000, -1.000000000000000000 ) ) ;
#47427=ORIENTED_EDGE ( 'NONE', *, *, #2216, .T. ) ;
#47433=ORIENTED_EDGE ( 'NONE', *, *, #7312, .T. ) ;
#47455=EDGE_CURVE ( 'NONE', #40202, #56118, #12614, .T. ) ;
#47457=ORIENTED_EDGE ( 'NONE', *, *, #55505, .F. ) ;
#47462=FACE_OUTER_BOUND ( 'NONE', #37029, .T. ) ;
#47465=DIRECTION ( 'NONE',  ( -0.000000000000000000, 1.000000000000000000, -0.000000000000000000 ) ) ;
#47480=AXIS2_PLACEMENT_3D ( 'NONE', #64445, #52867, #37058 ) ;
#47486=COLOUR_RGB ( '', 0.72549020, 0.75294118, 0.79215686) ;
#47530=CARTESIAN_POINT ( 'NONE',  ( 12.75000000000000533, 28.24999999999998224, 3.750000000000000000 ) ) ;
#47535=CARTESIAN_POINT ( 'NONE',  ( 7.899999999999995914, 11.99999999999999289, -3.499999999999991118 ) ) ;
#47539=DIRECTION ( 'NONE',  ( 0.000000000000000000, -0.000000000000000000, 1.000000000000000000 ) ) ;
#47545=EDGE_LOOP ( 'NONE', ( #49401, #60481, #51692, #48749 ) ) ;
#47549=VERTEX_POINT ( 'NONE', #19633 ) ;
#47558=ADVANCED_FACE ( 'NONE', ( #61159 ), #45717, .T. ) ;
#47566=ADVANCED_FACE ( 'NONE', ( #23514 ), #12967, .F. ) ;
#47569=DIRECTION ( 'NONE',  ( 0.000000000000000000, 1.000000000000000000, 0.000000000000000000 ) ) ;
#47574=EDGE_CURVE ( 'NONE', #44314, #51526, #2524, .T. ) ;
#47575=DIRECTION ( 'NONE',  ( 0.000000000000000000, 0.000000000000000000, -1.000000000000000000 ) ) ;
#47581=ADVANCED_FACE ( 'NONE', ( #34760 ), #36317, .F. ) ;
#47590=DIRECTION ( 'NONE',  ( 1.000000000000000000, 0.000000000000000000, 0.000000000000000000 ) ) ;
#47592=FACE_OUTER_BOUND ( 'NONE', #54119, .T. ) ;
#47609=DIRECTION ( 'NONE',  ( 1.000000000000000000, -0.000000000000000000, 0.000000000000000000 ) ) ;
#47622=AXIS2_PLACEMENT_3D ( 'NONE', #5875, #27318, #16820 ) ;
#47653=AXIS2_PLACEMENT_3D ( 'NONE', #43092, #64501, #15993 ) ;
#47686=CARTESIAN_POINT ( 'NONE',  ( 48.74999999999999289, 24.74999999999998579, -3.750000000000000000 ) ) ;
#47691=CYLINDRICAL_SURFACE ( 'NONE', #9559, 0.2500000000000002220 ) ;
#47709=VERTEX_POINT ( 'NONE', #42877 ) ;
#47716=ADVANCED_FACE ( 'NONE', ( #47462 ), #3765, .F. ) ;
#47736=CIRCLE ( 'NONE', #12858, 0.2500000000000002220 ) ;
#47744=CARTESIAN_POINT ( 'NONE',  ( 1.000000000000000000, 1.000000000000000222, 4.000000000000000000 ) ) ;
#47753=DIRECTION ( 'NONE',  ( 1.156482317317870344E-15, 1.000000000000000000, 0.000000000000000000 ) ) ;
#47775=CIRCLE ( 'NONE', #66859, 0.2500000000000002220 ) ;
#47779=LINE ( 'NONE', #37202, #63238 ) ;
#47794=ADVANCED_FACE ( 'NONE', ( #17162 ), #53709, .T. ) ;
#47795=VECTOR ( 'NONE', #57497, 1000.000000000000000 ) ;
#47819=DIRECTION ( 'NONE',  ( 0.000000000000000000, -1.000000000000000000, 0.000000000000000000 ) ) ;
#47851=DIRECTION ( 'NONE',  ( 0.000000000000000000, -1.000000000000000000, 0.000000000000000000 ) ) ;
#47868=EDGE_LOOP ( 'NONE', ( #48917, #33458, #64539, #31041 ) ) ;
#47878=ORIENTED_EDGE ( 'NONE', *, *, #65011, .T. ) ;
#47917=CARTESIAN_POINT ( 'NONE',  ( 66.24999999999998579, 34.24999999999999289, 3.750000000000000000 ) ) ;
#47918=CARTESIAN_POINT ( 'NONE',  ( 57.74999999999998579, 30.74999999999999289, 3.750000000000000000 ) ) ;
#47920=ORIENTED_EDGE ( 'NONE', *, *, #56795, .F. ) ;
#47925=CARTESIAN_POINT ( 'NONE',  ( 1.000000000000000000, 1.000000000000000222, 3.000000000000000000 ) ) ;
#47949=CARTESIAN_POINT ( 'NONE',  ( 3.499999999999998668, 36.99999999999999289, 4.000000000000000000 ) ) ;
#47955=DIRECTION ( 'NONE',  ( 0.000000000000000000, 0.000000000000000000, -1.000000000000000000 ) ) ;
#47973=EDGE_CURVE ( 'NONE', #16642, #6607, #25179, .T. ) ;
#47980=EDGE_CURVE ( 'NONE', #10058, #7106, #25077, .T. ) ;
#47981=DIRECTION ( 'NONE',  ( 0.000000000000000000, 0.000000000000000000, -1.000000000000000000 ) ) ;
#47982=COLOUR_RGB ( '', 0.72549020, 0.75294118, 0.79215686) ;
#47989=SURFACE_STYLE_USAGE ( .BOTH. , #26463 ) ;
#47990=VERTEX_POINT ( 'NONE', #57177 ) ;
#48005=CARTESIAN_POINT ( 'NONE',  ( 0.000000000000000000, 36.99999999999999289, 3.750000000000000000 ) ) ;
#48027=ADVANCED_FACE ( 'NONE', ( #46695 ), #68807, .T. ) ;
#48045=VERTEX_POINT ( 'NONE', #63633 ) ;
#48053=ORIENTED_EDGE ( 'NONE', *, *, #33909, .T. ) ;
#48059=AXIS2_PLACEMENT_3D ( 'NONE', #45385, #14024, #24548 ) ;
#48100=DIRECTION ( 'NONE',  ( -1.000000000000000000, 0.000000000000000000, 0.000000000000000000 ) ) ;
#48109=EDGE_CURVE ( 'NONE', #7659, #2804, #42920, .T. ) ;
#48117=LINE ( 'NONE', #15735, #11368 ) ;
#48121=DIRECTION ( 'NONE',  ( 0.000000000000000000, -1.000000000000000000, 0.000000000000000000 ) ) ;
#48134=CARTESIAN_POINT ( 'NONE',  ( 68.99999999999998579, 36.75000000000000000, -4.000000000000000000 ) ) ;
#48136=DIRECTION ( 'NONE',  ( 0.000000000000000000, -0.000000000000000000, 1.000000000000000000 ) ) ;
#48141=FACE_OUTER_BOUND ( 'NONE', #40415, .T. ) ;
#48142=DIRECTION ( 'NONE',  ( -1.156482317317870344E-15, 1.000000000000000000, 0.000000000000000000 ) ) ;
#48154=DIRECTION ( 'NONE',  ( 0.000000000000000000, 0.000000000000000000, 1.000000000000000000 ) ) ;
#48169=EDGE_CURVE ( 'NONE', #3561, #68782, #33354, .T. ) ;
#48191=CIRCLE ( 'NONE', #24525, 0.5000000000000004441 ) ;
#48201=ORIENTED_EDGE ( 'NONE', *, *, #61937, .F. ) ;
#48215=LINE ( 'NONE', #57343, #55301 ) ;
#48232=CARTESIAN_POINT ( 'NONE',  ( 39.74999999999999289, 18.74999999999997868, 4.000000000000000000 ) ) ;
#48243=DIRECTION ( 'NONE',  ( 1.000000000000000000, 0.000000000000000000, -0.000000000000000000 ) ) ;
#48274=EDGE_CURVE ( 'NONE', #13649, #60291, #51266, .T. ) ;
#48275=ORIENTED_EDGE ( 'NONE', *, *, #16402, .T. ) ;
#48308=CARTESIAN_POINT ( 'NONE',  ( 62.24999999999998579, 33.99999999999999289, -3.750000000000000000 ) ) ;
#48310=VECTOR ( 'NONE', #35060, 1000.000000000000000 ) ;
#48323=AXIS2_PLACEMENT_3D ( 'NONE', #58217, #63150, #68428 ) ;
#48325=FACE_OUTER_BOUND ( 'NONE', #69093, .T. ) ;
#48331=DIRECTION ( 'NONE',  ( 0.000000000000000000, 0.000000000000000000, -1.000000000000000000 ) ) ;
#48338=CIRCLE ( 'NONE', #6703, 0.2500000000000002220 ) ;
#48343=EDGE_CURVE ( 'NONE', #54480, #17044, #31522, .T. ) ;
#48367=CARTESIAN_POINT ( 'NONE',  ( 68.99999999999998579, 36.75000000000000000, -3.750000000000000000 ) ) ;
#48381=CARTESIAN_POINT ( 'NONE',  ( 21.24999999999998579, -2.457524924300472510E-14, 4.000000000000000000 ) ) ;
#48391=FACE_OUTER_BOUND ( 'NONE', #61993, .T. ) ;
#48408=EDGE_CURVE ( 'NONE', #54091, #58809, #9480, .T. ) ;
#48425=STYLED_ITEM ( 'NONE', ( #9129 ), #59640 ) ;
#48447=FACE_OUTER_BOUND ( 'NONE', #20115, .T. ) ;
#48459=DIRECTION ( 'NONE',  ( -0.000000000000000000, 1.000000000000000000, -0.000000000000000000 ) ) ;
#48478=TOROIDAL_SURFACE ( 'NONE', #36112, 0.5000000000000000000, 0.2500000000000000000 ) ;
#48487=CARTESIAN_POINT ( 'NONE',  ( 66.74999999999998579, 36.75000000000000000, 3.750000000000000000 ) ) ;
#48488=CARTESIAN_POINT ( 'NONE',  ( 3.250000000000003553, 4.698209414103854191E-16, 3.750000000000000000 ) ) ;
#48495=PLANE ( 'NONE',  #43368 ) ;
#48499=CARTESIAN_POINT ( 'NONE',  ( 8.250000000000001776, 31.24999999999998579, 3.750000000000000000 ) ) ;
#48504=EDGE_CURVE ( 'NONE', #52155, #13744, #45465, .T. ) ;
#48531=ORIENTED_EDGE ( 'NONE', *, *, #36356, .F. ) ;
#48553=DIRECTION ( 'NONE',  ( 0.000000000000000000, -0.000000000000000000, 1.000000000000000000 ) ) ;
#48584=ORIENTED_EDGE ( 'NONE', *, *, #36180, .T. ) ;
#48597=DIRECTION ( 'NONE',  ( 0.000000000000000000, 0.000000000000000000, 1.000000000000000000 ) ) ;
#48604=CARTESIAN_POINT ( 'NONE',  ( 62.24999999999998579, 33.74999999999999289, -4.000000000000000000 ) ) ;
#48623=CARTESIAN_POINT ( 'NONE',  ( 1.000000000000000000, 36.99999999999999289, -3.750000000000000000 ) ) ;
#48657=CARTESIAN_POINT ( 'NONE',  ( 7.750000000000001776, 31.24999999999998579, -3.750000000000000000 ) ) ;
#48658=ADVANCED_FACE ( 'NONE', ( #37831 ), #54432, .T. ) ;
#48686=EDGE_CURVE ( 'NONE', #62878, #18810, #60062, .T. ) ;
#48690=AXIS2_PLACEMENT_3D ( 'NONE', #33388, #1669, #5593 ) ;
#48693=VECTOR ( 'NONE', #20406, 1000.000000000000000 ) ;
#48709=DIRECTION ( 'NONE',  ( 0.000000000000000000, 1.000000000000000000, 0.000000000000000000 ) ) ;
#48727=ORIENTED_EDGE ( 'NONE', *, *, #28513, .T. ) ;
#48728=EDGE_CURVE ( 'NONE', #47709, #7106, #59912, .T. ) ;
#48749=ORIENTED_EDGE ( 'NONE', *, *, #18590, .T. ) ;
#48753=DIRECTION ( 'NONE',  ( -0.000000000000000000, 0.000000000000000000, -1.000000000000000000 ) ) ;
#48755=VERTEX_POINT ( 'NONE', #42755 ) ;
#48773=VECTOR ( 'NONE', #1271, 1000.000000000000000 ) ;
#48790=CARTESIAN_POINT ( 'NONE',  ( 39.24999999999999289, 15.74999999999997513, 3.750000000000000000 ) ) ;
#48800=EDGE_LOOP ( 'NONE', ( #46345, #19770, #31121, #66489 ) ) ;
#48812=ADVANCED_FACE ( 'NONE', ( #62589 ), #3103, .T. ) ;
#48835=ORIENTED_EDGE ( 'NONE', *, *, #48109, .F. ) ;
#48836=CARTESIAN_POINT ( 'NONE',  ( 30.75000000000001066, 15.99999999999997691, -3.750000000000000000 ) ) ;
#48839=LINE ( 'NONE', #62455, #49103 ) ;
#48858=CARTESIAN_POINT ( 'NONE',  ( 30.75000000000001066, 16.24999999999997513, -4.000000000000000000 ) ) ;
#48862=DIRECTION ( 'NONE',  ( -0.000000000000000000, 1.000000000000000000, -0.000000000000000000 ) ) ;
#48869=AXIS2_PLACEMENT_3D ( 'NONE', #7925, #61709, #18821 ) ;
#48892=ORIENTED_EDGE ( 'NONE', *, *, #15373, .F. ) ;
#48894=ORIENTED_EDGE ( 'NONE', *, *, #57754, .F. ) ;
#48897=ORIENTED_EDGE ( 'NONE', *, *, #41502, .F. ) ;
#48901=ADVANCED_FACE ( 'NONE', ( #19334 ), #38772, .T. ) ;
#48917=ORIENTED_EDGE ( 'NONE', *, *, #30893, .F. ) ;
#48928=DIRECTION ( 'NONE',  ( -1.000000000000000000, -1.224646799147353207E-16, -0.000000000000000000 ) ) ;
#48944=EDGE_LOOP ( 'NONE', ( #30035, #55938, #63681, #13432 ) ) ;
#48977=DIRECTION ( 'NONE',  ( 0.000000000000000000, 1.000000000000000000, 0.000000000000000000 ) ) ;
#48998=ORIENTED_EDGE ( 'NONE', *, *, #63838, .F. ) ;
#49000=LINE ( 'NONE', #63136, #26610 ) ;
#49005=ORIENTED_EDGE ( 'NONE', *, *, #13762, .T. ) ;
#49006=UNCERTAINTY_MEASURE_WITH_UNIT (LENGTH_MEASURE( 1.000000000000000082E-05 ), #16538, 'distance_accuracy_value', 'NONE');
#49036=CIRCLE ( 'NONE', #32124, 0.2500000000000002220 ) ;
#49057=ADVANCED_FACE ( 'NONE', ( #6601 ), #12578, .T. ) ;
#49064=FILL_AREA_STYLE ('',( #63800 ) ) ;
#49067=CARTESIAN_POINT ( 'NONE',  ( 44.25000000000000000, 19.24999999999998224, -3.750000000000000000 ) ) ;
#49073=ORIENTED_EDGE ( 'NONE', *, *, #13762, .F. ) ;
#49074=DIRECTION ( 'NONE',  ( 0.000000000000000000, 1.000000000000000000, 0.000000000000000000 ) ) ;
#49085=CYLINDRICAL_SURFACE ( 'NONE', #50550, 0.2500000000000002220 ) ;
#49094=CARTESIAN_POINT ( 'NONE',  ( 12.25000000000000533, 28.24999999999998224, -4.000000000000000000 ) ) ;
#49099=EDGE_LOOP ( 'NONE', ( #25301, #39704, #41962, #35543 ) ) ;
#49103=VECTOR ( 'NONE', #66341, 1000.000000000000000 ) ;
#49141=CIRCLE ( 'NONE', #27747, 0.2500000000000002220 ) ;
#49147=DIRECTION ( 'NONE',  ( -1.000000000000000000, 0.000000000000000000, 0.000000000000000000 ) ) ;
#49152=AXIS2_PLACEMENT_3D ( 'NONE', #50945, #45360, #45702 ) ;
#49159=CARTESIAN_POINT ( 'NONE',  ( 12.75000000000000533, 28.24999999999998224, 3.750000000000000000 ) ) ;
#49161=CARTESIAN_POINT ( 'NONE',  ( 44.25000000000000000, 19.24999999999998224, -4.000000000000000000 ) ) ;
#49167=DIRECTION ( 'NONE',  ( 0.000000000000000000, -1.000000000000000000, 0.000000000000000000 ) ) ;
#49198=ORIENTED_EDGE ( 'NONE', *, *, #68793, .F. ) ;
#49203=CARTESIAN_POINT ( 'NONE',  ( 0.000000000000000000, 0.000000000000000000, -3.000000000000000000 ) ) ;
#49225=DIRECTION ( 'NONE',  ( 0.000000000000000000, 0.000000000000000000, -1.000000000000000000 ) ) ;
#49227=DIRECTION ( 'NONE',  ( -1.000000000000000000, 0.000000000000000000, 0.000000000000000000 ) ) ;
#49228=ORIENTED_EDGE ( 'NONE', *, *, #66881, .F. ) ;
#49229=CARTESIAN_POINT ( 'NONE',  ( 61.74999999999998579, 31.24999999999999289, -4.000000000000000000 ) ) ;
#49237=ORIENTED_EDGE ( 'NONE', *, *, #11505, .F. ) ;
#49242=AXIS2_PLACEMENT_3D ( 'NONE', #15978, #31410, #31071 ) ;
#49253=ORIENTED_EDGE ( 'NONE', *, *, #40628, .T. ) ;
#49260=DIRECTION ( 'NONE',  ( 0.000000000000000000, 0.000000000000000000, 1.000000000000000000 ) ) ;
#49305=CIRCLE ( 'NONE', #18938, 0.5000000000000004441 ) ;
#49315=LINE ( 'NONE', #59857, #34026 ) ;
#49330=EDGE_CURVE ( 'NONE', #65996, #31245, #60165, .T. ) ;
#49341=FACE_OUTER_BOUND ( 'NONE', #39269, .T. ) ;
#49348=VECTOR ( 'NONE', #1864, 1000.000000000000000 ) ;
#49355=CIRCLE ( 'NONE', #32505, 3.100000000000005418 ) ;
#49360=FACE_OUTER_BOUND ( 'NONE', #29554, .T. ) ;
#49376=DIRECTION ( 'NONE',  ( -1.000000000000000000, 0.000000000000000000, 0.000000000000000000 ) ) ;
#49389=ORIENTED_EDGE ( 'NONE', *, *, #43771, .F. ) ;
#49401=ORIENTED_EDGE ( 'NONE', *, *, #18869, .F. ) ;
#49407=CARTESIAN_POINT ( 'NONE',  ( 7.750000000000002665, 31.24999999999998579, 4.000000000000000000 ) ) ;
#49421=ADVANCED_FACE ( 'NONE', ( #11471 ), #5833, .T. ) ;
#49426=EDGE_CURVE ( 'NONE', #60408, #13725, #8520, .T. ) ;
#49453=DIRECTION ( 'NONE',  ( 0.000000000000000000, -1.000000000000000000, 0.000000000000000000 ) ) ;
#49467=VERTEX_POINT ( 'NONE', #12150 ) ;
#49473=CARTESIAN_POINT ( 'NONE',  ( 25.75000000000001066, 21.74999999999998224, 3.750000000000000000 ) ) ;
#49486=DIRECTION ( 'NONE',  ( 0.000000000000000000, 0.000000000000000000, -1.000000000000000000 ) ) ;
#49488=AXIS2_PLACEMENT_3D ( 'NONE', #50557, #12548, #2280 ) ;
#49495=DIRECTION ( 'NONE',  ( 0.000000000000000000, 0.000000000000000000, 1.000000000000000000 ) ) ;
#49506=CARTESIAN_POINT ( 'NONE',  ( 61.99999999999998579, 31.24999999999999289, 3.750000000000000000 ) ) ;
#49522=PLANE ( 'NONE',  #67570 ) ;
#49525=CYLINDRICAL_SURFACE ( 'NONE', #14676, 0.2500000000000002220 ) ;
#49531=ADVANCED_FACE ( 'NONE', ( #62073 ), #39981, .T. ) ;
#49533=AXIS2_PLACEMENT_3D ( 'NONE', #41419, #45994, #56514 ) ;
#49554=DIRECTION ( 'NONE',  ( -1.000000000000000000, 0.000000000000000000, 0.000000000000000000 ) ) ;
#49557=AXIS2_PLACEMENT_3D ( 'NONE', #22194, #6692, #65802 ) ;
#49569=CARTESIAN_POINT ( 'NONE',  ( 17.00000000000000711, 27.74999999999998224, 3.750000000000000000 ) ) ;
#49586=AXIS2_PLACEMENT_3D ( 'NONE', #65174, #12390, #17711 ) ;
#49592=VECTOR ( 'NONE', #46869, 1000.000000000000000 ) ;
#49613=DIRECTION ( 'NONE',  ( -7.709882115452441682E-16, -1.000000000000000000, 0.000000000000000000 ) ) ;
#49615=CARTESIAN_POINT ( 'NONE',  ( 39.74999999999999289, 18.74999999999997868, 4.000000000000000000 ) ) ;
#49619=ORIENTED_EDGE ( 'NONE', *, *, #10104, .T. ) ;
#49661=VECTOR ( 'NONE', #67434, 1000.000000000000000 ) ;
#49667=VECTOR ( 'NONE', #3201, 1000.000000000000000 ) ;
#49685=ORIENTED_EDGE ( 'NONE', *, *, #48504, .F. ) ;
#49750=SPHERICAL_SURFACE ( 'NONE', #31436, 0.2500000000000000000 ) ;
#49757=AXIS2_PLACEMENT_3D ( 'NONE', #49911, #44661, #66053 ) ;
#49758=CARTESIAN_POINT ( 'NONE',  ( 21.75000000000001066, 21.99999999999998224, -3.750000000000000000 ) ) ;
#49760=CYLINDRICAL_SURFACE ( 'NONE', #7271, 0.2500000000000002220 ) ;
#49786=DIRECTION ( 'NONE',  ( 1.000000000000000000, 0.000000000000000000, 0.000000000000000000 ) ) ;
#49796=CIRCLE ( 'NONE', #31798, 0.2500000000000002220 ) ;
#49798=DIRECTION ( 'NONE',  ( 0.000000000000000000, 0.000000000000000000, -1.000000000000000000 ) ) ;
#49803=EDGE_LOOP ( 'NONE', ( #16102, #945, #21427, #29813 ) ) ;
#49807=EDGE_LOOP ( 'NONE', ( #64772, #65424, #349, #44740 ) ) ;
#49811=CIRCLE ( 'NONE', #19467, 3.599999999999992095 ) ;
#49814=TOROIDAL_SURFACE ( 'NONE', #36402, 0.7500000000000000000, 0.2500000000000000000 ) ;
#49817=VERTEX_POINT ( 'NONE', #59922 ) ;
#49845=DIRECTION ( 'NONE',  ( -1.000000000000000000, 0.000000000000000000, 0.000000000000000000 ) ) ;
#49898=CARTESIAN_POINT ( 'NONE',  ( 1.000000000000000000, 36.74999999999999289, -3.000000000000000000 ) ) ;
#49906=CIRCLE ( 'NONE', #420, 0.2500000000000002220 ) ;
#49907=ORIENTED_EDGE ( 'NONE', *, *, #42320, .F. ) ;
#49910=CIRCLE ( 'NONE', #64511, 0.2500000000000002220 ) ;
#49911=CARTESIAN_POINT ( 'NONE',  ( 48.25000000000000000, 22.24999999999998579, 3.750000000000000000 ) ) ;
#49916=LINE ( 'NONE', #1970, #40064 ) ;
#49923=DIRECTION ( 'NONE',  ( 0.000000000000000000, 1.000000000000000000, 0.000000000000000000 ) ) ;
#49926=DIRECTION ( 'NONE',  ( 0.000000000000000000, 0.000000000000000000, -1.000000000000000000 ) ) ;
#49955=CARTESIAN_POINT ( 'NONE',  ( 16.75000000000000711, 27.74999999999998224, 4.000000000000000000 ) ) ;
#49970=CYLINDRICAL_SURFACE ( 'NONE', #4525, 0.2500000000000002220 ) ;
#49971=DIRECTION ( 'NONE',  ( -1.000000000000000000, 0.000000000000000000, 0.000000000000000000 ) ) ;
#49974=ORIENTED_EDGE ( 'NONE', *, *, #5707, .T. ) ;
#49977=AXIS2_PLACEMENT_3D ( 'NONE', #37720, #1347, #49613 ) ;
#49988=DIRECTION ( 'NONE',  ( -1.000000000000000000, 0.000000000000000000, 0.000000000000000000 ) ) ;
#50001=AXIS2_PLACEMENT_3D ( 'NONE', #16779, #40227, #19072 ) ;
#50025=ADVANCED_FACE ( 'NONE', ( #9259 ), #14510, .T. ) ;
#50036=ORIENTED_EDGE ( 'NONE', *, *, #13369, .F. ) ;
#50065=EDGE_CURVE ( 'NONE', #5853, #60408, #28820, .T. ) ;
#50083=DIRECTION ( 'NONE',  ( 1.000000000000000000, -0.000000000000000000, 0.000000000000000000 ) ) ;
#50154=DIRECTION ( 'NONE',  ( 0.000000000000000000, 0.000000000000000000, 1.000000000000000000 ) ) ;
#50155=CARTESIAN_POINT ( 'NONE',  ( 44.25000000000000000, 21.74999999999998579, -3.750000000000000000 ) ) ;
#50162=ORIENTED_EDGE ( 'NONE', *, *, #3541, .F. ) ;
#50178=VERTEX_POINT ( 'NONE', #8484 ) ;
#50231=VERTEX_POINT ( 'NONE', #68605 ) ;
#50238=ORIENTED_EDGE ( 'NONE', *, *, #22503, .T. ) ;
#50248=CARTESIAN_POINT ( 'NONE',  ( 8.250000000000001776, 31.24999999999998579, -3.750000000000000000 ) ) ;
#50258=FACE_OUTER_BOUND ( 'NONE', #32504, .T. ) ;
#50263=ORIENTED_EDGE ( 'NONE', *, *, #8845, .T. ) ;
#50268=DIRECTION ( 'NONE',  ( 0.000000000000000000, 1.000000000000000000, -0.000000000000000000 ) ) ;
#50275=ORIENTED_EDGE ( 'NONE', *, *, #39642, .T. ) ;
#50287=CYLINDRICAL_SURFACE ( 'NONE', #21920, 0.2500000000000002220 ) ;
#50295=DIRECTION ( 'NONE',  ( -0.000000000000000000, -0.000000000000000000, -1.000000000000000000 ) ) ;
#50314=ORIENTED_EDGE ( 'NONE', *, *, #4417, .T. ) ;
#50339=FACE_OUTER_BOUND ( 'NONE', #55847, .T. ) ;
#50345=CIRCLE ( 'NONE', #47017, 0.2500000000000002220 ) ;
#50362=DIRECTION ( 'NONE',  ( 0.000000000000000000, 1.000000000000000000, -0.000000000000000000 ) ) ;
#50370=AXIS2_PLACEMENT_3D ( 'NONE', #33716, #30159, #24892 ) ;
#50374=DIRECTION ( 'NONE',  ( 0.000000000000000000, 1.000000000000000000, 0.000000000000000000 ) ) ;
#50390=VERTEX_POINT ( 'NONE', #27287 ) ;
#50400=CIRCLE ( 'NONE', #57121, 0.7499999999999997780 ) ;
#50420=AXIS2_PLACEMENT_3D ( 'NONE', #67238, #50374, #7794 ) ;
#50428=ORIENTED_EDGE ( 'NONE', *, *, #23047, .F. ) ;
#50433=EDGE_LOOP ( 'NONE', ( #34714, #44356, #25972, #43633 ) ) ;
#50443=DIRECTION ( 'NONE',  ( -0.000000000000000000, -0.000000000000000000, 1.000000000000000000 ) ) ;
#50489=ORIENTED_EDGE ( 'NONE', *, *, #39482, .F. ) ;
#50502=ORIENTED_EDGE ( 'NONE', *, *, #11112, .T. ) ;
#50510=AXIS2_PLACEMENT_3D ( 'NONE', #1089, #54953, #7821 ) ;
#50512=AXIS2_PLACEMENT_3D ( 'NONE', #46242, #14531, #19099 ) ;
#50513=EDGE_CURVE ( 'NONE', #36379, #58413, #54757, .T. ) ;
#50550=AXIS2_PLACEMENT_3D ( 'NONE', #44168, #11052, #54989 ) ;
#50557=CARTESIAN_POINT ( 'NONE',  ( 25.75000000000001066, 21.99999999999998224, -3.750000000000000000 ) ) ;
#50561=DIRECTION ( 'NONE',  ( -1.000000000000000000, 0.000000000000000000, 0.000000000000000000 ) ) ;
#50565=CARTESIAN_POINT ( 'NONE',  ( 3.249999999999998668, 36.74999999999999289, -4.000000000000000000 ) ) ;
#50572=AXIS2_PLACEMENT_3D ( 'NONE', #29865, #7710, #23893 ) ;
#50577=EDGE_LOOP ( 'NONE', ( #17968, #30831, #11103, #29810 ) ) ;
#50579=CARTESIAN_POINT ( 'NONE',  ( 30.75000000000001066, 15.74999999999997513, 4.000000000000000000 ) ) ;
#50585=DIRECTION ( 'NONE',  ( 1.000000000000000000, 0.000000000000000000, 0.000000000000000000 ) ) ;
#50610=DIRECTION ( 'NONE',  ( -1.000000000000000000, 0.000000000000000000, 0.000000000000000000 ) ) ;
#50616=ORIENTED_EDGE ( 'NONE', *, *, #29619, .T. ) ;
#50625=( GEOMETRIC_REPRESENTATION_CONTEXT ( 3 ) GLOBAL_UNCERTAINTY_ASSIGNED_CONTEXT ( ( #15904 ) ) GLOBAL_UNIT_ASSIGNED_CONTEXT ( ( #28086, #13313, #34772 ) ) REPRESENTATION_CONTEXT ( 'NONE', 'WORKASPACE' ) );
#50654=CIRCLE ( 'NONE', #39437, 0.2500000000000002220 ) ;
#50657=ORIENTED_EDGE ( 'NONE', *, *, #59242, .T. ) ;
#50663=CARTESIAN_POINT ( 'NONE',  ( 66.74999999999998579, 37.00000000000000000, 4.000000000000000000 ) ) ;
#50670=ORIENTED_EDGE ( 'NONE', *, *, #29636, .F. ) ;
#50678=DIRECTION ( 'NONE',  ( -1.000000000000000000, 0.000000000000000000, 0.000000000000000000 ) ) ;
#50688=DIRECTION ( 'NONE',  ( 0.000000000000000000, 0.000000000000000000, -1.000000000000000000 ) ) ;
#50697=DIRECTION ( 'NONE',  ( -0.000000000000000000, -0.000000000000000000, 1.000000000000000000 ) ) ;
#50711=CARTESIAN_POINT ( 'NONE',  ( 1.000000000000000000, 36.99999999999999289, 3.000000000000000000 ) ) ;
#50715=CIRCLE ( 'NONE', #61883, 0.2500000000000002220 ) ;
#50720=ORIENTED_EDGE ( 'NONE', *, *, #68793, .T. ) ;
#50727=CIRCLE ( 'NONE', #65328, 0.5000000000000004441 ) ;
#50728=DIRECTION ( 'NONE',  ( 0.000000000000000000, 0.000000000000000000, -1.000000000000000000 ) ) ;
#50747=DIRECTION ( 'NONE',  ( 0.000000000000000000, 0.000000000000000000, -1.000000000000000000 ) ) ;
#50748=CARTESIAN_POINT ( 'NONE',  ( 17.25000000000000711, 24.99999999999998224, -3.750000000000000000 ) ) ;
#50763=CYLINDRICAL_SURFACE ( 'NONE', #31932, 0.2500000000000002220 ) ;
#50793=PLANE ( 'NONE',  #42123 ) ;
#50859=LINE ( 'NONE', #35382, #59999 ) ;
#50861=ORIENTED_EDGE ( 'NONE', *, *, #63605, .F. ) ;
#50866=AXIS2_PLACEMENT_3D ( 'NONE', #68531, #42521, #15097 ) ;
#50867=DIRECTION ( 'NONE',  ( 0.000000000000000000, 0.000000000000000000, -1.000000000000000000 ) ) ;
#50903=AXIS2_PLACEMENT_3D ( 'NONE', #8818, #7767, #34173 ) ;
#50908=DIRECTION ( 'NONE',  ( -0.000000000000000000, -0.000000000000000000, 1.000000000000000000 ) ) ;
#50924=EDGE_CURVE ( 'NONE', #62693, #47990, #34636, .T. ) ;
#50925=DIRECTION ( 'NONE',  ( -1.000000000000000000, 0.000000000000000000, 0.000000000000000000 ) ) ;
#50938=VERTEX_POINT ( 'NONE', #25425 ) ;
#50945=CARTESIAN_POINT ( 'NONE',  ( 62.24999999999998579, 33.74999999999999289, -3.750000000000000000 ) ) ;
#50949=ORIENTED_EDGE ( 'NONE', *, *, #25736, .F. ) ;
#50950=MANIFOLD_SOLID_BREP ( 'Fillet4', #31758 ) ;
#51002=CARTESIAN_POINT ( 'NONE',  ( 26.25000000000001066, 19.24999999999997868, -4.000000000000000000 ) ) ;
#51014=CARTESIAN_POINT ( 'NONE',  ( 53.25000000000000000, 25.24999999999998579, -4.000000000000000000 ) ) ;
#51019=DIRECTION ( 'NONE',  ( -1.000000000000000000, 0.000000000000000000, 0.000000000000000000 ) ) ;
#51029=ORIENTED_EDGE ( 'NONE', *, *, #4252, .T. ) ;
#51044=ORIENTED_EDGE ( 'NONE', *, *, #25327, .F. ) ;
#51047=AXIS2_PLACEMENT_3D ( 'NONE', #43537, #64923, #65280 ) ;
#51048=CARTESIAN_POINT ( 'NONE',  ( 8.000000000000001776, 30.99999999999998579, 3.750000000000000000 ) ) ;
#51051=ORIENTED_EDGE ( 'NONE', *, *, #41265, .T. ) ;
#51058=DIRECTION ( 'NONE',  ( -2.312964634635740689E-15, 1.000000000000000000, -0.000000000000000000 ) ) ;
#51066=VERTEX_POINT ( 'NONE', #43173 ) ;
#51088=EDGE_CURVE ( 'NONE', #33844, #31555, #48191, .T. ) ;
#51096=ORIENTED_EDGE ( 'NONE', *, *, #59549, .T. ) ;
#51136=EDGE_CURVE ( 'NONE', #59005, #51323, #28650, .T. ) ;
#51167=DIRECTION ( 'NONE',  ( 1.000000000000000000, -7.709882115452469292E-16, 0.000000000000000000 ) ) ;
#51170=ADVANCED_FACE ( 'NONE', ( #59625 ), #25697, .T. ) ;
#51193=VECTOR ( 'NONE', #3329, 1000.000000000000000 ) ;
#51203=FACE_OUTER_BOUND ( 'NONE', #43643, .T. ) ;
#51210=ORIENTED_EDGE ( 'NONE', *, *, #12210, .T. ) ;
#51212=ORIENTED_EDGE ( 'NONE', *, *, #33291, .T. ) ;
#51218=CARTESIAN_POINT ( 'NONE',  ( 8.250000000000001776, 30.99999999999998579, -3.750000000000000000 ) ) ;
#51227=AXIS2_PLACEMENT_3D ( 'NONE', #1511, #39586, #22686 ) ;
#51234=SPHERICAL_SURFACE ( 'NONE', #66904, 0.2500000000000000000 ) ;
#51244=ORIENTED_EDGE ( 'NONE', *, *, #26539, .F. ) ;
#51266=LINE ( 'NONE', #67093, #15067 ) ;
#51267=EDGE_CURVE ( 'NONE', #7454, #20493, #5486, .T. ) ;
#51283=CARTESIAN_POINT ( 'NONE',  ( 25.75000000000001066, 21.74999999999998224, -4.000000000000000000 ) ) ;
#51292=CIRCLE ( 'NONE', #54645, 0.5000000000000004441 ) ;
#51295=EDGE_CURVE ( 'NONE', #62934, #33844, #42999, .T. ) ;
#51297=ORIENTED_EDGE ( 'NONE', *, *, #26210, .T. ) ;
#51312=LINE ( 'NONE', #46063, #60393 ) ;
#51323=VERTEX_POINT ( 'NONE', #58784 ) ;
#51329=PLANE ( 'NONE',  #50572 ) ;
#51368=ORIENTED_EDGE ( 'NONE', *, *, #57852, .T. ) ;
#51380=ORIENTED_EDGE ( 'NONE', *, *, #52123, .T. ) ;
#51419=CARTESIAN_POINT ( 'NONE',  ( 39.24999999999999289, 16.24999999999997513, 4.000000000000000000 ) ) ;
#51433=CARTESIAN_POINT ( 'NONE',  ( 1.000000000000000000, 1.000000000000000888, -4.000000000000000000 ) ) ;
#51438=CARTESIAN_POINT ( 'NONE',  ( 0.000000000000000000, 27.74999999999998224, 3.750000000000000000 ) ) ;
#51453=CARTESIAN_POINT ( 'NONE',  ( 17.00000000000000711, 27.74999999999998224, -3.750000000000000000 ) ) ;
#51472=ORIENTED_EDGE ( 'NONE', *, *, #61390, .F. ) ;
#51501=VECTOR ( 'NONE', #24310, 1000.000000000000000 ) ;
#51513=DIRECTION ( 'NONE',  ( -1.000000000000000000, 0.000000000000000000, 0.000000000000000000 ) ) ;
#51518=CARTESIAN_POINT ( 'NONE',  ( 12.25000000000000355, 30.74999999999998579, -4.000000000000000000 ) ) ;
#51526=VERTEX_POINT ( 'NONE', #46094 ) ;
#51558=CARTESIAN_POINT ( 'NONE',  ( 62.24999999999998579, 33.99999999999999289, -3.750000000000000000 ) ) ;
#51630=VERTEX_POINT ( 'NONE', #894 ) ;
#51651=CARTESIAN_POINT ( 'NONE',  ( 12.25000000000002132, 7.083454193571968087E-15, 3.750000000000000000 ) ) ;
#51660=VERTEX_POINT ( 'NONE', #50565 ) ;
#51679=AXIS2_PLACEMENT_3D ( 'NONE', #63539, #31863, #48100 ) ;
#51692=ORIENTED_EDGE ( 'NONE', *, *, #27283, .F. ) ;
#51705=ADVANCED_FACE ( 'NONE', ( #17860 ), #17929, .T. ) ;
#51709=PLANE ( 'NONE',  #64450 ) ;
#51712=VERTEX_POINT ( 'NONE', #39685 ) ;
#51717=CARTESIAN_POINT ( 'NONE',  ( 57.24999999999999289, 27.74999999999998934, -4.000000000000000000 ) ) ;
#51729=VERTEX_POINT ( 'NONE', #14307 ) ;
#51734=VECTOR ( 'NONE', #68833, 1000.000000000000000 ) ;
#51758=AXIS2_PLACEMENT_3D ( 'NONE', #62127, #35421, #46351 ) ;
#51764=CARTESIAN_POINT ( 'NONE',  ( 25.75000000000001066, 21.74999999999998224, -3.750000000000000000 ) ) ;
#51773=FACE_OUTER_BOUND ( 'NONE', #54740, .T. ) ;
#51778=EDGE_LOOP ( 'NONE', ( #40467, #36975, #51212, #65832 ) ) ;
#51795=DIRECTION ( 'NONE',  ( 1.000000000000000000, 2.312964634635740689E-15, -0.000000000000000000 ) ) ;
#51828=VERTEX_POINT ( 'NONE', #54013 ) ;
#51836=CARTESIAN_POINT ( 'NONE',  ( 17.00000000000000711, 24.74999999999997868, -3.750000000000000000 ) ) ;
#51846=AXIS2_PLACEMENT_3D ( 'NONE', #62051, #34633, #67346 ) ;
#51862=ORIENTED_EDGE ( 'NONE', *, *, #55440, .T. ) ;
#51871=ADVANCED_FACE ( 'NONE', ( #64590 ), #5602, .T. ) ;
#51876=EDGE_CURVE ( 'NONE', #43779, #1034, #5128, .T. ) ;
#51880=DIRECTION ( 'NONE',  ( 1.000000000000000000, 7.709882115452468306E-16, -0.000000000000000000 ) ) ;
#51886=LINE ( 'NONE', #41696, #47795 ) ;
#51888=ORIENTED_EDGE ( 'NONE', *, *, #24038, .F. ) ;
#51915=LINE ( 'NONE', #3673, #23510 ) ;
#51917=EDGE_LOOP ( 'NONE', ( #36912, #53522, #61300 ) ) ;
#51920=DIRECTION ( 'NONE',  ( -0.000000000000000000, 0.000000000000000000, -1.000000000000000000 ) ) ;
#51928=DIRECTION ( 'NONE',  ( 0.000000000000000000, -1.000000000000000000, 0.000000000000000000 ) ) ;
#51932=CARTESIAN_POINT ( 'NONE',  ( 1.000000000000000000, 36.99999999999999289, -3.750000000000000000 ) ) ;
#51951=EDGE_CURVE ( 'NONE', #29039, #51526, #57288, .T. ) ;
#51957=DIRECTION ( 'NONE',  ( 0.000000000000000000, -0.000000000000000000, 1.000000000000000000 ) ) ;
#51964=CARTESIAN_POINT ( 'NONE',  ( 26.25000000000001066, 19.24999999999997868, -3.750000000000000000 ) ) ;
#51968=VERTEX_POINT ( 'NONE', #32548 ) ;
#51990=CIRCLE ( 'NONE', #30622, 1.000000000000000000 ) ;
#52000=ORIENTED_EDGE ( 'NONE', *, *, #13785, .F. ) ;
#52015=CARTESIAN_POINT ( 'NONE',  ( 30.50000000000001066, 16.24999999999997513, 3.750000000000000000 ) ) ;
#52019=DIRECTION ( 'NONE',  ( 1.000000000000000000, 0.000000000000000000, -0.000000000000000000 ) ) ;
#52025=AXIS2_PLACEMENT_3D ( 'NONE', #50248, #28051, #603 ) ;
#52050=DIRECTION ( 'NONE',  ( 1.000000000000000000, 0.000000000000000000, 0.000000000000000000 ) ) ;
#52078=DIRECTION ( 'NONE',  ( 0.000000000000000000, 0.000000000000000000, -1.000000000000000000 ) ) ;
#52091=DIRECTION ( 'NONE',  ( 0.000000000000000000, 0.000000000000000000, 1.000000000000000000 ) ) ;
#52123=EDGE_CURVE ( 'NONE', #24250, #64166, #44970, .T. ) ;
#52126=CARTESIAN_POINT ( 'NONE',  ( 21.25000000000001066, 24.74999999999998224, -3.750000000000000000 ) ) ;
#52130=ADVANCED_FACE ( 'NONE', ( #11454 ), #22361, .F. ) ;
#52147=DIRECTION ( 'NONE',  ( -0.000000000000000000, 0.000000000000000000, -1.000000000000000000 ) ) ;
#52149=EDGE_CURVE ( 'NONE', #61605, #14417, #23740, .T. ) ;
#52154=AXIS2_PLACEMENT_3D ( 'NONE', #15161, #20032, #58372 ) ;
#52155=VERTEX_POINT ( 'NONE', #44210 ) ;
#52158=AXIS2_PLACEMENT_3D ( 'NONE', #68423, #53623, #20220 ) ;
#52166=ORIENTED_EDGE ( 'NONE', *, *, #46983, .T. ) ;
#52180=ORIENTED_EDGE ( 'NONE', *, *, #5307, .F. ) ;
#52182=SURFACE_SIDE_STYLE ('',( #26773 ) ) ;
#52192=( NAMED_UNIT ( * ) SI_UNIT ( $, .STERADIAN. ) SOLID_ANGLE_UNIT ( ) );
#52196=ORIENTED_EDGE ( 'NONE', *, *, #9246, .F. ) ;
#52203=DIRECTION ( 'NONE',  ( -1.000000000000000000, 0.000000000000000000, 0.000000000000000000 ) ) ;
#52205=CARTESIAN_POINT ( 'NONE',  ( 12.25000000000000533, 28.24999999999998224, -4.000000000000000000 ) ) ;
#52213=DIRECTION ( 'NONE',  ( 0.000000000000000000, 0.000000000000000000, -1.000000000000000000 ) ) ;
#52227=EDGE_LOOP ( 'NONE', ( #60097, #13890, #36073, #52196 ) ) ;
#52232=AXIS2_PLACEMENT_3D ( 'NONE', #8283, #36054, #52249 ) ;
#52243=CIRCLE ( 'NONE', #62355, 0.2500000000000002220 ) ;
#52247=ORIENTED_EDGE ( 'NONE', *, *, #67147, .T. ) ;
#52249=DIRECTION ( 'NONE',  ( 0.000000000000000000, -1.000000000000000000, 0.000000000000000000 ) ) ;
#52298=FACE_OUTER_BOUND ( 'NONE', #24414, .T. ) ;
#52310=EDGE_CURVE ( 'NONE', #6197, #33800, #38304, .T. ) ;
#52326=CIRCLE ( 'NONE', #55662, 0.2500000000000002220 ) ;
#52349=CARTESIAN_POINT ( 'NONE',  ( 21.50000000000000711, 21.99999999999998224, 3.750000000000000000 ) ) ;
#52376=CARTESIAN_POINT ( 'NONE',  ( 57.24999999999999289, 28.24999999999998934, -3.750000000000000000 ) ) ;
#52382=CARTESIAN_POINT ( 'NONE',  ( 69.99999999999998579, 37.00000000000000000, 3.750000000000000000 ) ) ;
#52388=CIRCLE ( 'NONE', #36649, 0.2500000000000002220 ) ;
#52418=ORIENTED_EDGE ( 'NONE', *, *, #10508, .T. ) ;
#52446=DIRECTION ( 'NONE',  ( -1.000000000000000000, 0.000000000000000000, 0.000000000000000000 ) ) ;
#52451=ORIENTED_EDGE ( 'NONE', *, *, #33898, .T. ) ;
#52472=VECTOR ( 'NONE', #55626, 1000.000000000000000 ) ;
#52474=EDGE_CURVE ( 'NONE', #37003, #66069, #38510, .T. ) ;
#52476=DIRECTION ( 'NONE',  ( 1.000000000000000000, -0.000000000000000000, 0.000000000000000000 ) ) ;
#52482=DIRECTION ( 'NONE',  ( -1.000000000000000000, 0.000000000000000000, 0.000000000000000000 ) ) ;
#52484=CARTESIAN_POINT ( 'NONE',  ( 66.24999999999998579, 33.74999999999999289, 3.750000000000000000 ) ) ;
#52492=CIRCLE ( 'NONE', #33994, 0.2500000000000002220 ) ;
#52495=FACE_OUTER_BOUND ( 'NONE', #57319, .T. ) ;
#52512=ORIENTED_EDGE ( 'NONE', *, *, #45166, .F. ) ;
#52526=CARTESIAN_POINT ( 'NONE',  ( 3.499999999999999112, 33.74999999999998579, -3.750000000000000000 ) ) ;
#52533=CYLINDRICAL_SURFACE ( 'NONE', #40660, 0.2500000000000002220 ) ;
#52541=CARTESIAN_POINT ( 'NONE',  ( 48.74999999999999289, 24.74999999999998579, -4.000000000000000000 ) ) ;
#52561=CARTESIAN_POINT ( 'NONE',  ( 48.25000000000000000, 21.99999999999998579, -4.000000000000000000 ) ) ;
#52582=CARTESIAN_POINT ( 'NONE',  ( 21.50000000000000711, 22.24999999999998224, -4.000000000000000000 ) ) ;
#52587=DIRECTION ( 'NONE',  ( 0.000000000000000000, 1.000000000000000000, -0.000000000000000000 ) ) ;
#52613=DIRECTION ( 'NONE',  ( -1.000000000000000000, 0.000000000000000000, 0.000000000000000000 ) ) ;
#52634=PLANE ( 'NONE',  #54866 ) ;
#52652=DIRECTION ( 'NONE',  ( 0.000000000000000000, 0.000000000000000000, -1.000000000000000000 ) ) ;
#52666=EDGE_LOOP ( 'NONE', ( #30603, #7371, #10714, #62012 ) ) ;
#52674=ADVANCED_FACE ( 'NONE', ( #25723 ), #68665, .T. ) ;
#52684=DIRECTION ( 'NONE',  ( -1.000000000000000000, 0.000000000000000000, 0.000000000000000000 ) ) ;
#52719=AXIS2_PLACEMENT_3D ( 'NONE', #12374, #12038, #7120 ) ;
#52731=AXIS2_PLACEMENT_3D ( 'NONE', #63496, #63824, #36802 ) ;
#52737=( NAMED_UNIT ( * ) SI_UNIT ( $, .STERADIAN. ) SOLID_ANGLE_UNIT ( ) );
#52751=AXIS2_PLACEMENT_3D ( 'NONE', #39674, #45988, #61095 ) ;
#52785=AXIS2_PLACEMENT_3D ( 'NONE', #18348, #67212, #18999 ) ;
#52800=ORIENTED_EDGE ( 'NONE', *, *, #68319, .T. ) ;
#52808=CARTESIAN_POINT ( 'NONE',  ( 30.25000000000000711, 18.74999999999997868, -3.750000000000000000 ) ) ;
#52809=CIRCLE ( 'NONE', #32526, 0.2500000000000002220 ) ;
#52811=DIRECTION ( 'NONE',  ( 0.000000000000000000, 0.000000000000000000, 1.000000000000000000 ) ) ;
#52817=DIRECTION ( 'NONE',  ( -1.000000000000000000, 0.000000000000000000, 0.000000000000000000 ) ) ;
#52826=AXIS2_PLACEMENT_3D ( 'NONE', #22180, #64747, #10593 ) ;
#52836=AXIS2_PLACEMENT_3D ( 'NONE', #33775, #68983, #31309 ) ;
#52841=CYLINDRICAL_SURFACE ( 'NONE', #43172, 0.2500000000000002220 ) ;
#52850=LINE ( 'NONE', #4980, #14450 ) ;
#52863=ORIENTED_EDGE ( 'NONE', *, *, #35742, .F. ) ;
#52867=DIRECTION ( 'NONE',  ( -0.000000000000000000, -0.000000000000000000, -1.000000000000000000 ) ) ;
#52876=DIRECTION ( 'NONE',  ( -1.000000000000000000, 0.000000000000000000, 0.000000000000000000 ) ) ;
#52881=ORIENTED_EDGE ( 'NONE', *, *, #51136, .T. ) ;
#52886=DIRECTION ( 'NONE',  ( 0.000000000000000000, 0.000000000000000000, -1.000000000000000000 ) ) ;
#52914=CARTESIAN_POINT ( 'NONE',  ( 39.24999999999999289, 15.99999999999997691, -3.750000000000000000 ) ) ;
#52946=ORIENTED_EDGE ( 'NONE', *, *, #42157, .F. ) ;
#52947=DIRECTION ( 'NONE',  ( 0.000000000000000000, 0.000000000000000000, 1.000000000000000000 ) ) ;
#52949=ORIENTED_EDGE ( 'NONE', *, *, #436, .T. ) ;
#52959=DIRECTION ( 'NONE',  ( -1.000000000000000000, 0.000000000000000000, 0.000000000000000000 ) ) ;
#52965=VECTOR ( 'NONE', #18498, 1000.000000000000000 ) ;
#52969=DIRECTION ( 'NONE',  ( -1.000000000000000000, 1.156482317317866203E-15, 0.000000000000000000 ) ) ;
#52979=DIRECTION ( 'NONE',  ( 0.000000000000000000, 0.000000000000000000, 1.000000000000000000 ) ) ;
#52980=EDGE_CURVE ( 'NONE', #31555, #28627, #54694, .T. ) ;
#53014=DIRECTION ( 'NONE',  ( 0.000000000000000000, -0.000000000000000000, 1.000000000000000000 ) ) ;
#53019=EDGE_LOOP ( 'NONE', ( #51862, #38177 ) ) ;
#53045=LINE ( 'NONE', #69225, #55084 ) ;
#53079=CARTESIAN_POINT ( 'NONE',  ( 57.74999999999998579, 30.99999999999999289, -3.750000000000000000 ) ) ;
#53083=EDGE_LOOP ( 'NONE', ( #44346, #65217, #52863, #58192 ) ) ;
#53107=CARTESIAN_POINT ( 'NONE',  ( 59.00000000000000000, 11.99999999999999822, -3.499999999999999556 ) ) ;
#53110=CIRCLE ( 'NONE', #41949, 0.9999999999999997780 ) ;
#53122=FACE_OUTER_BOUND ( 'NONE', #50433, .T. ) ;
#53127=AXIS2_PLACEMENT_3D ( 'NONE', #64698, #64340, #26349 ) ;
#53129=ORIENTED_EDGE ( 'NONE', *, *, #17662, .F. ) ;
#53148=ADVANCED_FACE ( 'NONE', ( #34986 ), #19132, .F. ) ;
#53151=ORIENTED_EDGE ( 'NONE', *, *, #37464, .T. ) ;
#53191=ORIENTED_EDGE ( 'NONE', *, *, #66881, .T. ) ;
#53238=EDGE_CURVE ( 'NONE', #31454, #27359, #14944, .T. ) ;
#53245=CARTESIAN_POINT ( 'NONE',  ( 1.000000000000000888, 1.224646799147365780E-16, 4.000000000000000000 ) ) ;
#53247=AXIS2_PLACEMENT_3D ( 'NONE', #35774, #42148, #46006 ) ;
#53251=ADVANCED_FACE ( 'NONE', ( #58181 ), #46977, .T. ) ;
#53291=DIRECTION ( 'NONE',  ( -0.000000000000000000, -0.000000000000000000, 1.000000000000000000 ) ) ;
#53326=DIRECTION ( 'NONE',  ( 0.000000000000000000, 0.000000000000000000, -1.000000000000000000 ) ) ;
#53347=CARTESIAN_POINT ( 'NONE',  ( 0.000000000000000000, 33.74999999999999289, 3.750000000000000000 ) ) ;
#53354=ORIENTED_EDGE ( 'NONE', *, *, #65439, .T. ) ;
#53355=AXIS2_PLACEMENT_3D ( 'NONE', #61512, #66113, #7035 ) ;
#53356=CARTESIAN_POINT ( 'NONE',  ( 7.399999999999989697, 11.99999999999999289, -4.000000000000000000 ) ) ;
#53370=CARTESIAN_POINT ( 'NONE',  ( 66.24999999999998579, 33.74999999999999289, -4.000000000000000000 ) ) ;
#53373=AXIS2_PLACEMENT_3D ( 'NONE', #57779, #40927, #45845 ) ;
#53374=DIRECTION ( 'NONE',  ( 0.000000000000000000, 1.000000000000000000, 0.000000000000000000 ) ) ;
#53385=ORIENTED_EDGE ( 'NONE', *, *, #15302, .F. ) ;
#53397=ORIENTED_EDGE ( 'NONE', *, *, #67033, .T. ) ;
#53423=ADVANCED_FACE ( 'NONE', ( #49360 ), #58498, .T. ) ;
#53440=CARTESIAN_POINT ( 'NONE',  ( 69.74999999999998579, 36.75000000000000000, 4.000000000000000000 ) ) ;
#53462=VECTOR ( 'NONE', #20025, 1000.000000000000000 ) ;
#53479=CARTESIAN_POINT ( 'NONE',  ( 48.25000000000000000, 22.24999999999998579, 3.750000000000000000 ) ) ;
#53480=ORIENTED_EDGE ( 'NONE', *, *, #25650, .T. ) ;
#53488=CYLINDRICAL_SURFACE ( 'NONE', #15003, 0.2500000000000002220 ) ;
#53490=DIRECTION ( 'NONE',  ( 0.000000000000000000, 0.000000000000000000, -1.000000000000000000 ) ) ;
#53515=EDGE_LOOP ( 'NONE', ( #58788, #25832, #2297, #64073 ) ) ;
#53522=ORIENTED_EDGE ( 'NONE', *, *, #59076, .T. ) ;
#53545=STYLED_ITEM ( 'NONE', ( #33375 ), #2964 ) ;
#53601=SPHERICAL_SURFACE ( 'NONE', #27974, 1.000000000000000000 ) ;
#53609=CARTESIAN_POINT ( 'NONE',  ( 12.25000000000000355, 30.99999999999998579, -3.750000000000000000 ) ) ;
#53621=ORIENTED_EDGE ( 'NONE', *, *, #58396, .F. ) ;
#53622=DIRECTION ( 'NONE',  ( 0.000000000000000000, 0.000000000000000000, 1.000000000000000000 ) ) ;
#53623=DIRECTION ( 'NONE',  ( -0.000000000000000000, 0.000000000000000000, -1.000000000000000000 ) ) ;
#53628=AXIS2_PLACEMENT_3D ( 'NONE', #52376, #10137, #25594 ) ;
#53631=ORIENTED_EDGE ( 'NONE', *, *, #18451, .F. ) ;
#53636=LINE ( 'NONE', #49094, #31117 ) ;
#53647=DIRECTION ( 'NONE',  ( 0.000000000000000000, 0.000000000000000000, -1.000000000000000000 ) ) ;
#53666=CIRCLE ( 'NONE', #17741, 0.5000000000000004441 ) ;
#53680=VECTOR ( 'NONE', #11704, 1000.000000000000000 ) ;
#53687=ORIENTED_EDGE ( 'NONE', *, *, #67691, .T. ) ;
#53708=CARTESIAN_POINT ( 'NONE',  ( -2.139492287038055877E-14, 27.74999999999994316, 4.000000000000000000 ) ) ;
#53709=SPHERICAL_SURFACE ( 'NONE', #25027, 0.2500000000000000000 ) ;
#53717=LINE ( 'NONE', #65321, #59020 ) ;
#53720=ORIENTED_EDGE ( 'NONE', *, *, #30059, .T. ) ;
#53726=ORIENTED_EDGE ( 'NONE', *, *, #41649, .F. ) ;
#53733=DIRECTION ( 'NONE',  ( 0.000000000000000000, 0.000000000000000000, -1.000000000000000000 ) ) ;
#53749=ADVANCED_FACE ( 'NONE', ( #60073 ), #40044, .F. ) ;
#53780=CARTESIAN_POINT ( 'NONE',  ( 39.24999999999999289, 16.24999999999997513, 3.750000000000000000 ) ) ;
#53785=ADVANCED_FACE ( 'NONE', ( #33684 ), #6955, .T. ) ;
#53836=AXIS2_PLACEMENT_3D ( 'NONE', #33079, #27418, #5980 ) ;
#53844=PLANE ( 'NONE',  #56111 ) ;
#53853=ORIENTED_EDGE ( 'NONE', *, *, #39642, .F. ) ;
#53857=AXIS2_PLACEMENT_3D ( 'NONE', #11082, #21287, #37543 ) ;
#53869=DIRECTION ( 'NONE',  ( -0.000000000000000000, -0.000000000000000000, 1.000000000000000000 ) ) ;
#53891=ORIENTED_EDGE ( 'NONE', *, *, #16794, .F. ) ;
#53898=ORIENTED_EDGE ( 'NONE', *, *, #35035, .F. ) ;
#53899=DIRECTION ( 'NONE',  ( -1.000000000000000000, 0.000000000000000000, 0.000000000000000000 ) ) ;
#53934=FACE_OUTER_BOUND ( 'NONE', #25102, .T. ) ;
#53960=VECTOR ( 'NONE', #11721, 1000.000000000000000 ) ;
#53968=ORIENTED_EDGE ( 'NONE', *, *, #30799, .F. ) ;
#53988=CARTESIAN_POINT ( 'NONE',  ( 53.24999999999999289, 27.74999999999998579, -3.750000000000000000 ) ) ;
#54013=CARTESIAN_POINT ( 'NONE',  ( 26.00000000000001066, 21.74999999999998224, -3.750000000000000000 ) ) ;
#54022=CIRCLE ( 'NONE', #9114, 0.2500000000000002220 ) ;
#54052=LINE ( 'NONE', #43222, #43679 ) ;
#54057=VECTOR ( 'NONE', #34308, 1000.000000000000000 ) ;
#54078=DIRECTION ( 'NONE',  ( 1.000000000000000000, 0.000000000000000000, 0.000000000000000000 ) ) ;
#54087=ADVANCED_FACE ( 'NONE', ( #48447 ), #138, .T. ) ;
#54088=DIRECTION ( 'NONE',  ( -1.000000000000000000, 0.000000000000000000, 0.000000000000000000 ) ) ;
#54091=VERTEX_POINT ( 'NONE', #6181 ) ;
#54113=EDGE_LOOP ( 'NONE', ( #37577, #50657, #32579, #26258 ) ) ;
#54114=CARTESIAN_POINT ( 'NONE',  ( 39.74999999999999289, 18.99999999999997868, -3.750000000000000000 ) ) ;
#54116=ORIENTED_EDGE ( 'NONE', *, *, #15823, .F. ) ;
#54119=EDGE_LOOP ( 'NONE', ( #44337, #17153, #8993, #67439 ) ) ;
#54140=STYLED_ITEM ( 'NONE', ( #16292 ), #46002 ) ;
#54141=ADVANCED_FACE ( 'NONE', ( #6505 ), #1544, .T. ) ;
#54148=ORIENTED_EDGE ( 'NONE', *, *, #36974, .T. ) ;
#54151=EDGE_CURVE ( 'NONE', #17986, #25904, #65960, .T. ) ;
#54158=CARTESIAN_POINT ( 'NONE',  ( 0.000000000000000000, 36.74999999999999289, 3.000000000000000000 ) ) ;
#54170=EDGE_CURVE ( 'NONE', #22828, #65411, #39495, .T. ) ;
#54191=CARTESIAN_POINT ( 'NONE',  ( 3.749999999999999556, 34.24999999999998579, 4.000000000000000000 ) ) ;
#54192=AXIS2_PLACEMENT_3D ( 'NONE', #58059, #25333, #30949 ) ;
#54199=ORIENTED_EDGE ( 'NONE', *, *, #13589, .F. ) ;
#54201=EDGE_LOOP ( 'NONE', ( #2446, #63781, #46598, #963 ) ) ;
#54208=DIRECTION ( 'NONE',  ( 0.000000000000000000, 0.000000000000000000, -1.000000000000000000 ) ) ;
#54211=CIRCLE ( 'NONE', #30607, 0.2500000000000002220 ) ;
#54220=AXIS2_PLACEMENT_3D ( 'NONE', #69205, #64253, #52684 ) ;
#54248=DIRECTION ( 'NONE',  ( 1.000000000000000000, -0.000000000000000000, -0.000000000000000000 ) ) ;
#54250=ADVANCED_FACE ( 'NONE', ( #19500 ), #61697, .T. ) ;
#54256=DIRECTION ( 'NONE',  ( 0.000000000000000000, 0.000000000000000000, -1.000000000000000000 ) ) ;
#54269=ORIENTED_EDGE ( 'NONE', *, *, #32812, .T. ) ;
#54284=( LENGTH_UNIT ( ) NAMED_UNIT ( * ) SI_UNIT ( .MILLI., .METRE. ) );
#54310=FACE_OUTER_BOUND ( 'NONE', #47119, .T. ) ;
#54311=ORIENTED_EDGE ( 'NONE', *, *, #21138, .T. ) ;
#54313=TOROIDAL_SURFACE ( 'NONE', #11644, 0.5000000000000000000, 0.2500000000000000000 ) ;
#54351=LINE ( 'NONE', #43845, #26414 ) ;
#54362=DIRECTION ( 'NONE',  ( 0.000000000000000000, 0.000000000000000000, -1.000000000000000000 ) ) ;
#54375=EDGE_LOOP ( 'NONE', ( #43047, #40674, #28045, #590 ) ) ;
#54394=CIRCLE ( 'NONE', #3812, 0.5000000000000000000 ) ;
#54400=CARTESIAN_POINT ( 'NONE',  ( 8.250000000000001776, 30.74999999999998579, 4.000000000000000000 ) ) ;
#54408=EDGE_CURVE ( 'NONE', #37329, #17336, #57334, .T. ) ;
#54412=VECTOR ( 'NONE', #44736, 1000.000000000000000 ) ;
#54416=DIRECTION ( 'NONE',  ( 0.000000000000000000, -1.000000000000000000, 0.000000000000000000 ) ) ;
#54420=ORIENTED_EDGE ( 'NONE', *, *, #20970, .F. ) ;
#54422=CIRCLE ( 'NONE', #34206, 0.2500000000000002220 ) ;
#54432=TOROIDAL_SURFACE ( 'NONE', #10670, 0.5000000000000000000, 0.2500000000000000000 ) ;
#54434=DIRECTION ( 'NONE',  ( 0.000000000000000000, 0.000000000000000000, -1.000000000000000000 ) ) ;
#54436=ADVANCED_FACE ( 'NONE', ( #61231 ), #30584, .T. ) ;
#54443=COLOUR_RGB ( '', 0.09019608, 0.27058824, 0.51372549) ;
#54467=ORIENTED_EDGE ( 'NONE', *, *, #68101, .F. ) ;
#54480=VERTEX_POINT ( 'NONE', #47535 ) ;
#54481=EDGE_CURVE ( 'NONE', #24854, #4102, #10354, .T. ) ;
#54504=DIRECTION ( 'NONE',  ( -0.000000000000000000, -0.000000000000000000, -1.000000000000000000 ) ) ;
#54509=CARTESIAN_POINT ( 'NONE',  ( 57.74999999999998579, 30.74999999999999289, -3.750000000000000000 ) ) ;
#54510=CIRCLE ( 'NONE', #44476, 1.000000000000000000 ) ;
#54517=DIRECTION ( 'NONE',  ( -0.000000000000000000, -0.000000000000000000, 1.000000000000000000 ) ) ;
#54528=AXIS2_PLACEMENT_3D ( 'NONE', #38986, #33654, #61077 ) ;
#54539=CARTESIAN_POINT ( 'NONE',  ( 39.24999999999999289, 15.74999999999997513, -4.000000000000000000 ) ) ;
#54553=ORIENTED_EDGE ( 'NONE', *, *, #16502, .F. ) ;
#54559=EDGE_LOOP ( 'NONE', ( #3233, #38849, #13377, #46489 ) ) ;
#54572=CARTESIAN_POINT ( 'NONE',  ( 26.25000000000001066, 19.24999999999997868, 4.000000000000000000 ) ) ;
#54585=CARTESIAN_POINT ( 'NONE',  ( 53.25000000000000000, 25.24999999999998579, 4.000000000000000000 ) ) ;
#54602=VECTOR ( 'NONE', #28760, 1000.000000000000000 ) ;
#54607=LINE ( 'NONE', #65158, #15563 ) ;
#54624=LINE ( 'NONE', #10089, #16256 ) ;
#54635=CARTESIAN_POINT ( 'NONE',  ( 12.50000000000000355, 30.74999999999998579, -3.750000000000000000 ) ) ;
#54645=AXIS2_PLACEMENT_3D ( 'NONE', #11120, #64610, #22733 ) ;
#54669=DIRECTION ( 'NONE',  ( 5.782411586589351722E-16, -1.000000000000000000, -0.000000000000000000 ) ) ;
#54685=ORIENTED_EDGE ( 'NONE', *, *, #1773, .F. ) ;
#54694=LINE ( 'NONE', #2205, #55218 ) ;
#54710=ORIENTED_EDGE ( 'NONE', *, *, #33793, .F. ) ;
#54711=ORIENTED_EDGE ( 'NONE', *, *, #11599, .F. ) ;
#54740=EDGE_LOOP ( 'NONE', ( #59664, #10230, #60375, #10483 ) ) ;
#54757=CIRCLE ( 'NONE', #5357, 0.2500000000000002220 ) ;
#54775=EDGE_CURVE ( 'NONE', #6066, #67943, #57438, .T. ) ;
#54790=DIRECTION ( 'NONE',  ( -1.000000000000000000, -2.168404344971006896E-16, 0.000000000000000000 ) ) ;
#54794=LINE ( 'NONE', #39026, #54602 ) ;
#54796=CARTESIAN_POINT ( 'NONE',  ( 62.24999999999998579, 33.74999999999999289, -3.750000000000000000 ) ) ;
#54825=EDGE_LOOP ( 'NONE', ( #40132, #8445, #69303 ) ) ;
#54827=ORIENTED_EDGE ( 'NONE', *, *, #14469, .F. ) ;
#54835=DIRECTION ( 'NONE',  ( -0.7071067811865447972, 8.659560562354899578E-17, 0.7071067811865502373 ) ) ;
#54842=LINE ( 'NONE', #52561, #58417 ) ;
#54852=FACE_OUTER_BOUND ( 'NONE', #41820, .T. ) ;
#54861=STYLED_ITEM ( 'NONE', ( #15950 ), #50950 ) ;
#54866=AXIS2_PLACEMENT_3D ( 'NONE', #8670, #68813, #30099 ) ;
#54868=DIRECTION ( 'NONE',  ( 1.000000000000000000, 0.000000000000000000, -0.000000000000000000 ) ) ;
#54880=LINE ( 'NONE', #60859, #65808 ) ;
#54926=EDGE_CURVE ( 'NONE', #25430, #26545, #64447, .T. ) ;
#54927=EDGE_CURVE ( 'NONE', #47340, #69646, #54211, .T. ) ;
#54943=ORIENTED_EDGE ( 'NONE', *, *, #50924, .F. ) ;
#54953=DIRECTION ( 'NONE',  ( 0.000000000000000000, 0.000000000000000000, -1.000000000000000000 ) ) ;
#54960=DIRECTION ( 'NONE',  ( 0.000000000000000000, 1.000000000000000000, -0.000000000000000000 ) ) ;
#54989=DIRECTION ( 'NONE',  ( 1.000000000000000000, 2.312964634635707951E-15, 0.000000000000000000 ) ) ;
#54995=CARTESIAN_POINT ( 'NONE',  ( 0.000000000000000000, 36.99999999999999289, 4.000000000000000000 ) ) ;
#55001=CARTESIAN_POINT ( 'NONE',  ( 39.49999999999999289, 16.24999999999997513, 4.000000000000000000 ) ) ;
#55007=ORIENTED_EDGE ( 'NONE', *, *, #3034, .F. ) ;
#55019=VECTOR ( 'NONE', #45493, 1000.000000000000000 ) ;
#55026=EDGE_CURVE ( 'NONE', #13223, #32655, #49315, .T. ) ;
#55027=LINE ( 'NONE', #6853, #19291 ) ;
#55050=CARTESIAN_POINT ( 'NONE',  ( 57.24999999999999289, 28.24999999999998934, 4.000000000000000000 ) ) ;
#55051=CIRCLE ( 'NONE', #52836, 0.2500000000000002220 ) ;
#55081=CARTESIAN_POINT ( 'NONE',  ( 26.00000000000001066, 21.74999999999998224, 3.750000000000000000 ) ) ;
#55084=VECTOR ( 'NONE', #48142, 1000.000000000000000 ) ;
#55116=CIRCLE ( 'NONE', #16949, 0.5000000000000000000 ) ;
#55121=DIRECTION ( 'NONE',  ( 0.000000000000000000, 1.000000000000000000, 0.000000000000000000 ) ) ;
#55156=VERTEX_POINT ( 'NONE', #57002 ) ;
#55196=LINE ( 'NONE', #7379, #3294 ) ;
#55200=CARTESIAN_POINT ( 'NONE',  ( 14.09999999999999609, 11.99999999999999289, 4.000000000000000000 ) ) ;
#55207=CYLINDRICAL_SURFACE ( 'NONE', #24090, 0.2500000000000000000 ) ;
#55218=VECTOR ( 'NONE', #17456, 1000.000000000000000 ) ;
#55246=CARTESIAN_POINT ( 'NONE',  ( 66.49999999999998579, 34.24999999999999289, -3.750000000000000000 ) ) ;
#55250=DIRECTION ( 'NONE',  ( 1.000000000000000000, 0.000000000000000000, 0.000000000000000000 ) ) ;
#55263=CARTESIAN_POINT ( 'NONE',  ( 12.50000000000000533, 27.74999999999998224, -3.750000000000000000 ) ) ;
#55269=EDGE_CURVE ( 'NONE', #59375, #42973, #38010, .T. ) ;
#55277=ORIENTED_EDGE ( 'NONE', *, *, #11779, .F. ) ;
#55299=DIRECTION ( 'NONE',  ( 1.000000000000000000, 0.000000000000000000, -0.000000000000000000 ) ) ;
#55301=VECTOR ( 'NONE', #41208, 1000.000000000000000 ) ;
#55304=ADVANCED_FACE ( 'NONE', ( #58739 ), #36337, .T. ) ;
#55305=CARTESIAN_POINT ( 'NONE',  ( 57.74999999999999289, 28.24999999999998934, -4.000000000000000000 ) ) ;
#55312=DIRECTION ( 'NONE',  ( -1.000000000000000000, 0.000000000000000000, 0.000000000000000000 ) ) ;
#55318=DIRECTION ( 'NONE',  ( -1.000000000000000000, -7.709882115452468306E-16, 0.000000000000000000 ) ) ;
#55323=ORIENTED_EDGE ( 'NONE', *, *, #30083, .T. ) ;
#55344=ORIENTED_EDGE ( 'NONE', *, *, #578, .F. ) ;
#55372=DIRECTION ( 'NONE',  ( 0.000000000000000000, 1.000000000000000000, -0.000000000000000000 ) ) ;
#55381=AXIS2_PLACEMENT_3D ( 'NONE', #18154, #66331, #38618 ) ;
#55405=DIRECTION ( 'NONE',  ( 0.000000000000000000, 1.000000000000000000, 0.000000000000000000 ) ) ;
#55409=DIRECTION ( 'NONE',  ( 0.000000000000000000, 1.000000000000000000, 0.000000000000000000 ) ) ;
#55416=LINE ( 'NONE', #64921, #64151 ) ;
#55440=EDGE_CURVE ( 'NONE', #11647, #18309, #49811, .T. ) ;
#55443=EDGE_LOOP ( 'NONE', ( #15081, #21256, #22029, #49237 ) ) ;
#55445=ORIENTED_EDGE ( 'NONE', *, *, #19047, .F. ) ;
#55469=ORIENTED_EDGE ( 'NONE', *, *, #59549, .F. ) ;
#55498=FACE_OUTER_BOUND ( 'NONE', #59930, .T. ) ;
#55505=EDGE_CURVE ( 'NONE', #40281, #37989, #59765, .T. ) ;
#55520=ORIENTED_EDGE ( 'NONE', *, *, #59076, .F. ) ;
#55526=DIRECTION ( 'NONE',  ( -1.000000000000000000, 0.000000000000000000, 0.000000000000000000 ) ) ;
#55527=EDGE_LOOP ( 'NONE', ( #50275, #42817, #56532, #23253 ) ) ;
#55539=SURFACE_STYLE_FILL_AREA ( #45377 ) ;
#55550=DIRECTION ( 'NONE',  ( -0.000000000000000000, 0.000000000000000000, -1.000000000000000000 ) ) ;
#55589=DIRECTION ( 'NONE',  ( 0.000000000000000000, -1.000000000000000000, 0.000000000000000000 ) ) ;
#55601=AXIS2_PLACEMENT_3D ( 'NONE', #62506, #24180, #40386 ) ;
#55603=EDGE_CURVE ( 'NONE', #62878, #36379, #3037, .T. ) ;
#55626=DIRECTION ( 'NONE',  ( 1.000000000000000000, -0.000000000000000000, -0.000000000000000000 ) ) ;
#55645=CYLINDRICAL_SURFACE ( 'NONE', #47185, 0.2500000000000002220 ) ;
#55654=AXIS2_PLACEMENT_3D ( 'NONE', #14356, #41835, #20330 ) ;
#55662=AXIS2_PLACEMENT_3D ( 'NONE', #60442, #49926, #55526 ) ;
#55687=FACE_OUTER_BOUND ( 'NONE', #63179, .T. ) ;
#55719=CARTESIAN_POINT ( 'NONE',  ( 0.000000000000000000, 36.75000000000000000, 3.750000000000000000 ) ) ;
#55742=CIRCLE ( 'NONE', #46814, 0.2500000000000002220 ) ;
#55766=CARTESIAN_POINT ( 'NONE',  ( 44.25000000000000000, 21.74999999999998579, 3.750000000000000000 ) ) ;
#55779=DIRECTION ( 'NONE',  ( 0.000000000000000000, 0.000000000000000000, 1.000000000000000000 ) ) ;
#55788=EDGE_LOOP ( 'NONE', ( #38365, #12177, #9225, #6547 ) ) ;
#55816=LINE ( 'NONE', #2278, #30477 ) ;
#55828=DIRECTION ( 'NONE',  ( -0.000000000000000000, 0.000000000000000000, -1.000000000000000000 ) ) ;
#55835=ADVANCED_FACE ( 'NONE', ( #61732 ), #62094, .T. ) ;
#55847=EDGE_LOOP ( 'NONE', ( #65889, #54148, #50720, #23167 ) ) ;
#55854=ORIENTED_EDGE ( 'NONE', *, *, #40681, .F. ) ;
#55856=FACE_OUTER_BOUND ( 'NONE', #10982, .T. ) ;
#55881=EDGE_CURVE ( 'NONE', #35167, #61482, #40680, .T. ) ;
#55888=VECTOR ( 'NONE', #52019, 1000.000000000000000 ) ;
#55894=FILL_AREA_STYLE ('',( #44698 ) ) ;
#55913=DIRECTION ( 'NONE',  ( -1.000000000000000000, 0.000000000000000000, 0.000000000000000000 ) ) ;
#55931=CARTESIAN_POINT ( 'NONE',  ( 3.749999999999999556, 34.24999999999998579, -3.750000000000000000 ) ) ;
#55936=ORIENTED_EDGE ( 'NONE', *, *, #48274, .T. ) ;
#55938=ORIENTED_EDGE ( 'NONE', *, *, #40204, .F. ) ;
#55941=VECTOR ( 'NONE', #12128, 1000.000000000000000 ) ;
#55942=CARTESIAN_POINT ( 'NONE',  ( 3.499999999999998668, 36.74999999999999289, 4.000000000000000000 ) ) ;
#55946=ORIENTED_EDGE ( 'NONE', *, *, #65751, .F. ) ;
#55961=CARTESIAN_POINT ( 'NONE',  ( 48.50000000000000000, 22.24999999999998579, -3.750000000000000000 ) ) ;
#55979=CIRCLE ( 'NONE', #12174, 1.000000000000000000 ) ;
#55984=( GEOMETRIC_REPRESENTATION_CONTEXT ( 3 ) GLOBAL_UNCERTAINTY_ASSIGNED_CONTEXT ( ( #20079 ) ) GLOBAL_UNIT_ASSIGNED_CONTEXT ( ( #41639, #41294, #52192 ) ) REPRESENTATION_CONTEXT ( 'NONE', 'WORKASPACE' ) );
#56005=CARTESIAN_POINT ( 'NONE',  ( 30.25000000000001066, 16.24999999999997513, 3.750000000000000000 ) ) ;
#56013=DIRECTION ( 'NONE',  ( 0.000000000000000000, 0.000000000000000000, 1.000000000000000000 ) ) ;
#56037=DIRECTION ( 'NONE',  ( 0.000000000000000000, 0.000000000000000000, -1.000000000000000000 ) ) ;
#56038=ORIENTED_EDGE ( 'NONE', *, *, #67361, .T. ) ;
#56050=FACE_OUTER_BOUND ( 'NONE', #61711, .T. ) ;
#56097=CARTESIAN_POINT ( 'NONE',  ( 12.25000000000000355, 30.74999999999998579, -3.750000000000000000 ) ) ;
#56099=DIRECTION ( 'NONE',  ( 0.000000000000000000, 0.000000000000000000, -1.000000000000000000 ) ) ;
#56105=DIRECTION ( 'NONE',  ( 0.000000000000000000, 0.000000000000000000, -1.000000000000000000 ) ) ;
#56106=AXIS2_PLACEMENT_3D ( 'NONE', #20520, #36017, #57817 ) ;
#56107=ORIENTED_EDGE ( 'NONE', *, *, #39425, .T. ) ;
#56111=AXIS2_PLACEMENT_3D ( 'NONE', #7049, #32739, #23237 ) ;
#56113=VECTOR ( 'NONE', #28912, 1000.000000000000000 ) ;
#56117=DIRECTION ( 'NONE',  ( -2.312964634635740689E-15, 1.000000000000000000, -0.000000000000000000 ) ) ;
#56118=VERTEX_POINT ( 'NONE', #49758 ) ;
#56129=CIRCLE ( 'NONE', #34797, 0.2500000000000002220 ) ;
#56185=ORIENTED_EDGE ( 'NONE', *, *, #57235, .F. ) ;
#56193=TOROIDAL_SURFACE ( 'NONE', #69670, 0.5000000000000000000, 0.2500000000000000000 ) ;
#56197=CARTESIAN_POINT ( 'NONE',  ( 12.75000000000000533, 27.99999999999998224, -3.750000000000000000 ) ) ;
#56215=SURFACE_SIDE_STYLE ('',( #55539 ) ) ;
#56216=VECTOR ( 'NONE', #67784, 1000.000000000000000 ) ;
#56233=FACE_OUTER_BOUND ( 'NONE', #11969, .T. ) ;
#56241=MECHANICAL_DESIGN_GEOMETRIC_PRESENTATION_REPRESENTATION('',(#18095),#31529);
#56260=AXIS2_PLACEMENT_3D ( 'NONE', #17636, #28481, #49988 ) ;
#56269=CARTESIAN_POINT ( 'NONE',  ( 8.250000000000001776, 31.24999999999998579, 3.750000000000000000 ) ) ;
#56282=FACE_OUTER_BOUND ( 'NONE', #67123, .T. ) ;
#56286=DIRECTION ( 'NONE',  ( 0.000000000000000000, 0.000000000000000000, -1.000000000000000000 ) ) ;
#56314=DIRECTION ( 'NONE',  ( 1.000000000000000000, 0.000000000000000000, 0.000000000000000000 ) ) ;
#56334=CIRCLE ( 'NONE', #51846, 0.2500000000000002220 ) ;
#56343=VERTEX_POINT ( 'NONE', #5741 ) ;
#56369=CARTESIAN_POINT ( 'NONE',  ( 66.24999999999998579, 34.24999999999999289, 4.000000000000000000 ) ) ;
#56390=ORIENTED_EDGE ( 'NONE', *, *, #47455, .F. ) ;
#56394=ORIENTED_EDGE ( 'NONE', *, *, #39425, .F. ) ;
#56411=CONICAL_SURFACE ( 'NONE', #45256, 3.100000000000000533, 0.7853981633974447263 ) ;
#56416=FACE_OUTER_BOUND ( 'NONE', #10292, .T. ) ;
#56422=CARTESIAN_POINT ( 'NONE',  ( 53.00000000000000000, 24.74999999999998224, -3.750000000000000000 ) ) ;
#56426=DIRECTION ( 'NONE',  ( 1.000000000000000000, 2.312964634635707951E-15, 0.000000000000000000 ) ) ;
#56429=SURFACE_STYLE_FILL_AREA ( #34980 ) ;
#56436=ORIENTED_EDGE ( 'NONE', *, *, #36067, .T. ) ;
#56514=DIRECTION ( 'NONE',  ( -1.000000000000000000, 0.000000000000000000, 0.000000000000000000 ) ) ;
#56528=ADVANCED_FACE ( 'NONE', ( #36357 ), #24351, .T. ) ;
#56529=LINE ( 'NONE', #7323, #49661 ) ;
#56532=ORIENTED_EDGE ( 'NONE', *, *, #15385, .T. ) ;
#56559=CARTESIAN_POINT ( 'NONE',  ( 44.25000000000000000, 21.74999999999998579, -4.000000000000000000 ) ) ;
#56561=DIRECTION ( 'NONE',  ( 0.000000000000000000, -0.000000000000000000, 1.000000000000000000 ) ) ;
#56562=FACE_OUTER_BOUND ( 'NONE', #40387, .T. ) ;
#56582=CIRCLE ( 'NONE', #21741, 0.2500000000000002220 ) ;
#56620=DIRECTION ( 'NONE',  ( 0.000000000000000000, 0.000000000000000000, -1.000000000000000000 ) ) ;
#56627=CYLINDRICAL_SURFACE ( 'NONE', #10635, 0.2500000000000002220 ) ;
#56648=AXIS2_PLACEMENT_3D ( 'NONE', #18099, #60308, #1513 ) ;
#56652=EDGE_CURVE ( 'NONE', #51660, #21355, #58459, .T. ) ;
#56653=LINE ( 'NONE', #9859, #21796 ) ;
#56660=CARTESIAN_POINT ( 'NONE',  ( 7.750000000000019540, 4.481368979606759023E-15, 4.000000000000000000 ) ) ;
#56666=AXIS2_PLACEMENT_3D ( 'NONE', #44908, #34320, #61379 ) ;
#56668=DIRECTION ( 'NONE',  ( 0.000000000000000000, 0.000000000000000000, -1.000000000000000000 ) ) ;
#56717=CIRCLE ( 'NONE', #3913, 0.7499999999999997780 ) ;
#56733=ADVANCED_FACE ( 'NONE', ( #43705 ), #26086, .T. ) ;
#56780=CARTESIAN_POINT ( 'NONE',  ( 8.250000000000001776, 30.74999999999998579, -4.000000000000000000 ) ) ;
#56783=CIRCLE ( 'NONE', #60139, 0.2500000000000002220 ) ;
#56795=EDGE_CURVE ( 'NONE', #1034, #10730, #54510, .T. ) ;
#56812=DIRECTION ( 'NONE',  ( -1.000000000000000000, 0.000000000000000000, 0.000000000000000000 ) ) ;
#56820=ORIENTED_EDGE ( 'NONE', *, *, #22876, .T. ) ;
#56853=EDGE_LOOP ( 'NONE', ( #12419, #41558, #68622, #53191 ) ) ;
#56897=ORIENTED_EDGE ( 'NONE', *, *, #67686, .F. ) ;
#56938=EDGE_CURVE ( 'NONE', #835, #28382, #67192, .T. ) ;
#56961=ORIENTED_EDGE ( 'NONE', *, *, #65044, .T. ) ;
#56979=CARTESIAN_POINT ( 'NONE',  ( 17.25000000000000711, 25.24999999999998224, -3.750000000000000000 ) ) ;
#56982=FACE_OUTER_BOUND ( 'NONE', #16190, .T. ) ;
#56985=DIRECTION ( 'NONE',  ( -0.000000000000000000, -0.000000000000000000, 1.000000000000000000 ) ) ;
#57002=CARTESIAN_POINT ( 'NONE',  ( 53.24999999999999289, 27.74999999999998579, 4.000000000000000000 ) ) ;
#57006=DIRECTION ( 'NONE',  ( 0.000000000000000000, -1.000000000000000000, 0.000000000000000000 ) ) ;
#57013=CARTESIAN_POINT ( 'NONE',  ( 39.74999999999999289, 18.74999999999997868, -3.750000000000000000 ) ) ;
#57025=FACE_OUTER_BOUND ( 'NONE', #18735, .T. ) ;
#57039=ORIENTED_EDGE ( 'NONE', *, *, #66005, .F. ) ;
#57053=CARTESIAN_POINT ( 'NONE',  ( 1.000000000000000000, 1.000000000000000222, 3.000000000000000000 ) ) ;
#57063=DIRECTION ( 'NONE',  ( -1.000000000000000000, 0.000000000000000000, 0.000000000000000000 ) ) ;
#57066=EDGE_CURVE ( 'NONE', #67453, #28073, #19763, .T. ) ;
#57071=ORIENTED_EDGE ( 'NONE', *, *, #40055, .F. ) ;
#57074=DIRECTION ( 'NONE',  ( 1.000000000000000000, 0.000000000000000000, 0.000000000000000000 ) ) ;
#57077=VERTEX_POINT ( 'NONE', #10878 ) ;
#57121=AXIS2_PLACEMENT_3D ( 'NONE', #50711, #47465, #10133 ) ;
#57132=EDGE_LOOP ( 'NONE', ( #5651, #55469, #2503, #7334 ) ) ;
#57138=AXIS2_PLACEMENT_3D ( 'NONE', #41, #64830, #44123 ) ;
#57152=CARTESIAN_POINT ( 'NONE',  ( 10.99999999999999645, 11.99999999999999289, 3.500000000000004885 ) ) ;
#57155=PRESENTATION_STYLE_ASSIGNMENT (( #58212 ) ) ;
#57177=CARTESIAN_POINT ( 'NONE',  ( 16.75000000000000711, 25.24999999999998224, 4.000000000000000000 ) ) ;
#57178=EDGE_CURVE ( 'NONE', #4180, #28025, #52388, .T. ) ;
#57205=EDGE_CURVE ( 'NONE', #69157, #24621, #7430, .T. ) ;
#57216=DIRECTION ( 'NONE',  ( -1.000000000000000000, 0.000000000000000000, 0.000000000000000000 ) ) ;
#57217=EDGE_LOOP ( 'NONE', ( #38420, #18071, #5249, #35371 ) ) ;
#57225=AXIS2_PLACEMENT_3D ( 'NONE', #5764, #48753, #452 ) ;
#57235=EDGE_CURVE ( 'NONE', #21322, #54480, #23145, .T. ) ;
#57240=CIRCLE ( 'NONE', #52751, 0.2500000000000002220 ) ;
#57241=CYLINDRICAL_SURFACE ( 'NONE', #62510, 3.100000000000005418 ) ;
#57257=CARTESIAN_POINT ( 'NONE',  ( 17.25000000000000711, 25.24999999999998224, 4.000000000000000000 ) ) ;
#57260=VECTOR ( 'NONE', #66892, 1000.000000000000000 ) ;
#57262=AXIS2_PLACEMENT_3D ( 'NONE', #69338, #21130, #4599 ) ;
#57277=VECTOR ( 'NONE', #40818, 1000.000000000000000 ) ;
#57288=CIRCLE ( 'NONE', #67422, 0.2500000000000002220 ) ;
#57294=CIRCLE ( 'NONE', #14630, 1.000000000000000888 ) ;
#57300=CARTESIAN_POINT ( 'NONE',  ( 1.000000000000000000, 36.74999999999999289, 3.750000000000000000 ) ) ;
#57314=LINE ( 'NONE', #9148, #19197 ) ;
#57319=EDGE_LOOP ( 'NONE', ( #66332, #64679, #38729 ) ) ;
#57334=LINE ( 'NONE', #25325, #2384 ) ;
#57340=DIRECTION ( 'NONE',  ( 0.000000000000000000, 0.000000000000000000, -1.000000000000000000 ) ) ;
#57343=CARTESIAN_POINT ( 'NONE',  ( -1.445602896647333671E-14, 18.74999999999994671, 4.000000000000000000 ) ) ;
#57359=CIRCLE ( 'NONE', #29262, 0.2500000000000002220 ) ;
#57387=AXIS2_PLACEMENT_3D ( 'NONE', #25814, #58884, #58527 ) ;
#57390=AXIS2_PLACEMENT_3D ( 'NONE', #67717, #63123, #2303 ) ;
#57395=CARTESIAN_POINT ( 'NONE',  ( 53.24999999999999289, 27.74999999999998579, 3.750000000000000000 ) ) ;
#57417=AXIS2_PLACEMENT_3D ( 'NONE', #4321, #31778, #25806 ) ;
#57421=EDGE_CURVE ( 'NONE', #51968, #57077, #17590, .T. ) ;
#57424=CIRCLE ( 'NONE', #27066, 0.2500000000000002220 ) ;
#57426=DIRECTION ( 'NONE',  ( 1.000000000000000000, 0.000000000000000000, 0.000000000000000000 ) ) ;
#57431=EDGE_CURVE ( 'NONE', #51630, #11647, #69119, .T. ) ;
#57436=CIRCLE ( 'NONE', #27075, 0.5000000000000004441 ) ;
#57438=LINE ( 'NONE', #46223, #19366 ) ;
#57449=CYLINDRICAL_SURFACE ( 'NONE', #32166, 0.2500000000000002220 ) ;
#57471=FACE_OUTER_BOUND ( 'NONE', #4280, .T. ) ;
#57497=DIRECTION ( 'NONE',  ( 0.000000000000000000, 1.000000000000000000, 0.000000000000000000 ) ) ;
#57518=VERTEX_POINT ( 'NONE', #439 ) ;
#57519=MECHANICAL_DESIGN_GEOMETRIC_PRESENTATION_REPRESENTATION('',(#54140),#58668);
#57523=VERTEX_POINT ( 'NONE', #43474 ) ;
#57542=EDGE_LOOP ( 'NONE', ( #6516, #253, #37103, #67847 ) ) ;
#57552=ORIENTED_EDGE ( 'NONE', *, *, #21781, .T. ) ;
#57563=CARTESIAN_POINT ( 'NONE',  ( 57.74999999999998579, 30.74999999999999289, -3.750000000000000000 ) ) ;
#57630=CARTESIAN_POINT ( 'NONE',  ( 61.74999999999998579, 30.74999999999999289, -4.000000000000000000 ) ) ;
#57633=CARTESIAN_POINT ( 'NONE',  ( 62.24999999999998579, 31.24999999999999289, -4.000000000000000000 ) ) ;
#57639=CARTESIAN_POINT ( 'NONE',  ( 3.749999999999999556, 34.24999999999998579, 3.750000000000000000 ) ) ;
#57671=CARTESIAN_POINT ( 'NONE',  ( 16.75000000000000711, 25.24999999999998224, 3.750000000000000000 ) ) ;
#57684=VERTEX_POINT ( 'NONE', #60598 ) ;
#57702=SPHERICAL_SURFACE ( 'NONE', #63541, 0.2500000000000000000 ) ;
#57717=CARTESIAN_POINT ( 'NONE',  ( 16.75000000000000711, 27.74999999999998224, -4.000000000000000000 ) ) ;
#57722=DIRECTION ( 'NONE',  ( -0.7071067811865451302, 8.659560562354903276E-17, 0.7071067811865500152 ) ) ;
#57748=AXIS2_PLACEMENT_3D ( 'NONE', #29246, #65245, #50728 ) ;
#57754=EDGE_CURVE ( 'NONE', #3926, #14977, #14511, .T. ) ;
#57772=CIRCLE ( 'NONE', #33004, 1.000000000000000000 ) ;
#57779=CARTESIAN_POINT ( 'NONE',  ( 62.24999999999998579, 0.000000000000000000, 3.750000000000000000 ) ) ;
#57785=LINE ( 'NONE', #51453, #37511 ) ;
#57796=ORIENTED_EDGE ( 'NONE', *, *, #59797, .F. ) ;
#57817=DIRECTION ( 'NONE',  ( 1.000000000000000000, 7.709882115452468306E-16, 0.000000000000000000 ) ) ;
#57828=CIRCLE ( 'NONE', #38734, 0.2500000000000002220 ) ;
#57852=EDGE_CURVE ( 'NONE', #14977, #59828, #8488, .T. ) ;
#57887=CARTESIAN_POINT ( 'NONE',  ( 7.899999999999995914, 11.99999999999999289, 4.000000000000000000 ) ) ;
#57890=ORIENTED_EDGE ( 'NONE', *, *, #53238, .T. ) ;
#57892=EDGE_LOOP ( 'NONE', ( #52166, #23600, #38421, #54711 ) ) ;
#57894=FACE_OUTER_BOUND ( 'NONE', #14573, .T. ) ;
#57903=VERTEX_POINT ( 'NONE', #26452 ) ;
#57912=EDGE_CURVE ( 'NONE', #27898, #44763, #56783, .T. ) ;
#57938=DIRECTION ( 'NONE',  ( 0.000000000000000000, 0.000000000000000000, -1.000000000000000000 ) ) ;
#57948=SPHERICAL_SURFACE ( 'NONE', #40679, 0.2500000000000000000 ) ;
#57957=CARTESIAN_POINT ( 'NONE',  ( 12.25000000000000533, 28.24999999999998224, 3.750000000000000000 ) ) ;
#58018=DIRECTION ( 'NONE',  ( -1.000000000000000000, 0.000000000000000000, 0.000000000000000000 ) ) ;
#58024=DIRECTION ( 'NONE',  ( 0.000000000000000000, 0.000000000000000000, -1.000000000000000000 ) ) ;
#58048=CARTESIAN_POINT ( 'NONE',  ( 48.50000000000000000, 21.99999999999998579, 3.750000000000000000 ) ) ;
#58059=CARTESIAN_POINT ( 'NONE',  ( 44.25000000000000000, 0.000000000000000000, 3.750000000000000000 ) ) ;
#58060=DIRECTION ( 'NONE',  ( 0.000000000000000000, -0.000000000000000000, 1.000000000000000000 ) ) ;
#58076=ORIENTED_EDGE ( 'NONE', *, *, #21871, .F. ) ;
#58088=DIRECTION ( 'NONE',  ( 1.000000000000000000, 0.000000000000000000, 0.000000000000000000 ) ) ;
#58097=DIRECTION ( 'NONE',  ( -1.156482317317870344E-15, -1.000000000000000000, 0.000000000000000000 ) ) ;
#58109=ORIENTED_EDGE ( 'NONE', *, *, #2216, .F. ) ;
#58111=ADVANCED_FACE ( 'NONE', ( #45786 ), #57702, .T. ) ;
#58137=FILL_AREA_STYLE ('',( #37420 ) ) ;
#58163=DIRECTION ( 'NONE',  ( -1.000000000000000000, 0.000000000000000000, 0.000000000000000000 ) ) ;
#58166=EDGE_CURVE ( 'NONE', #23317, #34747, #69180, .T. ) ;
#58173=PLANE ( 'NONE',  #67204 ) ;
#58181=FACE_OUTER_BOUND ( 'NONE', #29240, .T. ) ;
#58192=ORIENTED_EDGE ( 'NONE', *, *, #51295, .F. ) ;
#58212=SURFACE_STYLE_USAGE ( .BOTH. , #26536 ) ;
#58217=CARTESIAN_POINT ( 'NONE',  ( 52.75000000000000000, 25.24999999999998579, 3.750000000000000000 ) ) ;
#58223=EDGE_CURVE ( 'NONE', #68534, #1034, #14148, .T. ) ;
#58229=ADVANCED_FACE ( 'NONE', ( #10554 ), #16202, .T. ) ;
#58237=CARTESIAN_POINT ( 'NONE',  ( 66.49999999999998579, 34.24999999999999289, 3.750000000000000000 ) ) ;
#58254=VECTOR ( 'NONE', #31417, 1000.000000000000000 ) ;
#58258=DIRECTION ( 'NONE',  ( 0.000000000000000000, 0.000000000000000000, 1.000000000000000000 ) ) ;
#58266=ORIENTED_EDGE ( 'NONE', *, *, #14455, .T. ) ;
#58267=DIRECTION ( 'NONE',  ( -0.7071067811865451302, 0.000000000000000000, -0.7071067811865500152 ) ) ;
#58271=FACE_OUTER_BOUND ( 'NONE', #2738, .T. ) ;
#58284=DIRECTION ( 'NONE',  ( 1.000000000000000000, 0.000000000000000000, 0.000000000000000000 ) ) ;
#58344=DIRECTION ( 'NONE',  ( 0.000000000000000000, -1.000000000000000000, 0.000000000000000000 ) ) ;
#58372=DIRECTION ( 'NONE',  ( -1.000000000000000000, 0.000000000000000000, 0.000000000000000000 ) ) ;
#58377=EDGE_LOOP ( 'NONE', ( #13290, #50238, #50670 ) ) ;
#58379=DIRECTION ( 'NONE',  ( -1.000000000000000000, 0.000000000000000000, 0.000000000000000000 ) ) ;
#58390=DIRECTION ( 'NONE',  ( 0.000000000000000000, 0.000000000000000000, -1.000000000000000000 ) ) ;
#58396=EDGE_CURVE ( 'NONE', #60291, #47340, #52326, .T. ) ;
#58407=DIRECTION ( 'NONE',  ( 1.000000000000000000, 2.168404344971008868E-16, 0.000000000000000000 ) ) ;
#58413=VERTEX_POINT ( 'NONE', #22482 ) ;
#58414=CYLINDRICAL_SURFACE ( 'NONE', #60469, 0.2500000000000002220 ) ;
#58417=VECTOR ( 'NONE', #4307, 1000.000000000000000 ) ;
#58423=DIRECTION ( 'NONE',  ( -0.000000000000000000, -0.000000000000000000, 1.000000000000000000 ) ) ;
#58455=DIRECTION ( 'NONE',  ( -1.000000000000000000, 0.000000000000000000, 0.000000000000000000 ) ) ;
#58459=LINE ( 'NONE', #10282, #24132 ) ;
#58462=ORIENTED_EDGE ( 'NONE', *, *, #63368, .F. ) ;
#58464=EDGE_CURVE ( 'NONE', #68782, #49817, #67134, .T. ) ;
#58475=ORIENTED_EDGE ( 'NONE', *, *, #48343, .F. ) ;
#58498=TOROIDAL_SURFACE ( 'NONE', #36179, 0.5000000000000000000, 0.2500000000000000000 ) ;
#58510=ORIENTED_EDGE ( 'NONE', *, *, #29451, .T. ) ;
#58520=CIRCLE ( 'NONE', #18104, 0.2500000000000002220 ) ;
#58524=AXIS2_PLACEMENT_3D ( 'NONE', #23250, #28848, #34487 ) ;
#58526=DIRECTION ( 'NONE',  ( 0.000000000000000000, 0.000000000000000000, -1.000000000000000000 ) ) ;
#58527=DIRECTION ( 'NONE',  ( 0.000000000000000000, 0.000000000000000000, -1.000000000000000000 ) ) ;
#58534=DIRECTION ( 'NONE',  ( 1.000000000000000000, -0.000000000000000000, 0.000000000000000000 ) ) ;
#58543=AXIS2_PLACEMENT_3D ( 'NONE', #47245, #20464, #41968 ) ;
#58553=ORIENTED_EDGE ( 'NONE', *, *, #48686, .T. ) ;
#58592=DIRECTION ( 'NONE',  ( 0.000000000000000000, 1.000000000000000000, 0.000000000000000000 ) ) ;
#58606=CIRCLE ( 'NONE', #26067, 0.2500000000000002220 ) ;
#58635=CARTESIAN_POINT ( 'NONE',  ( 59.00000000000000000, 11.99999999999999822, 4.000000000000000000 ) ) ;
#58650=DIRECTION ( 'NONE',  ( -1.000000000000000000, 0.000000000000000000, 0.000000000000000000 ) ) ;
#58668=( GEOMETRIC_REPRESENTATION_CONTEXT ( 3 ) GLOBAL_UNCERTAINTY_ASSIGNED_CONTEXT ( ( #64900 ) ) GLOBAL_UNIT_ASSIGNED_CONTEXT ( ( #9615, #31370, #10296 ) ) REPRESENTATION_CONTEXT ( 'NONE', 'WORKASPACE' ) );
#58676=CIRCLE ( 'NONE', #17191, 0.2500000000000002220 ) ;
#58691=EDGE_CURVE ( 'NONE', #10058, #35167, #69355, .T. ) ;
#58725=FACE_OUTER_BOUND ( 'NONE', #44989, .T. ) ;
#58735=DIRECTION ( 'NONE',  ( -1.000000000000000000, 0.000000000000000000, 0.000000000000000000 ) ) ;
#58739=FACE_OUTER_BOUND ( 'NONE', #2676, .T. ) ;
#58758=ORIENTED_EDGE ( 'NONE', *, *, #39344, .T. ) ;
#58776=PLANE ( 'NONE',  #59517 ) ;
#58784=CARTESIAN_POINT ( 'NONE',  ( 52.75000000000000000, 24.74999999999998224, -4.000000000000000000 ) ) ;
#58788=ORIENTED_EDGE ( 'NONE', *, *, #21282, .T. ) ;
#58797=DIRECTION ( 'NONE',  ( 0.000000000000000000, 0.000000000000000000, 1.000000000000000000 ) ) ;
#58804=ORIENTED_EDGE ( 'NONE', *, *, #7948, .T. ) ;
#58809=VERTEX_POINT ( 'NONE', #13210 ) ;
#58827=ORIENTED_EDGE ( 'NONE', *, *, #57421, .T. ) ;
#58847=VECTOR ( 'NONE', #24530, 1000.000000000000000 ) ;
#58871=ADVANCED_FACE ( 'NONE', ( #30080 ), #40321, .T. ) ;
#58873=CARTESIAN_POINT ( 'NONE',  ( 62.24999999999998579, 31.24999999999999289, 4.000000000000000000 ) ) ;
#58884=DIRECTION ( 'NONE',  ( 1.000000000000000000, 0.000000000000000000, 0.000000000000000000 ) ) ;
#58923=ORIENTED_EDGE ( 'NONE', *, *, #24779, .T. ) ;
#58931=EDGE_CURVE ( 'NONE', #4102, #29672, #51915, .T. ) ;
#58933=ORIENTED_EDGE ( 'NONE', *, *, #62902, .F. ) ;
#58938=VECTOR ( 'NONE', #42067, 1000.000000000000000 ) ;
#58940=ADVANCED_FACE ( 'NONE', ( #69133 ), #36465, .F. ) ;
#58941=CYLINDRICAL_SURFACE ( 'NONE', #67349, 1.000000000000000000 ) ;
#58974=ORIENTED_EDGE ( 'NONE', *, *, #5273, .T. ) ;
#59003=LINE ( 'NONE', #63588, #65187 ) ;
#59005=VERTEX_POINT ( 'NONE', #65218 ) ;
#59016=CARTESIAN_POINT ( 'NONE',  ( 61.99999999999998579, 31.24999999999999289, -3.750000000000000000 ) ) ;
#59020=VECTOR ( 'NONE', #5869, 1000.000000000000000 ) ;
#59022=VERTEX_POINT ( 'NONE', #49407 ) ;
#59030=EDGE_CURVE ( 'NONE', #13725, #51712, #66535, .T. ) ;
#59058=VERTEX_POINT ( 'NONE', #17067 ) ;
#59076=EDGE_CURVE ( 'NONE', #8197, #21622, #32543, .T. ) ;
#59088=FACE_OUTER_BOUND ( 'NONE', #66938, .T. ) ;
#59094=LINE ( 'NONE', #4580, #24724 ) ;
#59097=DIRECTION ( 'NONE',  ( 0.000000000000000000, 1.000000000000000000, 0.000000000000000000 ) ) ;
#59119=EDGE_LOOP ( 'NONE', ( #47019, #32664, #39486, #33727 ) ) ;
#59146=AXIS2_PLACEMENT_3D ( 'NONE', #21787, #38699, #22474 ) ;
#59151=DIRECTION ( 'NONE',  ( -1.000000000000000000, 0.000000000000000000, 0.000000000000000000 ) ) ;
#59155=EDGE_CURVE ( 'NONE', #38116, #62934, #35915, .T. ) ;
#59210=ORIENTED_EDGE ( 'NONE', *, *, #30893, .T. ) ;
#59218=ORIENTED_EDGE ( 'NONE', *, *, #10087, .F. ) ;
#59224=EDGE_LOOP ( 'NONE', ( #25223, #67900, #29179, #6808 ) ) ;
#59225=DIRECTION ( 'NONE',  ( -1.000000000000000000, 0.000000000000000000, 0.000000000000000000 ) ) ;
#59226=EDGE_LOOP ( 'NONE', ( #59552, #26786, #6553 ) ) ;
#59242=EDGE_CURVE ( 'NONE', #48045, #27359, #68521, .T. ) ;
#59272=ORIENTED_EDGE ( 'NONE', *, *, #31120, .T. ) ;
#59275=ORIENTED_EDGE ( 'NONE', *, *, #15438, .T. ) ;
#59276=CARTESIAN_POINT ( 'NONE',  ( 21.25000000000000711, 22.24999999999998224, 3.750000000000000000 ) ) ;
#59283=CARTESIAN_POINT ( 'NONE',  ( 57.24999999999999289, 27.74999999999998934, -3.750000000000000000 ) ) ;
#59288=DIRECTION ( 'NONE',  ( 0.000000000000000000, -1.000000000000000000, 0.000000000000000000 ) ) ;
#59294=CARTESIAN_POINT ( 'NONE',  ( 25.75000000000001066, 21.99999999999998224, -3.750000000000000000 ) ) ;
#59308=VERTEX_POINT ( 'NONE', #20324 ) ;
#59324=CARTESIAN_POINT ( 'NONE',  ( 48.75000000000004974, 1.127570259384924864E-13, 4.000000000000000000 ) ) ;
#59348=CARTESIAN_POINT ( 'NONE',  ( 14.60000000000000142, 11.99999999999999289, -4.000000000000000000 ) ) ;
#59375=VERTEX_POINT ( 'NONE', #52015 ) ;
#59414=FACE_OUTER_BOUND ( 'NONE', #12049, .T. ) ;
#59418=DIRECTION ( 'NONE',  ( 0.000000000000000000, 0.000000000000000000, 1.000000000000000000 ) ) ;
#59423=DIRECTION ( 'NONE',  ( -1.000000000000000000, -2.168404344971008868E-16, 0.000000000000000000 ) ) ;
#59462=ORIENTED_EDGE ( 'NONE', *, *, #15758, .F. ) ;
#59471=EDGE_CURVE ( 'NONE', #51828, #4422, #59003, .T. ) ;
#59472=DIRECTION ( 'NONE',  ( 0.000000000000000000, -1.000000000000000000, 0.000000000000000000 ) ) ;
#59473=VECTOR ( 'NONE', #51880, 1000.000000000000000 ) ;
#59506=ORIENTED_EDGE ( 'NONE', *, *, #59797, .T. ) ;
#59517=AXIS2_PLACEMENT_3D ( 'NONE', #38406, #69666, #16243 ) ;
#59522=DIRECTION ( 'NONE',  ( -1.000000000000000000, 0.000000000000000000, 0.000000000000000000 ) ) ;
#59532=CIRCLE ( 'NONE', #20221, 3.599999999999992095 ) ;
#59548=CARTESIAN_POINT ( 'NONE',  ( 10.99999999999999645, 11.99999999999999289, -4.000000000000000000 ) ) ;
#59549=EDGE_CURVE ( 'NONE', #68323, #3926, #53045, .T. ) ;
#59550=CARTESIAN_POINT ( 'NONE',  ( 62.59999999999998721, 11.99999999999999822, -4.000000000000000000 ) ) ;
#59552=ORIENTED_EDGE ( 'NONE', *, *, #63387, .T. ) ;
#59560=AXIS2_PLACEMENT_3D ( 'NONE', #62230, #14054, #52050 ) ;
#59625=FACE_OUTER_BOUND ( 'NONE', #43621, .T. ) ;
#59640=ADVANCED_FACE ( 'NONE', ( #9829 ), #30369, .F. ) ;
#59664=ORIENTED_EDGE ( 'NONE', *, *, #17209, .T. ) ;
#59665=DIRECTION ( 'NONE',  ( 1.156482317317870344E-15, -1.000000000000000000, 0.000000000000000000 ) ) ;
#59698=PRODUCT_DEFINITION ( 'UNKNOWN', '', #41676, #7902 ) ;
#59715=LINE ( 'NONE', #7990, #60750 ) ;
#59722=EDGE_CURVE ( 'NONE', #19333, #43779, #59715, .T. ) ;
#59725=DIRECTION ( 'NONE',  ( 1.000000000000000000, 0.000000000000000000, 0.000000000000000000 ) ) ;
#59745=FACE_OUTER_BOUND ( 'NONE', #3102, .T. ) ;
#59752=ORIENTED_EDGE ( 'NONE', *, *, #334, .T. ) ;
#59763=DIRECTION ( 'NONE',  ( 1.000000000000000000, 0.000000000000000000, 0.000000000000000000 ) ) ;
#59765=LINE ( 'NONE', #12957, #3716 ) ;
#59797=EDGE_CURVE ( 'NONE', #68610, #2459, #65345, .T. ) ;
#59799=CARTESIAN_POINT ( 'NONE',  ( 52.99999999999999289, 27.74999999999998579, -3.750000000000000000 ) ) ;
#59802=EDGE_CURVE ( 'NONE', #13725, #49467, #32645, .T. ) ;
#59807=DIRECTION ( 'NONE',  ( -1.000000000000000000, 0.000000000000000000, 0.000000000000000000 ) ) ;
#59817=EDGE_CURVE ( 'NONE', #12327, #48755, #58520, .T. ) ;
#59821=AXIS2_PLACEMENT_3D ( 'NONE', #55766, #55409, #6876 ) ;
#59828=VERTEX_POINT ( 'NONE', #43936 ) ;
#59837=ORIENTED_EDGE ( 'NONE', *, *, #51088, .F. ) ;
#59857=CARTESIAN_POINT ( 'NONE',  ( 62.24999999999998579, 0.000000000000000000, 4.000000000000000000 ) ) ;
#59872=AXIS2_PLACEMENT_3D ( 'NONE', #51651, #24540, #18612 ) ;
#59878=LINE ( 'NONE', #22955, #38209 ) ;
#59890=AXIS2_PLACEMENT_3D ( 'NONE', #63295, #41182, #14774 ) ;
#59903=CARTESIAN_POINT ( 'NONE',  ( -1.224646799147353207E-16, 1.000000000000000000, 4.000000000000000000 ) ) ;
#59912=LINE ( 'NONE', #54635, #45509 ) ;
#59922=CARTESIAN_POINT ( 'NONE',  ( 16.75000000000000711, 27.74999999999998224, 4.000000000000000000 ) ) ;
#59926=CIRCLE ( 'NONE', #3712, 0.2500000000000002220 ) ;
#59930=EDGE_LOOP ( 'NONE', ( #7935, #36947, #1810, #61469 ) ) ;
#59935=VERTEX_POINT ( 'NONE', #4699 ) ;
#59951=EDGE_CURVE ( 'NONE', #31359, #13744, #20295, .T. ) ;
#59977=CARTESIAN_POINT ( 'NONE',  ( 0.000000000000000000, 0.000000000000000000, 0.000000000000000000 ) ) ;
#59989=CYLINDRICAL_SURFACE ( 'NONE', #20108, 0.2500000000000002220 ) ;
#59990=AXIS2_PLACEMENT_3D ( 'NONE', #24341, #35618, #12749 ) ;
#59994=ORIENTED_EDGE ( 'NONE', *, *, #19817, .F. ) ;
#59999=VECTOR ( 'NONE', #56117, 1000.000000000000000 ) ;
#60004=CARTESIAN_POINT ( 'NONE',  ( 1.000000000000000000, 36.99999999999999289, -3.000000000000000000 ) ) ;
#60007=VERTEX_POINT ( 'NONE', #16674 ) ;
#60013=ORIENTED_EDGE ( 'NONE', *, *, #52149, .F. ) ;
#60028=DIRECTION ( 'NONE',  ( -0.000000000000000000, 0.000000000000000000, 1.000000000000000000 ) ) ;
#60036=DIRECTION ( 'NONE',  ( -1.000000000000000000, 0.000000000000000000, 0.000000000000000000 ) ) ;
#60042=LINE ( 'NONE', #18172, #1891 ) ;
#60062=CIRCLE ( 'NONE', #459, 0.2500000000000002220 ) ;
#60073=FACE_OUTER_BOUND ( 'NONE', #12658, .T. ) ;
#60097=ORIENTED_EDGE ( 'NONE', *, *, #25169, .T. ) ;
#60114=DIRECTION ( 'NONE',  ( 0.000000000000000000, -0.000000000000000000, 1.000000000000000000 ) ) ;
#60117=CARTESIAN_POINT ( 'NONE',  ( 1.000000000000000222, 1.224646799147373175E-16, 3.000000000000000000 ) ) ;
#60135=ORIENTED_EDGE ( 'NONE', *, *, #21022, .F. ) ;
#60136=SURFACE_STYLE_USAGE ( .BOTH. , #17601 ) ;
#60139=AXIS2_PLACEMENT_3D ( 'NONE', #48657, #6041, #47981 ) ;
#60155=DIRECTION ( 'NONE',  ( 0.000000000000000000, 0.000000000000000000, -1.000000000000000000 ) ) ;
#60165=CIRCLE ( 'NONE', #19746, 0.5000000000000004441 ) ;
#60169=CARTESIAN_POINT ( 'NONE',  ( 66.74999999999998579, 0.000000000000000000, 4.000000000000000000 ) ) ;
#60174=CARTESIAN_POINT ( 'NONE',  ( 44.25000000000000000, 21.99999999999998579, -3.750000000000000000 ) ) ;
#60195=CYLINDRICAL_SURFACE ( 'NONE', #41971, 0.2500000000000002220 ) ;
#60230=DIRECTION ( 'NONE',  ( 0.000000000000000000, 0.000000000000000000, 1.000000000000000000 ) ) ;
#60248=CARTESIAN_POINT ( 'NONE',  ( 30.50000000000001066, 15.99999999999997691, 3.750000000000000000 ) ) ;
#60255=CARTESIAN_POINT ( 'NONE',  ( 21.75000000000001066, 21.99999999999998224, 3.750000000000000000 ) ) ;
#60257=AXIS2_PLACEMENT_3D ( 'NONE', #46324, #35737, #35033 ) ;
#60276=EDGE_CURVE ( 'NONE', #61571, #41886, #64187, .T. ) ;
#60288=ORIENTED_EDGE ( 'NONE', *, *, #26385, .T. ) ;
#60291=VERTEX_POINT ( 'NONE', #35608 ) ;
#60308=DIRECTION ( 'NONE',  ( 1.000000000000000000, 0.000000000000000000, 0.000000000000000000 ) ) ;
#60310=CARTESIAN_POINT ( 'NONE',  ( 16.75000000000000711, 27.99999999999998224, 3.750000000000000000 ) ) ;
#60315=ORIENTED_EDGE ( 'NONE', *, *, #46929, .T. ) ;
#60317=CYLINDRICAL_SURFACE ( 'NONE', #53857, 0.2500000000000002220 ) ;
#60347=FACE_OUTER_BOUND ( 'NONE', #27661, .T. ) ;
#60363=CIRCLE ( 'NONE', #32297, 0.2500000000000002220 ) ;
#60371=SPHERICAL_SURFACE ( 'NONE', #14182, 0.2500000000000000000 ) ;
#60375=ORIENTED_EDGE ( 'NONE', *, *, #21871, .T. ) ;
#60389=DIRECTION ( 'NONE',  ( -0.000000000000000000, 0.000000000000000000, -1.000000000000000000 ) ) ;
#60393=VECTOR ( 'NONE', #35824, 1000.000000000000000 ) ;
#60401=ORIENTED_EDGE ( 'NONE', *, *, #65266, .T. ) ;
#60408=VERTEX_POINT ( 'NONE', #48623 ) ;
#60413=FACE_OUTER_BOUND ( 'NONE', #33572, .T. ) ;
#60426=DIRECTION ( 'NONE',  ( -0.000000000000000000, -0.000000000000000000, -1.000000000000000000 ) ) ;
#60442=CARTESIAN_POINT ( 'NONE',  ( 48.74999999999999289, 24.74999999999998579, 3.750000000000000000 ) ) ;
#60452=CARTESIAN_POINT ( 'NONE',  ( 21.75000000000001066, 21.99999999999998224, -3.750000000000000000 ) ) ;
#60455=ORIENTED_EDGE ( 'NONE', *, *, #50924, .T. ) ;
#60469=AXIS2_PLACEMENT_3D ( 'NONE', #31676, #26045, #16913 ) ;
#60470=CARTESIAN_POINT ( 'NONE',  ( 44.25000000000000000, 19.24999999999998224, 4.000000000000000000 ) ) ;
#60473=VECTOR ( 'NONE', #23965, 1000.000000000000000 ) ;
#60479=DIRECTION ( 'NONE',  ( -0.000000000000000000, 0.000000000000000000, -1.000000000000000000 ) ) ;
#60481=ORIENTED_EDGE ( 'NONE', *, *, #33836, .T. ) ;
#60498=ORIENTED_EDGE ( 'NONE', *, *, #68319, .F. ) ;
#60504=VERTEX_POINT ( 'NONE', #40466 ) ;
#60517=DIRECTION ( 'NONE',  ( 0.000000000000000000, 0.000000000000000000, -1.000000000000000000 ) ) ;
#60522=VERTEX_POINT ( 'NONE', #68228 ) ;
#60544=DIRECTION ( 'NONE',  ( 0.000000000000000000, 0.000000000000000000, -1.000000000000000000 ) ) ;
#60573=AXIS2_PLACEMENT_3D ( 'NONE', #19503, #52587, #9322 ) ;
#60598=CARTESIAN_POINT ( 'NONE',  ( 8.000000000000000000, 33.74999999999998579, -3.750000000000000000 ) ) ;
#60616=VECTOR ( 'NONE', #20440, 1000.000000000000000 ) ;
#60625=CARTESIAN_POINT ( 'NONE',  ( 7.899999999999995914, 11.99999999999999289, 3.500000000000004885 ) ) ;
#60653=CARTESIAN_POINT ( 'NONE',  ( 39.74999999999999289, 18.99999999999997868, 3.750000000000000000 ) ) ;
#60654=DIRECTION ( 'NONE',  ( 1.000000000000000000, -7.709882115452468306E-16, -0.000000000000000000 ) ) ;
#60669=ORIENTED_EDGE ( 'NONE', *, *, #22174, .F. ) ;
#60687=VECTOR ( 'NONE', #4939, 1000.000000000000000 ) ;
#60717=DIRECTION ( 'NONE',  ( 0.000000000000000000, 0.000000000000000000, -1.000000000000000000 ) ) ;
#60750=VECTOR ( 'NONE', #55121, 1000.000000000000000 ) ;
#60760=ORIENTED_EDGE ( 'NONE', *, *, #10508, .F. ) ;
#60764=CARTESIAN_POINT ( 'NONE',  ( 52.75000000000000000, 24.99999999999998579, -4.000000000000000000 ) ) ;
#60812=AXIS2_PLACEMENT_3D ( 'NONE', #61713, #2947, #9336 ) ;
#60815=DIRECTION ( 'NONE',  ( 1.000000000000000000, -0.000000000000000000, 0.000000000000000000 ) ) ;
#60830=DIRECTION ( 'NONE',  ( -1.000000000000000000, 7.709882115452468306E-16, 0.000000000000000000 ) ) ;
#60832=CARTESIAN_POINT ( 'NONE',  ( 30.75000000000001066, 15.74999999999997513, -3.750000000000000000 ) ) ;
#60849=CARTESIAN_POINT ( 'NONE',  ( 25.75000000000001066, 21.74999999999998224, 4.000000000000000000 ) ) ;
#60851=DIRECTION ( 'NONE',  ( -0.000000000000000000, -0.000000000000000000, 1.000000000000000000 ) ) ;
#60854=ORIENTED_EDGE ( 'NONE', *, *, #45528, .F. ) ;
#60859=CARTESIAN_POINT ( 'NONE',  ( 12.25000000000000355, 30.99999999999998579, 4.000000000000000000 ) ) ;
#60875=AXIS2_PLACEMENT_3D ( 'NONE', #36869, #58284, #10113 ) ;
#60880=AXIS2_PLACEMENT_3D ( 'NONE', #8000, #29450, #50925 ) ;
#60886=EDGE_LOOP ( 'NONE', ( #13043, #4373, #19821, #4660 ) ) ;
#60902=ADVANCED_FACE ( 'NONE', ( #25896 ), #43862, .T. ) ;
#60904=CARTESIAN_POINT ( 'NONE',  ( 0.000000000000000000, 18.74999999999997868, 3.750000000000000000 ) ) ;
#60905=ORIENTED_EDGE ( 'NONE', *, *, #68710, .F. ) ;
#60908=CARTESIAN_POINT ( 'NONE',  ( 66.24999999999998579, 33.74999999999999289, -4.000000000000000000 ) ) ;
#60925=ORIENTED_EDGE ( 'NONE', *, *, #46904, .F. ) ;
#60944=LINE ( 'NONE', #45173, #49667 ) ;
#60988=EDGE_CURVE ( 'NONE', #31359, #58413, #47779, .T. ) ;
#61006=ADVANCED_FACE ( 'NONE', ( #31870 ), #33274, .T. ) ;
#61011=CARTESIAN_POINT ( 'NONE',  ( 62.24999999999998579, 33.74999999999999289, -3.750000000000000000 ) ) ;
#61033=VECTOR ( 'NONE', #906, 1000.000000000000000 ) ;
#61040=FILL_AREA_STYLE ('',( #39629 ) ) ;
#61051=EDGE_CURVE ( 'NONE', #2459, #26491, #65450, .T. ) ;
#61058=ORIENTED_EDGE ( 'NONE', *, *, #55603, .T. ) ;
#61062=DIRECTION ( 'NONE',  ( 0.000000000000000000, 1.000000000000000000, 0.000000000000000000 ) ) ;
#61077=DIRECTION ( 'NONE',  ( 0.000000000000000000, 0.000000000000000000, -1.000000000000000000 ) ) ;
#61095=DIRECTION ( 'NONE',  ( 0.000000000000000000, 0.000000000000000000, -1.000000000000000000 ) ) ;
#61101=DIRECTION ( 'NONE',  ( -0.000000000000000000, -0.000000000000000000, -1.000000000000000000 ) ) ;
#61103=CARTESIAN_POINT ( 'NONE',  ( 44.25000000000000000, 21.74999999999998579, 4.000000000000000000 ) ) ;
#61104=EDGE_CURVE ( 'NONE', #37003, #36322, #53110, .T. ) ;
#61107=CARTESIAN_POINT ( 'NONE',  ( 48.25000000000000000, 22.24999999999998579, -3.750000000000000000 ) ) ;
#61112=VERTEX_POINT ( 'NONE', #23749 ) ;
#61117=CARTESIAN_POINT ( 'NONE',  ( 57.74999999999998579, 30.74999999999999289, 4.000000000000000000 ) ) ;
#61132=ORIENTED_EDGE ( 'NONE', *, *, #62095, .T. ) ;
#61144=DIRECTION ( 'NONE',  ( -1.000000000000000000, 0.000000000000000000, 0.000000000000000000 ) ) ;
#61145=VECTOR ( 'NONE', #25545, 1000.000000000000000 ) ;
#61146=EDGE_CURVE ( 'NONE', #65666, #43970, #36318, .T. ) ;
#61151=CARTESIAN_POINT ( 'NONE',  ( 3.749999999999999556, 34.24999999999998579, -4.000000000000000000 ) ) ;
#61159=FACE_OUTER_BOUND ( 'NONE', #32029, .T. ) ;
#61218=DIRECTION ( 'NONE',  ( -1.000000000000000000, 0.000000000000000000, 0.000000000000000000 ) ) ;
#61225=DIRECTION ( 'NONE',  ( 0.000000000000000000, 0.000000000000000000, -1.000000000000000000 ) ) ;
#61231=FACE_OUTER_BOUND ( 'NONE', #47868, .T. ) ;
#61300=ORIENTED_EDGE ( 'NONE', *, *, #173, .F. ) ;
#61308=EDGE_CURVE ( 'NONE', #59005, #10834, #2576, .T. ) ;
#61310=VERTEX_POINT ( 'NONE', #43463 ) ;
#61324=AXIS2_PLACEMENT_3D ( 'NONE', #36165, #31181, #68857 ) ;
#61379=DIRECTION ( 'NONE',  ( 0.000000000000000000, 0.000000000000000000, 1.000000000000000000 ) ) ;
#61390=EDGE_CURVE ( 'NONE', #18083, #24587, #30680, .T. ) ;
#61412=CARTESIAN_POINT ( 'NONE',  ( 3.249999999999998668, 36.74999999999999289, 3.750000000000000000 ) ) ;
#61422=DIRECTION ( 'NONE',  ( -1.000000000000000000, 0.000000000000000000, 0.000000000000000000 ) ) ;
#61428=UNCERTAINTY_MEASURE_WITH_UNIT (LENGTH_MEASURE( 1.000000000000000082E-05 ), #35686, 'distance_accuracy_value', 'NONE');
#61433=EDGE_CURVE ( 'NONE', #28127, #26382, #23969, .T. ) ;
#61435=EDGE_CURVE ( 'NONE', #823, #49817, #62119, .T. ) ;
#61448=VERTEX_POINT ( 'NONE', #29897 ) ;
#61468=CARTESIAN_POINT ( 'NONE',  ( 16.75000000000000711, 27.74999999999998224, 3.750000000000000000 ) ) ;
#61469=ORIENTED_EDGE ( 'NONE', *, *, #45552, .T. ) ;
#61479=DIRECTION ( 'NONE',  ( -0.000000000000000000, 0.000000000000000000, -1.000000000000000000 ) ) ;
#61482=VERTEX_POINT ( 'NONE', #65185 ) ;
#61490=VERTEX_POINT ( 'NONE', #51014 ) ;
#61512=CARTESIAN_POINT ( 'NONE',  ( 66.74999999999998579, 34.24999999999999289, 3.750000000000000000 ) ) ;
#61514=ADVANCED_FACE ( 'NONE', ( #24593 ), #39797, .F. ) ;
#61522=EDGE_LOOP ( 'NONE', ( #53129, #19044, #29898, #25261 ) ) ;
#61527=DIRECTION ( 'NONE',  ( -0.000000000000000000, 0.000000000000000000, -1.000000000000000000 ) ) ;
#61531=AXIS2_PLACEMENT_3D ( 'NONE', #3687, #3330, #35046 ) ;
#61537=CARTESIAN_POINT ( 'NONE',  ( 12.25000000000000355, 30.74999999999998579, -4.000000000000000000 ) ) ;
#61549=PLANE ( 'NONE',  #45327 ) ;
#61571=VERTEX_POINT ( 'NONE', #26336 ) ;
#61590=CARTESIAN_POINT ( 'NONE',  ( 48.75000000000000000, 22.24999999999998579, -4.000000000000000000 ) ) ;
#61599=CIRCLE ( 'NONE', #13306, 0.2500000000000002220 ) ;
#61605=VERTEX_POINT ( 'NONE', #20377 ) ;
#61608=ADVANCED_FACE ( 'NONE', ( #15819 ), #51709, .F. ) ;
#61616=ORIENTED_EDGE ( 'NONE', *, *, #23282, .F. ) ;
#61629=CARTESIAN_POINT ( 'NONE',  ( 55.40000000000000568, 11.99999999999999822, -4.000000000000000000 ) ) ;
#61645=LINE ( 'NONE', #34583, #7155 ) ;
#61671=CYLINDRICAL_SURFACE ( 'NONE', #9990, 0.2500000000000002220 ) ;
#61694=EDGE_CURVE ( 'NONE', #61490, #59935, #37654, .T. ) ;
#61697=CYLINDRICAL_SURFACE ( 'NONE', #41760, 1.000000000000000000 ) ;
#61699=FACE_OUTER_BOUND ( 'NONE', #8364, .T. ) ;
#61702=ORIENTED_EDGE ( 'NONE', *, *, #62582, .F. ) ;
#61709=DIRECTION ( 'NONE',  ( 0.000000000000000000, -0.000000000000000000, 1.000000000000000000 ) ) ;
#61711=EDGE_LOOP ( 'NONE', ( #69627, #43681, #52418, #8336 ) ) ;
#61713=CARTESIAN_POINT ( 'NONE',  ( 3.249999999999998668, 36.74999999999999289, -3.750000000000000000 ) ) ;
#61732=FACE_OUTER_BOUND ( 'NONE', #4202, .T. ) ;
#61733=EDGE_LOOP ( 'NONE', ( #50502, #47457, #34072, #17815 ) ) ;
#61750=DIRECTION ( 'NONE',  ( -1.000000000000000000, 0.000000000000000000, 0.000000000000000000 ) ) ;
#61756=AXIS2_PLACEMENT_3D ( 'NONE', #6464, #43485, #8146 ) ;
#61788=AXIS2_PLACEMENT_3D ( 'NONE', #42542, #47851, #21044 ) ;
#61807=AXIS2_PLACEMENT_3D ( 'NONE', #5029, #10997, #53899 ) ;
#61809=ORIENTED_EDGE ( 'NONE', *, *, #33620, .F. ) ;
#61882=DIRECTION ( 'NONE',  ( 1.000000000000000000, -0.000000000000000000, 0.000000000000000000 ) ) ;
#61883=AXIS2_PLACEMENT_3D ( 'NONE', #4975, #47609, #47955 ) ;
#61891=FACE_OUTER_BOUND ( 'NONE', #55443, .T. ) ;
#61910=CIRCLE ( 'NONE', #49586, 0.2500000000000002220 ) ;
#61912=CARTESIAN_POINT ( 'NONE',  ( 25.75000000000001066, 21.74999999999998224, 3.750000000000000000 ) ) ;
#61914=DIRECTION ( 'NONE',  ( 1.000000000000000000, 0.000000000000000000, -0.000000000000000000 ) ) ;
#61920=ORIENTED_EDGE ( 'NONE', *, *, #18466, .F. ) ;
#61937=EDGE_CURVE ( 'NONE', #17044, #9702, #33072, .T. ) ;
#61941=EDGE_CURVE ( 'NONE', #22202, #32736, #2678, .T. ) ;
#61963=CIRCLE ( 'NONE', #33893, 0.2500000000000002220 ) ;
#61979=FACE_OUTER_BOUND ( 'NONE', #34358, .T. ) ;
#61989=ORIENTED_EDGE ( 'NONE', *, *, #65044, .F. ) ;
#61993=EDGE_LOOP ( 'NONE', ( #37124, #17084, #26479, #17230 ) ) ;
#61997=AXIS2_PLACEMENT_3D ( 'NONE', #24900, #46413, #35819 ) ;
#62008=DIRECTION ( 'NONE',  ( -0.000000000000000000, -1.000000000000000000, -0.000000000000000000 ) ) ;
#62012=ORIENTED_EDGE ( 'NONE', *, *, #3460, .T. ) ;
#62016=ORIENTED_EDGE ( 'NONE', *, *, #15043, .F. ) ;
#62027=( GEOMETRIC_REPRESENTATION_CONTEXT ( 3 ) GLOBAL_UNCERTAINTY_ASSIGNED_CONTEXT ( ( #65197 ) ) GLOBAL_UNIT_ASSIGNED_CONTEXT ( ( #40667, #1897, #45266 ) ) REPRESENTATION_CONTEXT ( 'NONE', 'WORKASPACE' ) );
#62040=CARTESIAN_POINT ( 'NONE',  ( 48.25000000000000000, 21.99999999999998579, -3.750000000000000000 ) ) ;
#62051=CARTESIAN_POINT ( 'NONE',  ( 3.749999999999999556, 33.74999999999998579, -3.750000000000000000 ) ) ;
#62073=FACE_OUTER_BOUND ( 'NONE', #35705, .T. ) ;
#62091=ADVANCED_FACE ( 'NONE', ( #23758 ), #23079, .T. ) ;
#62094=CYLINDRICAL_SURFACE ( 'NONE', #26241, 1.000000000000000888 ) ;
#62095=EDGE_CURVE ( 'NONE', #17887, #40202, #57828, .T. ) ;
#62101=EDGE_CURVE ( 'NONE', #59375, #25904, #460, .T. ) ;
#62119=CIRCLE ( 'NONE', #36374, 0.2500000000000002220 ) ;
#62127=CARTESIAN_POINT ( 'NONE',  ( 12.75000000000000533, 27.74999999999998224, -3.750000000000000000 ) ) ;
#62136=VECTOR ( 'NONE', #60851, 1000.000000000000000 ) ;
#62142=ORIENTED_EDGE ( 'NONE', *, *, #11086, .T. ) ;
#62146=DIRECTION ( 'NONE',  ( 0.000000000000000000, 0.000000000000000000, -1.000000000000000000 ) ) ;
#62191=PRESENTATION_STYLE_ASSIGNMENT (( #29837 ) ) ;
#62203=ORIENTED_EDGE ( 'NONE', *, *, #61694, .T. ) ;
#62223=CARTESIAN_POINT ( 'NONE',  ( 0.2500000000000000000, 36.74999999999999289, 4.000000000000000000 ) ) ;
#62230=CARTESIAN_POINT ( 'NONE',  ( 10.99999999999999645, 11.99999999999999289, 3.500000000000004885 ) ) ;
#62236=LINE ( 'NONE', #35523, #66258 ) ;
#62241=ORIENTED_EDGE ( 'NONE', *, *, #40681, .T. ) ;
#62242=CIRCLE ( 'NONE', #30749, 0.5000000000000004441 ) ;
#62245=CARTESIAN_POINT ( 'NONE',  ( 52.75000000000000000, 24.99999999999998579, 3.750000000000000000 ) ) ;
#62351=FACE_BOUND ( 'NONE', #16128, .T. ) ;
#62355=AXIS2_PLACEMENT_3D ( 'NONE', #44964, #24484, #50561 ) ;
#62364=ORIENTED_EDGE ( 'NONE', *, *, #54151, .T. ) ;
#62374=LINE ( 'NONE', #52541, #10832 ) ;
#62406=( NAMED_UNIT ( * ) SI_UNIT ( $, .STERADIAN. ) SOLID_ANGLE_UNIT ( ) );
#62422=CARTESIAN_POINT ( 'NONE',  ( 1.000000000000000888, 1.000000000000000222, 4.000000000000000000 ) ) ;
#62443=FACE_OUTER_BOUND ( 'NONE', #43381, .T. ) ;
#62455=CARTESIAN_POINT ( 'NONE',  ( 12.50000000000000355, 30.99999999999998579, 3.750000000000000000 ) ) ;
#62458=DIRECTION ( 'NONE',  ( -1.000000000000000000, 0.000000000000000000, 0.000000000000000000 ) ) ;
#62465=FACE_OUTER_BOUND ( 'NONE', #57892, .T. ) ;
#62498=ADVANCED_FACE ( 'NONE', ( #40936 ), #41626, .F. ) ;
#62506=CARTESIAN_POINT ( 'NONE',  ( 7.750000000000000000, 33.99999999999998579, -3.750000000000000000 ) ) ;
#62510=AXIS2_PLACEMENT_3D ( 'NONE', #32577, #21334, #27636 ) ;
#62511=ORIENTED_EDGE ( 'NONE', *, *, #7167, .F. ) ;
#62572=EDGE_CURVE ( 'NONE', #14650, #19502, #43154, .T. ) ;
#62582=EDGE_CURVE ( 'NONE', #34747, #61571, #2386, .T. ) ;
#62585=CARTESIAN_POINT ( 'NONE',  ( 12.50000000000000355, 30.99999999999998579, 4.000000000000000000 ) ) ;
#62589=FACE_OUTER_BOUND ( 'NONE', #19170, .T. ) ;
#62591=ORIENTED_EDGE ( 'NONE', *, *, #40896, .F. ) ;
#62613=CARTESIAN_POINT ( 'NONE',  ( 48.25000000000000000, 21.74999999999998579, -3.750000000000000000 ) ) ;
#62622=ORIENTED_EDGE ( 'NONE', *, *, #1057, .T. ) ;
#62630=CARTESIAN_POINT ( 'NONE',  ( 39.24999999999999289, 15.99999999999997691, 3.750000000000000000 ) ) ;
#62638=EDGE_CURVE ( 'NONE', #43970, #55156, #22885, .T. ) ;
#62650=ADVANCED_FACE ( 'NONE', ( #4835 ), #15089, .F. ) ;
#62670=ORIENTED_EDGE ( 'NONE', *, *, #25693, .T. ) ;
#62674=ORIENTED_EDGE ( 'NONE', *, *, #26564, .F. ) ;
#62691=CARTESIAN_POINT ( 'NONE',  ( 48.50000000000000000, 22.24999999999998579, -3.750000000000000000 ) ) ;
#62693=VERTEX_POINT ( 'NONE', #26618 ) ;
#62697=MECHANICAL_DESIGN_GEOMETRIC_PRESENTATION_REPRESENTATION('',(#54861),#55984);
#62704=AXIS2_PLACEMENT_3D ( 'NONE', #47686, #42051, #14571 ) ;
#62747=VECTOR ( 'NONE', #33831, 1000.000000000000000 ) ;
#62758=ORIENTED_EDGE ( 'NONE', *, *, #14563, .F. ) ;
#62785=ORIENTED_EDGE ( 'NONE', *, *, #62095, .F. ) ;
#62795=DIRECTION ( 'NONE',  ( -1.000000000000000000, 0.000000000000000000, 0.000000000000000000 ) ) ;
#62835=ORIENTED_EDGE ( 'NONE', *, *, #18590, .F. ) ;
#62838=AXIS2_PLACEMENT_3D ( 'NONE', #14585, #13891, #56812 ) ;
#62878=VERTEX_POINT ( 'NONE', #49161 ) ;
#62890=VECTOR ( 'NONE', #6689, 1000.000000000000000 ) ;
#62902=EDGE_CURVE ( 'NONE', #66069, #61310, #57772, .T. ) ;
#62929=DIRECTION ( 'NONE',  ( 5.782411586589351722E-16, -1.000000000000000000, 0.000000000000000000 ) ) ;
#62934=VERTEX_POINT ( 'NONE', #27992 ) ;
#62953=CARTESIAN_POINT ( 'NONE',  ( 16.75000000000000711, 27.74999999999998224, 3.750000000000000000 ) ) ;
#63019=DIRECTION ( 'NONE',  ( -2.312964634635740689E-15, 1.000000000000000000, 0.000000000000000000 ) ) ;
#63020=DIRECTION ( 'NONE',  ( -0.000000000000000000, 1.000000000000000000, -0.000000000000000000 ) ) ;
#63022=ORIENTED_EDGE ( 'NONE', *, *, #60988, .T. ) ;
#63040=PRODUCT_DEFINITION_SHAPE ( 'NONE', 'NONE',  #59698 ) ;
#63053=DIRECTION ( 'NONE',  ( 0.000000000000000000, 0.000000000000000000, 1.000000000000000000 ) ) ;
#63061=EDGE_LOOP ( 'NONE', ( #14869, #56390, #62785, #36874 ) ) ;
#63079=ORIENTED_EDGE ( 'NONE', *, *, #30195, .T. ) ;
#63089=CARTESIAN_POINT ( 'NONE',  ( 57.24999999999999289, 27.74999999999998934, 4.000000000000000000 ) ) ;
#63095=( NAMED_UNIT ( * ) PLANE_ANGLE_UNIT ( ) SI_UNIT ( $, .RADIAN. ) );
#63123=DIRECTION ( 'NONE',  ( 1.000000000000000000, 0.000000000000000000, 0.000000000000000000 ) ) ;
#63129=CONICAL_SURFACE ( 'NONE', #28241, 3.100000000000005418, 0.7853981633974445042 ) ;
#63136=CARTESIAN_POINT ( 'NONE',  ( 0.000000000000000000, 27.74999999999998224, 4.000000000000000000 ) ) ;
#63149=CARTESIAN_POINT ( 'NONE',  ( 68.99999999999998579, 36.75000000000000000, 4.000000000000000000 ) ) ;
#63150=DIRECTION ( 'NONE',  ( 0.000000000000000000, -0.000000000000000000, 1.000000000000000000 ) ) ;
#63153=CARTESIAN_POINT ( 'NONE',  ( 21.75000000000001066, 22.24999999999998224, 4.000000000000000000 ) ) ;
#63176=AXIS2_PLACEMENT_3D ( 'NONE', #9890, #68277, #15191 ) ;
#63179=EDGE_LOOP ( 'NONE', ( #32642, #53720, #16510, #46577, #38698, #58804, #30300, #23392, #53687, #44441, #11816, #36442, #60401, #5237, #32633, #66888, #29046, #9487, #4718, #33033, #41623, #2592, #58510, #36759, #28240, #42622, #2220, #4702, #53151, #30123, #35030, #61058, #44169, #14520, #40295, #52881, #49005, #62203, #43237, #6716, #17761, #4880, #4729, #47214, #40513, #40372 ) ) ;
#63216=EDGE_CURVE ( 'NONE', #59935, #48045, #34209, .T. ) ;
#63217=AXIS2_PLACEMENT_3D ( 'NONE', #21466, #22512, #11256 ) ;
#63238=VECTOR ( 'NONE', #32930, 1000.000000000000000 ) ;
#63247=ORIENTED_EDGE ( 'NONE', *, *, #2861, .F. ) ;
#63255=LINE ( 'NONE', #52382, #10513 ) ;
#63257=AXIS2_PLACEMENT_3D ( 'NONE', #47530, #68944, #26680 ) ;
#63259=CIRCLE ( 'NONE', #17251, 0.2500000000000002220 ) ;
#63278=( NAMED_UNIT ( * ) PLANE_ANGLE_UNIT ( ) SI_UNIT ( $, .RADIAN. ) );
#63284=ADVANCED_FACE ( 'NONE', ( #68631 ), #3882, .T. ) ;
#63295=CARTESIAN_POINT ( 'NONE',  ( 7.750000000000000000, 33.74999999999998579, -3.750000000000000000 ) ) ;
#63301=ADVANCED_FACE ( 'NONE', ( #57025 ), #35586, .T. ) ;
#63309=LINE ( 'NONE', #36631, #9339 ) ;
#63311=ORIENTED_EDGE ( 'NONE', *, *, #28307, .T. ) ;
#63368=EDGE_CURVE ( 'NONE', #32850, #27009, #16272, .T. ) ;
#63369=DIRECTION ( 'NONE',  ( -1.000000000000000000, -1.445602896647337931E-16, 0.000000000000000000 ) ) ;
#63387=EDGE_CURVE ( 'NONE', #28627, #42069, #47736, .T. ) ;
#63391=CARTESIAN_POINT ( 'NONE',  ( 3.499999999999999112, 34.24999999999998579, -4.000000000000000000 ) ) ;
#63407=CARTESIAN_POINT ( 'NONE',  ( 0.000000000000000000, 18.74999999999997868, 4.000000000000000000 ) ) ;
#63418=DIRECTION ( 'NONE',  ( 0.000000000000000000, 0.000000000000000000, -1.000000000000000000 ) ) ;
#63425=CARTESIAN_POINT ( 'NONE',  ( 66.74999999999998579, 37.00000000000000000, -3.750000000000000000 ) ) ;
#63428=DIRECTION ( 'NONE',  ( -0.000000000000000000, -0.000000000000000000, 1.000000000000000000 ) ) ;
#63436=EDGE_LOOP ( 'NONE', ( #65089, #3267, #51888 ) ) ;
#63439=AXIS2_PLACEMENT_3D ( 'NONE', #10919, #48597, #59423 ) ;
#63441=LINE ( 'NONE', #15288, #40462 ) ;
#63453=ADVANCED_FACE ( 'NONE', ( #31674 ), #30266, .T. ) ;
#63461=DIRECTION ( 'NONE',  ( -1.156482317317870344E-15, 1.000000000000000000, 0.000000000000000000 ) ) ;
#63467=EDGE_LOOP ( 'NONE', ( #21780, #52800, #46417 ) ) ;
#63483=ORIENTED_EDGE ( 'NONE', *, *, #65202, .F. ) ;
#63496=CARTESIAN_POINT ( 'NONE',  ( 68.99999999999998579, 1.000000000000008438, 3.000000000000000000 ) ) ;
#63503=DIRECTION ( 'NONE',  ( 0.000000000000000000, 0.000000000000000000, 1.000000000000000000 ) ) ;
#63519=APPLICATION_CONTEXT ( 'automotive_design' ) ;
#63539=CARTESIAN_POINT ( 'NONE',  ( 17.25000000000000711, 25.24999999999998224, 3.750000000000000000 ) ) ;
#63541=AXIS2_PLACEMENT_3D ( 'NONE', #3484, #3851, #24986 ) ;
#63542=LINE ( 'NONE', #29801, #21850 ) ;
#63553=ADVANCED_FACE ( 'NONE', ( #16231 ), #37355, .T. ) ;
#63554=DIRECTION ( 'NONE',  ( -1.000000000000000000, 0.000000000000000000, 0.000000000000000000 ) ) ;
#63563=CYLINDRICAL_SURFACE ( 'NONE', #34474, 1.000000000000000000 ) ;
#63587=FACE_OUTER_BOUND ( 'NONE', #5080, .T. ) ;
#63588=CARTESIAN_POINT ( 'NONE',  ( 26.00000000000001066, 21.74999999999998224, 4.000000000000000000 ) ) ;
#63591=ORIENTED_EDGE ( 'NONE', *, *, #32750, .F. ) ;
#63598=DIRECTION ( 'NONE',  ( -2.312964634635740689E-15, 1.000000000000000000, -0.000000000000000000 ) ) ;
#63603=ORIENTED_EDGE ( 'NONE', *, *, #12935, .T. ) ;
#63605=EDGE_CURVE ( 'NONE', #4180, #835, #47775, .T. ) ;
#63612=ADVANCED_FACE ( 'NONE', ( #64383 ), #38033, .T. ) ;
#63617=DIRECTION ( 'NONE',  ( -0.000000000000000000, 0.000000000000000000, -1.000000000000000000 ) ) ;
#63632=ORIENTED_EDGE ( 'NONE', *, *, #46362, .T. ) ;
#63633=CARTESIAN_POINT ( 'NONE',  ( 53.24999999999999289, 27.99999999999998579, -3.750000000000000000 ) ) ;
#63646=LINE ( 'NONE', #10538, #66973 ) ;
#63658=LINE ( 'NONE', #21429, #30042 ) ;
#63669=LINE ( 'NONE', #64010, #14843 ) ;
#63671=CARTESIAN_POINT ( 'NONE',  ( 68.99999999999998579, 37.00000000000000000, -3.000000000000000000 ) ) ;
#63681=ORIENTED_EDGE ( 'NONE', *, *, #9158, .F. ) ;
#63694=ADVANCED_FACE ( 'NONE', ( #56233 ), #50287, .T. ) ;
#63725=ORIENTED_EDGE ( 'NONE', *, *, #20310, .T. ) ;
#63733=AXIS2_PLACEMENT_3D ( 'NONE', #47043, #58592, #52979 ) ;
#63754=CARTESIAN_POINT ( 'NONE',  ( 12.25000000000000355, 30.74999999999998579, 3.750000000000000000 ) ) ;
#63764=ORIENTED_EDGE ( 'NONE', *, *, #33674, .F. ) ;
#63770=AXIS2_PLACEMENT_3D ( 'NONE', #31306, #47569, #68625 ) ;
#63781=ORIENTED_EDGE ( 'NONE', *, *, #47327, .F. ) ;
#63800=FILL_AREA_STYLE_COLOUR ( '', #54443 ) ;
#63815=DIRECTION ( 'NONE',  ( 0.000000000000000000, -1.000000000000000000, 0.000000000000000000 ) ) ;
#63818=CARTESIAN_POINT ( 'NONE',  ( 57.49999999999999289, 28.24999999999998934, 4.000000000000000000 ) ) ;
#63824=DIRECTION ( 'NONE',  ( 1.000000000000000000, 0.000000000000000000, -0.000000000000000000 ) ) ;
#63838=EDGE_CURVE ( 'NONE', #26540, #2804, #42144, .T. ) ;
#63843=ADVANCED_FACE ( 'NONE', ( #41146 ), #42813, .F. ) ;
#63857=DIRECTION ( 'NONE',  ( 1.000000000000000000, -0.000000000000000000, 0.000000000000000000 ) ) ;
#63881=FACE_OUTER_BOUND ( 'NONE', #58377, .T. ) ;
#63885=CARTESIAN_POINT ( 'NONE',  ( 48.25000000000000000, 22.24999999999998579, -4.000000000000000000 ) ) ;
#63901=AXIS2_PLACEMENT_3D ( 'NONE', #33259, #1167, #4610 ) ;
#63905=EDGE_CURVE ( 'NONE', #59935, #27359, #14077, .T. ) ;
#63912=CIRCLE ( 'NONE', #42634, 0.2500000000000002220 ) ;
#63913=CARTESIAN_POINT ( 'NONE',  ( 3.249999999999998668, 36.74999999999999289, -4.000000000000000000 ) ) ;
#63914=VECTOR ( 'NONE', #48331, 1000.000000000000000 ) ;
#63930=DIRECTION ( 'NONE',  ( 0.000000000000000000, 1.000000000000000000, -0.000000000000000000 ) ) ;
#63934=ORIENTED_EDGE ( 'NONE', *, *, #5307, .T. ) ;
#63942=CARTESIAN_POINT ( 'NONE',  ( 66.74999999999998579, 37.00000000000000000, -3.750000000000000000 ) ) ;
#63951=DIRECTION ( 'NONE',  ( 0.7071067811865451302, 8.659560562354903276E-17, -0.7071067811865500152 ) ) ;
#63960=CARTESIAN_POINT ( 'NONE',  ( 66.24999999999998579, 33.99999999999999289, 3.750000000000000000 ) ) ;
#63975=DIRECTION ( 'NONE',  ( -1.000000000000000000, 0.000000000000000000, 0.000000000000000000 ) ) ;
#63986=LINE ( 'NONE', #58048, #16080 ) ;
#63994=DIRECTION ( 'NONE',  ( -1.000000000000000000, 0.000000000000000000, 0.000000000000000000 ) ) ;
#64008=CARTESIAN_POINT ( 'NONE',  ( 61.99999999999998579, 33.99999999999999289, 3.750000000000000000 ) ) ;
#64010=CARTESIAN_POINT ( 'NONE',  ( 69.99999999999998579, 8.572527594031471415E-15, 3.000000000000000000 ) ) ;
#64023=CYLINDRICAL_SURFACE ( 'NONE', #295, 0.2500000000000002220 ) ;
#64044=VERTEX_POINT ( 'NONE', #16424 ) ;
#64054=DIRECTION ( 'NONE',  ( 1.000000000000000000, 0.000000000000000000, 0.000000000000000000 ) ) ;
#64063=ORIENTED_EDGE ( 'NONE', *, *, #48343, .T. ) ;
#64073=ORIENTED_EDGE ( 'NONE', *, *, #26385, .F. ) ;
#64074=EDGE_CURVE ( 'NONE', #45200, #61112, #42466, .T. ) ;
#64087=EDGE_CURVE ( 'NONE', #57077, #47284, #54351, .T. ) ;
#64088=DIRECTION ( 'NONE',  ( 0.000000000000000000, 0.000000000000000000, -1.000000000000000000 ) ) ;
#64117=DIRECTION ( 'NONE',  ( -1.000000000000000000, 0.000000000000000000, 0.000000000000000000 ) ) ;
#64124=AXIS2_PLACEMENT_3D ( 'NONE', #66447, #23879, #33732 ) ;
#64131=VERTEX_POINT ( 'NONE', #60653 ) ;
#64142=DIRECTION ( 'NONE',  ( -1.000000000000000000, 0.000000000000000000, 0.000000000000000000 ) ) ;
#64143=AXIS2_PLACEMENT_3D ( 'NONE', #22790, #18195, #54088 ) ;
#64151=VECTOR ( 'NONE', #16773, 1000.000000000000000 ) ;
#64166=VERTEX_POINT ( 'NONE', #23055 ) ;
#64187=CIRCLE ( 'NONE', #33847, 0.2500000000000002220 ) ;
#64246=EDGE_CURVE ( 'NONE', #35469, #835, #41956, .T. ) ;
#64253=DIRECTION ( 'NONE',  ( 0.000000000000000000, 0.000000000000000000, -1.000000000000000000 ) ) ;
#64254=ORIENTED_EDGE ( 'NONE', *, *, #14455, .F. ) ;
#64280=CARTESIAN_POINT ( 'NONE',  ( 12.25000000000000355, 30.99999999999998579, -3.750000000000000000 ) ) ;
#64284=CARTESIAN_POINT ( 'NONE',  ( 62.59999999999998721, 11.99999999999999822, -4.000000000000000000 ) ) ;
#64294=CARTESIAN_POINT ( 'NONE',  ( 1.000000000000000000, 36.74999999999999289, 3.000000000000000000 ) ) ;
#64303=CYLINDRICAL_SURFACE ( 'NONE', #24820, 0.2500000000000002220 ) ;
#64331=ORIENTED_EDGE ( 'NONE', *, *, #42127, .T. ) ;
#64340=DIRECTION ( 'NONE',  ( 0.000000000000000000, -1.000000000000000000, 0.000000000000000000 ) ) ;
#64341=ORIENTED_EDGE ( 'NONE', *, *, #12721, .T. ) ;
#64343=SURFACE_SIDE_STYLE ('',( #32322 ) ) ;
#64350=SPHERICAL_SURFACE ( 'NONE', #69381, 0.2500000000000000000 ) ;
#64383=FACE_OUTER_BOUND ( 'NONE', #22107, .T. ) ;
#64388=FACE_OUTER_BOUND ( 'NONE', #23505, .T. ) ;
#64405=ADVANCED_FACE ( 'NONE', ( #52495 ), #37375, .T. ) ;
#64444=AXIS2_PLACEMENT_3D ( 'NONE', #7722, #18296, #44720 ) ;
#64445=CARTESIAN_POINT ( 'NONE',  ( 59.00000000000000000, 11.99999999999999822, -4.000000000000000000 ) ) ;
#64447=LINE ( 'NONE', #42688, #31766 ) ;
#64450=AXIS2_PLACEMENT_3D ( 'NONE', #62585, #67894, #62929 ) ;
#64451=FACE_OUTER_BOUND ( 'NONE', #20655, .T. ) ;
#64465=DIRECTION ( 'NONE',  ( 0.000000000000000000, 0.000000000000000000, 1.000000000000000000 ) ) ;
#64474=AXIS2_PLACEMENT_3D ( 'NONE', #14841, #58097, #47590 ) ;
#64483=CIRCLE ( 'NONE', #52154, 0.5000000000000004441 ) ;
#64501=DIRECTION ( 'NONE',  ( 1.000000000000000000, 0.000000000000000000, 0.000000000000000000 ) ) ;
#64511=AXIS2_PLACEMENT_3D ( 'NONE', #49159, #48136, #181 ) ;
#64517=CARTESIAN_POINT ( 'NONE',  ( 57.24999999999999289, 27.99999999999998934, -4.000000000000000000 ) ) ;
#64539=ORIENTED_EDGE ( 'NONE', *, *, #15369, .F. ) ;
#64544=CARTESIAN_POINT ( 'NONE',  ( 53.25000000000000000, 25.24999999999998579, -3.750000000000000000 ) ) ;
#64590=FACE_OUTER_BOUND ( 'NONE', #34155, .T. ) ;
#64591=CARTESIAN_POINT ( 'NONE',  ( 16.75000000000000711, 27.99999999999998224, -3.750000000000000000 ) ) ;
#64610=DIRECTION ( 'NONE',  ( -0.000000000000000000, 0.000000000000000000, -1.000000000000000000 ) ) ;
#64626=CARTESIAN_POINT ( 'NONE',  ( 68.99999999999998579, 1.000000000000008438, -3.000000000000000000 ) ) ;
#64628=FACE_OUTER_BOUND ( 'NONE', #43457, .T. ) ;
#64634=ORIENTED_EDGE ( 'NONE', *, *, #5778, .T. ) ;
#64637=DIRECTION ( 'NONE',  ( 2.312964634635740689E-15, -1.000000000000000000, 0.000000000000000000 ) ) ;
#64639=VECTOR ( 'NONE', #43518, 1000.000000000000000 ) ;
#64679=ORIENTED_EDGE ( 'NONE', *, *, #38955, .T. ) ;
#64695=AXIS2_PLACEMENT_3D ( 'NONE', #912, #38338, #39703 ) ;
#64698=CARTESIAN_POINT ( 'NONE',  ( 30.50000000000001066, 15.99999999999997691, 4.000000000000000000 ) ) ;
#64701=SURFACE_STYLE_USAGE ( .BOTH. , #64343 ) ;
#64709=CIRCLE ( 'NONE', #36688, 3.100000000000005418 ) ;
#64721=ORIENTED_EDGE ( 'NONE', *, *, #11826, .F. ) ;
#64726=LINE ( 'NONE', #27055, #60687 ) ;
#64739=ADVANCED_FACE ( 'NONE', ( #19626 ), #35813, .F. ) ;
#64743=AXIS2_PLACEMENT_3D ( 'NONE', #6208, #53374, #49147 ) ;
#64747=DIRECTION ( 'NONE',  ( 1.000000000000000000, 0.000000000000000000, 0.000000000000000000 ) ) ;
#64759=ORIENTED_EDGE ( 'NONE', *, *, #38614, .F. ) ;
#64761=CARTESIAN_POINT ( 'NONE',  ( 3.249999999999998668, 36.74999999999999289, -3.750000000000000000 ) ) ;
#64772=ORIENTED_EDGE ( 'NONE', *, *, #36584, .T. ) ;
#64778=ORIENTED_EDGE ( 'NONE', *, *, #59817, .F. ) ;
#64789=DIRECTION ( 'NONE',  ( 1.000000000000000000, 0.000000000000000000, 0.000000000000000000 ) ) ;
#64812=VERTEX_POINT ( 'NONE', #42189 ) ;
#64815=DIRECTION ( 'NONE',  ( -0.000000000000000000, -0.000000000000000000, 1.000000000000000000 ) ) ;
#64819=EDGE_CURVE ( 'NONE', #4261, #2790, #69220, .T. ) ;
#64830=DIRECTION ( 'NONE',  ( 1.000000000000000000, -0.000000000000000000, 0.000000000000000000 ) ) ;
#64832=ORIENTED_EDGE ( 'NONE', *, *, #32331, .F. ) ;
#64842=( NAMED_UNIT ( * ) SI_UNIT ( $, .STERADIAN. ) SOLID_ANGLE_UNIT ( ) );
#64844=DIRECTION ( 'NONE',  ( -5.782411586589351722E-16, 1.000000000000000000, 0.000000000000000000 ) ) ;
#64886=ADVANCED_FACE ( 'NONE', ( #64628 ), #60371, .T. ) ;
#64896=ORIENTED_EDGE ( 'NONE', *, *, #15074, .T. ) ;
#64900=UNCERTAINTY_MEASURE_WITH_UNIT (LENGTH_MEASURE( 1.000000000000000082E-05 ), #9615, 'distance_accuracy_value', 'NONE');
#64912=TOROIDAL_SURFACE ( 'NONE', #61531, 0.5000000000000000000, 0.2500000000000000000 ) ;
#64921=CARTESIAN_POINT ( 'NONE',  ( 30.25000000000001066, 16.24999999999997513, -4.000000000000000000 ) ) ;
#64923=DIRECTION ( 'NONE',  ( 0.000000000000000000, -0.000000000000000000, 1.000000000000000000 ) ) ;
#64928=FACE_OUTER_BOUND ( 'NONE', #26351, .T. ) ;
#64962=CARTESIAN_POINT ( 'NONE',  ( 44.00000000000000000, 18.99999999999998224, 4.000000000000000000 ) ) ;
#64963=EDGE_CURVE ( 'NONE', #37864, #46687, #48839, .T. ) ;
#64968=CARTESIAN_POINT ( 'NONE',  ( 17.00000000000000711, 27.99999999999998224, 3.750000000000000000 ) ) ;
#64978=DIRECTION ( 'NONE',  ( 0.000000000000000000, 0.000000000000000000, 1.000000000000000000 ) ) ;
#64994=CIRCLE ( 'NONE', #25688, 0.2500000000000002220 ) ;
#65004=ORIENTED_EDGE ( 'NONE', *, *, #69432, .F. ) ;
#65011=EDGE_CURVE ( 'NONE', #14417, #67683, #20957, .T. ) ;
#65044=EDGE_CURVE ( 'NONE', #61571, #4261, #67046, .T. ) ;
#65061=VECTOR ( 'NONE', #21137, 1000.000000000000000 ) ;
#65078=ORIENTED_EDGE ( 'NONE', *, *, #3034, .T. ) ;
#65089=ORIENTED_EDGE ( 'NONE', *, *, #21781, .F. ) ;
#65114=DIRECTION ( 'NONE',  ( 0.000000000000000000, 0.000000000000000000, -1.000000000000000000 ) ) ;
#65125=ORIENTED_EDGE ( 'NONE', *, *, #26488, .F. ) ;
#65154=AXIS2_PLACEMENT_3D ( 'NONE', #50155, #44894, #49798 ) ;
#65155=AXIS2_PLACEMENT_3D ( 'NONE', #44357, #27410, #39067 ) ;
#65158=CARTESIAN_POINT ( 'NONE',  ( 7.750000000000000000, 33.74999999999998579, -4.000000000000000000 ) ) ;
#65166=VECTOR ( 'NONE', #54517, 1000.000000000000000 ) ;
#65174=CARTESIAN_POINT ( 'NONE',  ( 44.25000000000000000, 21.74999999999998579, 3.750000000000000000 ) ) ;
#65185=CARTESIAN_POINT ( 'NONE',  ( 8.250000000000001776, 30.99999999999998579, -3.750000000000000000 ) ) ;
#65187=VECTOR ( 'NONE', #10132, 1000.000000000000000 ) ;
#65195=CIRCLE ( 'NONE', #31665, 0.2500000000000002220 ) ;
#65197=UNCERTAINTY_MEASURE_WITH_UNIT (LENGTH_MEASURE( 1.000000000000000082E-05 ), #40667, 'distance_accuracy_value', 'NONE');
#65202=EDGE_CURVE ( 'NONE', #18309, #11647, #5208, .T. ) ;
#65217=ORIENTED_EDGE ( 'NONE', *, *, #6203, .F. ) ;
#65218=CARTESIAN_POINT ( 'NONE',  ( 48.74999999999999289, 24.74999999999998579, -4.000000000000000000 ) ) ;
#65235=CARTESIAN_POINT ( 'NONE',  ( 68.99999999999998579, 36.75000000000000000, -3.000000000000000000 ) ) ;
#65245=DIRECTION ( 'NONE',  ( 0.000000000000000000, -1.000000000000000000, 0.000000000000000000 ) ) ;
#65250=CIRCLE ( 'NONE', #39483, 0.2500000000000002220 ) ;
#65258=AXIS2_PLACEMENT_3D ( 'NONE', #38601, #38245, #44224 ) ;
#65266=EDGE_CURVE ( 'NONE', #10058, #28793, #53636, .T. ) ;
#65272=ORIENTED_EDGE ( 'NONE', *, *, #59722, .T. ) ;
#65280=DIRECTION ( 'NONE',  ( -1.000000000000000000, 0.000000000000000000, 0.000000000000000000 ) ) ;
#65284=DIRECTION ( 'NONE',  ( -1.000000000000000000, 0.000000000000000000, 0.000000000000000000 ) ) ;
#65299=DIRECTION ( 'NONE',  ( -1.224646799147353207E-16, 1.000000000000000000, 0.000000000000000000 ) ) ;
#65312=DIRECTION ( 'NONE',  ( -1.000000000000000000, 0.000000000000000000, 0.000000000000000000 ) ) ;
#65316=AXIS2_PLACEMENT_3D ( 'NONE', #56097, #55405, #18131 ) ;
#65321=CARTESIAN_POINT ( 'NONE',  ( 39.24999999999999289, 15.99999999999997691, -4.000000000000000000 ) ) ;
#65325=DIRECTION ( 'NONE',  ( 0.000000000000000000, 0.000000000000000000, -1.000000000000000000 ) ) ;
#65328=AXIS2_PLACEMENT_3D ( 'NONE', #23964, #40880, #67945 ) ;
#65335=AXIS2_PLACEMENT_3D ( 'NONE', #30165, #35816, #30871 ) ;
#65336=LINE ( 'NONE', #35418, #68298 ) ;
#65341=CARTESIAN_POINT ( 'NONE',  ( 30.25000000000001066, 16.24999999999997513, -4.000000000000000000 ) ) ;
#65345=LINE ( 'NONE', #29433, #27059 ) ;
#65348=EDGE_CURVE ( 'NONE', #33237, #18309, #19731, .T. ) ;
#65392=( GEOMETRIC_REPRESENTATION_CONTEXT ( 3 ) GLOBAL_UNCERTAINTY_ASSIGNED_CONTEXT ( ( #11737 ) ) GLOBAL_UNIT_ASSIGNED_CONTEXT ( ( #10034, #4734, #41718 ) ) REPRESENTATION_CONTEXT ( 'NONE', 'WORKASPACE' ) );
#65411=VERTEX_POINT ( 'NONE', #48232 ) ;
#65424=ORIENTED_EDGE ( 'NONE', *, *, #42098, .F. ) ;
#65428=FACE_OUTER_BOUND ( 'NONE', #40407, .T. ) ;
#65436=DIRECTION ( 'NONE',  ( -1.000000000000000000, 0.000000000000000000, 0.000000000000000000 ) ) ;
#65439=EDGE_CURVE ( 'NONE', #18810, #39701, #32233, .T. ) ;
#65448=VERTEX_POINT ( 'NONE', #42971 ) ;
#65450=CIRCLE ( 'NONE', #248, 3.599999999999992095 ) ;
#65451=DIRECTION ( 'NONE',  ( 0.000000000000000000, -1.000000000000000000, 0.000000000000000000 ) ) ;
#65456=EDGE_CURVE ( 'NONE', #28382, #47284, #36804, .T. ) ;
#65461=CARTESIAN_POINT ( 'NONE',  ( 55.39999999999999147, 11.99999999999999822, 4.000000000000000000 ) ) ;
#65495=CARTESIAN_POINT ( 'NONE',  ( 1.000000000000000000, 1.000000000000000222, -3.000000000000000000 ) ) ;
#65496=AXIS2_PLACEMENT_3D ( 'NONE', #9796, #41827, #58650 ) ;
#65505=DIRECTION ( 'NONE',  ( 0.000000000000000000, 1.000000000000000000, 0.000000000000000000 ) ) ;
#65523=ADVANCED_FACE ( 'NONE', ( #59414 ), #37347, .T. ) ;
#65554=DIRECTION ( 'NONE',  ( 1.000000000000000000, -0.000000000000000000, -0.000000000000000000 ) ) ;
#65584=DIRECTION ( 'NONE',  ( 0.000000000000000000, -1.000000000000000000, 0.000000000000000000 ) ) ;
#65588=CARTESIAN_POINT ( 'NONE',  ( 62.24999999999998579, 33.99999999999999289, 4.000000000000000000 ) ) ;
#65597=FACE_OUTER_BOUND ( 'NONE', #67377, .T. ) ;
#65603=EDGE_CURVE ( 'NONE', #41177, #9969, #67136, .T. ) ;
#65609=CARTESIAN_POINT ( 'NONE',  ( 57.75000000000005684, 1.335737076502141715E-13, 4.000000000000000000 ) ) ;
#65629=CARTESIAN_POINT ( 'NONE',  ( 3.499999999999998668, 36.74999999999999289, 3.750000000000000000 ) ) ;
#65648=LINE ( 'NONE', #12162, #41493 ) ;
#65663=CARTESIAN_POINT ( 'NONE',  ( 21.25000000000000711, 22.24999999999998224, -3.750000000000000000 ) ) ;
#65666=VERTEX_POINT ( 'NONE', #3413 ) ;
#65668=EDGE_CURVE ( 'NONE', #25571, #19536, #51312, .T. ) ;
#65686=EDGE_CURVE ( 'NONE', #62934, #19236, #16604, .T. ) ;
#65720=DIRECTION ( 'NONE',  ( 0.000000000000000000, 0.000000000000000000, -1.000000000000000000 ) ) ;
#65740=DIRECTION ( 'NONE',  ( -1.000000000000000000, 0.000000000000000000, 0.000000000000000000 ) ) ;
#65745=DIRECTION ( 'NONE',  ( 0.000000000000000000, 0.000000000000000000, 1.000000000000000000 ) ) ;
#65751=EDGE_CURVE ( 'NONE', #4180, #57518, #40096, .T. ) ;
#65758=EDGE_CURVE ( 'NONE', #46687, #47709, #46419, .T. ) ;
#65762=CYLINDRICAL_SURFACE ( 'NONE', #65155, 0.2500000000000002220 ) ;
#65763=FACE_OUTER_BOUND ( 'NONE', #24425, .T. ) ;
#65802=DIRECTION ( 'NONE',  ( 0.000000000000000000, 0.000000000000000000, 1.000000000000000000 ) ) ;
#65808=VECTOR ( 'NONE', #6020, 1000.000000000000000 ) ;
#65816=CARTESIAN_POINT ( 'NONE',  ( 68.99999999999998579, 36.75000000000000000, 3.000000000000000000 ) ) ;
#65832=ORIENTED_EDGE ( 'NONE', *, *, #47973, .T. ) ;
#65853=CARTESIAN_POINT ( 'NONE',  ( 30.75000000000001066, 15.99999999999997691, 3.750000000000000000 ) ) ;
#65872=FACE_OUTER_BOUND ( 'NONE', #65993, .T. ) ;
#65874=ORIENTED_EDGE ( 'NONE', *, *, #31348, .T. ) ;
#65889=ORIENTED_EDGE ( 'NONE', *, *, #27283, .T. ) ;
#65920=ADVANCED_FACE ( 'NONE', ( #21028 ), #34540, .T. ) ;
#65938=DIRECTION ( 'NONE',  ( 0.000000000000000000, 0.000000000000000000, -1.000000000000000000 ) ) ;
#65947=CARTESIAN_POINT ( 'NONE',  ( 57.24999999999999289, 27.99999999999998934, 3.750000000000000000 ) ) ;
#65958=DIRECTION ( 'NONE',  ( 1.000000000000000000, 7.709882115452468306E-16, -0.000000000000000000 ) ) ;
#65960=LINE ( 'NONE', #45242, #54057 ) ;
#65963=CARTESIAN_POINT ( 'NONE',  ( 59.00000000000000000, 11.99999999999999822, -4.000000000000000000 ) ) ;
#65982=EDGE_CURVE ( 'NONE', #34547, #4261, #60042, .T. ) ;
#65986=ORIENTED_EDGE ( 'NONE', *, *, #40775, .T. ) ;
#65988=DIRECTION ( 'NONE',  ( 0.000000000000000000, 0.000000000000000000, -1.000000000000000000 ) ) ;
#65990=EDGE_CURVE ( 'NONE', #6607, #59022, #17747, .T. ) ;
#65993=EDGE_LOOP ( 'NONE', ( #42996, #44721, #50861 ) ) ;
#65996=VERTEX_POINT ( 'NONE', #9016 ) ;
#66005=EDGE_CURVE ( 'NONE', #5374, #32655, #8744, .T. ) ;
#66007=ORIENTED_EDGE ( 'NONE', *, *, #57205, .F. ) ;
#66013=LINE ( 'NONE', #17840, #15654 ) ;
#66033=AXIS2_PLACEMENT_3D ( 'NONE', #2837, #29250, #7471 ) ;
#66053=DIRECTION ( 'NONE',  ( -1.000000000000000000, 0.000000000000000000, 0.000000000000000000 ) ) ;
#66069=VERTEX_POINT ( 'NONE', #8669 ) ;
#66071=ADVANCED_FACE ( 'NONE', ( #62465 ), #64912, .T. ) ;
#66087=ORIENTED_EDGE ( 'NONE', *, *, #30604, .T. ) ;
#66089=DIRECTION ( 'NONE',  ( -1.000000000000000000, 0.000000000000000000, 0.000000000000000000 ) ) ;
#66113=DIRECTION ( 'NONE',  ( 0.000000000000000000, 1.000000000000000000, -0.000000000000000000 ) ) ;
#66129=CIRCLE ( 'NONE', #37027, 3.100000000000005418 ) ;
#66139=EDGE_LOOP ( 'NONE', ( #45438, #36621, #13796, #36988 ) ) ;
#66144=CARTESIAN_POINT ( 'NONE',  ( 21.25000000000000711, 22.24999999999998224, -4.000000000000000000 ) ) ;
#66154=ADVANCED_FACE ( 'NONE', ( #52298 ), #5107, .T. ) ;
#66184=DIRECTION ( 'NONE',  ( -1.000000000000000000, 0.000000000000000000, 0.000000000000000000 ) ) ;
#66205=CIRCLE ( 'NONE', #7815, 0.2500000000000002220 ) ;
#66206=CIRCLE ( 'NONE', #50512, 0.2500000000000002220 ) ;
#66211=CARTESIAN_POINT ( 'NONE',  ( 3.250000000000003553, 4.698209414103854191E-16, 4.000000000000000000 ) ) ;
#66215=ORIENTED_EDGE ( 'NONE', *, *, #33921, .T. ) ;
#66248=TOROIDAL_SURFACE ( 'NONE', #28010, 0.5000000000000000000, 0.2500000000000000000 ) ;
#66258=VECTOR ( 'NONE', #30205, 1000.000000000000000 ) ;
#66260=VECTOR ( 'NONE', #54868, 1000.000000000000000 ) ;
#66277=DIRECTION ( 'NONE',  ( 0.000000000000000000, 1.000000000000000000, 0.000000000000000000 ) ) ;
#66280=DIRECTION ( 'NONE',  ( -0.000000000000000000, 0.000000000000000000, -1.000000000000000000 ) ) ;
#66287=VECTOR ( 'NONE', #69573, 1000.000000000000000 ) ;
#66331=DIRECTION ( 'NONE',  ( -1.000000000000000000, 0.000000000000000000, 0.000000000000000000 ) ) ;
#66332=ORIENTED_EDGE ( 'NONE', *, *, #44149, .F. ) ;
#66334=DIRECTION ( 'NONE',  ( 1.000000000000000000, -0.000000000000000000, 0.000000000000000000 ) ) ;
#66341=DIRECTION ( 'NONE',  ( 5.782411586589351722E-16, -1.000000000000000000, -0.000000000000000000 ) ) ;
#66379=DIRECTION ( 'NONE',  ( 0.000000000000000000, -0.000000000000000000, 1.000000000000000000 ) ) ;
#66399=ORIENTED_EDGE ( 'NONE', *, *, #64074, .T. ) ;
#66447=CARTESIAN_POINT ( 'NONE',  ( 59.00000000000000000, 11.99999999999999822, 3.499999999999992895 ) ) ;
#66449=CYLINDRICAL_SURFACE ( 'NONE', #34089, 0.2500000000000002220 ) ;
#66451=ORIENTED_EDGE ( 'NONE', *, *, #42127, .F. ) ;
#66460=CARTESIAN_POINT ( 'NONE',  ( 0.000000000000000000, 30.74999999999999289, 3.750000000000000000 ) ) ;
#66466=DIRECTION ( 'NONE',  ( -1.000000000000000000, 0.000000000000000000, 0.000000000000000000 ) ) ;
#66468=DIRECTION ( 'NONE',  ( -0.000000000000000000, -0.000000000000000000, 1.000000000000000000 ) ) ;
#66472=EDGE_CURVE ( 'NONE', #18083, #43779, #1979, .T. ) ;
#66474=DIRECTION ( 'NONE',  ( 0.000000000000000000, 0.000000000000000000, -1.000000000000000000 ) ) ;
#66489=ORIENTED_EDGE ( 'NONE', *, *, #67026, .F. ) ;
#66490=LINE ( 'NONE', #8092, #22046 ) ;
#66501=ORIENTED_EDGE ( 'NONE', *, *, #56938, .F. ) ;
#66502=CARTESIAN_POINT ( 'NONE',  ( 53.24999999999999289, 27.74999999999998579, 3.750000000000000000 ) ) ;
#66503=EDGE_LOOP ( 'NONE', ( #56961, #57071, #6534 ) ) ;
#66505=CARTESIAN_POINT ( 'NONE',  ( 12.75000000000000533, 28.24999999999998224, 4.000000000000000000 ) ) ;
#66521=ORIENTED_EDGE ( 'NONE', *, *, #46929, .F. ) ;
#66525=PLANE ( 'NONE',  #52785 ) ;
#66535=LINE ( 'NONE', #11406, #57260 ) ;
#66547=AXIS2_PLACEMENT_3D ( 'NONE', #63754, #31388, #52886 ) ;
#66569=ORIENTED_EDGE ( 'NONE', *, *, #63905, .F. ) ;
#66579=CYLINDRICAL_SURFACE ( 'NONE', #2659, 0.2500000000000002220 ) ;
#66647=CARTESIAN_POINT ( 'NONE',  ( 12.50000000000000533, 27.99999999999998224, 4.000000000000000000 ) ) ;
#66732=CARTESIAN_POINT ( 'NONE',  ( 44.00000000000000000, 19.24999999999998224, -3.750000000000000000 ) ) ;
#66753=DIRECTION ( 'NONE',  ( -1.000000000000000000, 0.000000000000000000, 0.000000000000000000 ) ) ;
#66760=CIRCLE ( 'NONE', #21833, 0.2500000000000002220 ) ;
#66771=EDGE_LOOP ( 'NONE', ( #42638, #49974, #8033 ) ) ;
#66793=CARTESIAN_POINT ( 'NONE',  ( 53.25000000000000000, 25.24999999999998579, 3.750000000000000000 ) ) ;
#66794=CARTESIAN_POINT ( 'NONE',  ( 8.250000000000001776, 30.74999999999998579, -3.750000000000000000 ) ) ;
#66803=VERTEX_POINT ( 'NONE', #45815 ) ;
#66810=ORIENTED_EDGE ( 'NONE', *, *, #27934, .F. ) ;
#66811=EDGE_CURVE ( 'NONE', #37989, #14037, #3210, .T. ) ;
#66814=LINE ( 'NONE', #23208, #3121 ) ;
#66838=DIRECTION ( 'NONE',  ( -0.000000000000000000, 1.000000000000000000, -0.000000000000000000 ) ) ;
#66846=ORIENTED_EDGE ( 'NONE', *, *, #5707, .F. ) ;
#66847=ORIENTED_EDGE ( 'NONE', *, *, #27124, .F. ) ;
#66859=AXIS2_PLACEMENT_3D ( 'NONE', #54509, #16576, #53490 ) ;
#66861=DIRECTION ( 'NONE',  ( 0.000000000000000000, 0.000000000000000000, -1.000000000000000000 ) ) ;
#66872=FACE_OUTER_BOUND ( 'NONE', #50577, .T. ) ;
#66881=EDGE_CURVE ( 'NONE', #64131, #28127, #18010, .T. ) ;
#66888=ORIENTED_EDGE ( 'NONE', *, *, #51295, .T. ) ;
#66892=DIRECTION ( 'NONE',  ( -0.000000000000000000, -0.000000000000000000, 1.000000000000000000 ) ) ;
#66901=EDGE_CURVE ( 'NONE', #69157, #23317, #12366, .T. ) ;
#66904=AXIS2_PLACEMENT_3D ( 'NONE', #39315, #34684, #61750 ) ;
#66910=DIRECTION ( 'NONE',  ( 0.000000000000000000, 0.000000000000000000, -1.000000000000000000 ) ) ;
#66936=CARTESIAN_POINT ( 'NONE',  ( 12.25000000000002132, 7.083454193571968087E-15, 4.000000000000000000 ) ) ;
#66938=EDGE_LOOP ( 'NONE', ( #15175, #63247, #69281, #50428 ) ) ;
#66944=CARTESIAN_POINT ( 'NONE',  ( 0.000000000000000000, 30.74999999999998579, 4.000000000000000000 ) ) ;
#66948=FACE_OUTER_BOUND ( 'NONE', #47545, .T. ) ;
#66956=AXIS2_PLACEMENT_3D ( 'NONE', #10889, #42271, #16545 ) ;
#66967=CARTESIAN_POINT ( 'NONE',  ( 69.99999999999998579, 8.572527594031471415E-15, 3.000000000000000000 ) ) ;
#66973=VECTOR ( 'NONE', #15153, 1000.000000000000000 ) ;
#66980=CARTESIAN_POINT ( 'NONE',  ( 17.00000000000000711, 27.99999999999998224, 4.000000000000000000 ) ) ;
#67005=MECHANICAL_DESIGN_GEOMETRIC_PRESENTATION_REPRESENTATION('',(#53545),#68159);
#67026=EDGE_CURVE ( 'NONE', #31792, #25558, #53666, .T. ) ;
#67027=DIRECTION ( 'NONE',  ( -0.000000000000000000, -0.000000000000000000, 1.000000000000000000 ) ) ;
#67033=EDGE_CURVE ( 'NONE', #54480, #21322, #25584, .T. ) ;
#67046=CIRCLE ( 'NONE', #43500, 0.2500000000000002220 ) ;
#67092=ORIENTED_EDGE ( 'NONE', *, *, #61308, .T. ) ;
#67093=CARTESIAN_POINT ( 'NONE',  ( 48.49999999999999289, 24.99999999999998579, 3.750000000000000000 ) ) ;
#67106=VERTEX_POINT ( 'NONE', #11868 ) ;
#67120=DIRECTION ( 'NONE',  ( 0.000000000000000000, 0.000000000000000000, 1.000000000000000000 ) ) ;
#67123=EDGE_LOOP ( 'NONE', ( #55007, #46826, #40241, #5338 ) ) ;
#67134=CIRCLE ( 'NONE', #43588, 0.2500000000000002220 ) ;
#67135=ORIENTED_EDGE ( 'NONE', *, *, #55269, .T. ) ;
#67136=CIRCLE ( 'NONE', #30026, 3.600000000000005862 ) ;
#67147=EDGE_CURVE ( 'NONE', #4422, #45200, #65336, .T. ) ;
#67149=EDGE_LOOP ( 'NONE', ( #64721, #40942, #25387 ) ) ;
#67187=ORIENTED_EDGE ( 'NONE', *, *, #11122, .T. ) ;
#67188=CARTESIAN_POINT ( 'NONE',  ( 44.25000000000000000, 21.99999999999998579, -3.750000000000000000 ) ) ;
#67192=LINE ( 'NONE', #19698, #23091 ) ;
#67204=AXIS2_PLACEMENT_3D ( 'NONE', #3985, #46967, #33 ) ;
#67212=DIRECTION ( 'NONE',  ( 0.000000000000000000, -1.000000000000000000, 0.000000000000000000 ) ) ;
#67238=CARTESIAN_POINT ( 'NONE',  ( 1.000000000000000000, 1.000000000000000222, -3.000000000000000000 ) ) ;
#67272=CIRCLE ( 'NONE', #23471, 0.2500000000000002220 ) ;
#67298=ORIENTED_EDGE ( 'NONE', *, *, #5886, .F. ) ;
#67310=FACE_BOUND ( 'NONE', #5946, .T. ) ;
#67326=DIRECTION ( 'NONE',  ( -1.000000000000000000, 0.000000000000000000, 0.000000000000000000 ) ) ;
#67346=DIRECTION ( 'NONE',  ( 0.000000000000000000, 0.000000000000000000, -1.000000000000000000 ) ) ;
#67349=AXIS2_PLACEMENT_3D ( 'NONE', #10753, #32200, #53647 ) ;
#67361=EDGE_CURVE ( 'NONE', #34747, #2790, #41329, .T. ) ;
#67377=EDGE_LOOP ( 'NONE', ( #60669, #35906, #68349, #31675 ) ) ;
#67422=AXIS2_PLACEMENT_3D ( 'NONE', #48790, #42828, #69174 ) ;
#67434=DIRECTION ( 'NONE',  ( -0.000000000000000000, -0.000000000000000000, 1.000000000000000000 ) ) ;
#67439=ORIENTED_EDGE ( 'NONE', *, *, #58166, .F. ) ;
#67444=CARTESIAN_POINT ( 'NONE',  ( 61.74999999999998579, 30.74999999999999289, 3.750000000000000000 ) ) ;
#67453=VERTEX_POINT ( 'NONE', #65947 ) ;
#67457=CARTESIAN_POINT ( 'NONE',  ( 39.74999999999999289, 16.24999999999997513, -3.750000000000000000 ) ) ;
#67459=ORIENTED_EDGE ( 'NONE', *, *, #32392, .F. ) ;
#67525=DIRECTION ( 'NONE',  ( -1.000000000000000000, -7.709882115452469292E-16, 0.000000000000000000 ) ) ;
#67549=DIRECTION ( 'NONE',  ( 0.000000000000000000, 0.000000000000000000, -1.000000000000000000 ) ) ;
#67560=ORIENTED_EDGE ( 'NONE', *, *, #32228, .T. ) ;
#67570=AXIS2_PLACEMENT_3D ( 'NONE', #22781, #38996, #60389 ) ;
#67577=ORIENTED_EDGE ( 'NONE', *, *, #25950, .T. ) ;
#67584=ADVANCED_FACE ( 'NONE', ( #36757 ), #58173, .F. ) ;
#67605=ADVANCED_FACE ( 'NONE', ( #57471 ), #36415, .T. ) ;
#67623=CARTESIAN_POINT ( 'NONE',  ( 14.60000000000000142, 11.99999999999999289, -4.000000000000000000 ) ) ;
#67668=FACE_OUTER_BOUND ( 'NONE', #55527, .T. ) ;
#67672=DIRECTION ( 'NONE',  ( 0.000000000000000000, 0.000000000000000000, -1.000000000000000000 ) ) ;
#67683=VERTEX_POINT ( 'NONE', #6759 ) ;
#67686=EDGE_CURVE ( 'NONE', #14650, #34547, #43437, .T. ) ;
#67691=EDGE_CURVE ( 'NONE', #14431, #30410, #54607, .T. ) ;
#67696=CARTESIAN_POINT ( 'NONE',  ( 57.49999999999999289, 27.99999999999998934, 4.000000000000000000 ) ) ;
#67717=CARTESIAN_POINT ( 'NONE',  ( 26.00000000000001066, 18.74999999999997868, -3.750000000000000000 ) ) ;
#67738=ORIENTED_EDGE ( 'NONE', *, *, #45487, .F. ) ;
#67743=CARTESIAN_POINT ( 'NONE',  ( 0.000000000000000000, 15.74999999999997513, 3.750000000000000000 ) ) ;
#67750=CARTESIAN_POINT ( 'NONE',  ( 66.74999999999998579, 36.75000000000000000, -3.750000000000000000 ) ) ;
#67781=CARTESIAN_POINT ( 'NONE',  ( 26.25000000000001066, 19.24999999999997868, 3.750000000000000000 ) ) ;
#67784=DIRECTION ( 'NONE',  ( -0.000000000000000000, -0.000000000000000000, 1.000000000000000000 ) ) ;
#67837=EDGE_CURVE ( 'NONE', #32655, #57077, #26709, .T. ) ;
#67839=DIRECTION ( 'NONE',  ( -0.000000000000000000, 0.000000000000000000, -1.000000000000000000 ) ) ;
#67847=ORIENTED_EDGE ( 'NONE', *, *, #1504, .T. ) ;
#67891=CARTESIAN_POINT ( 'NONE',  ( 8.250000000000001776, 31.24999999999998579, 4.000000000000000000 ) ) ;
#67894=DIRECTION ( 'NONE',  ( -1.000000000000000000, -5.782411586589351722E-16, 0.000000000000000000 ) ) ;
#67900=ORIENTED_EDGE ( 'NONE', *, *, #48728, .T. ) ;
#67922=DIRECTION ( 'NONE',  ( -5.782411586589351722E-16, 1.000000000000000000, 0.000000000000000000 ) ) ;
#67943=VERTEX_POINT ( 'NONE', #54158 ) ;
#67945=DIRECTION ( 'NONE',  ( -1.000000000000000000, 0.000000000000000000, 0.000000000000000000 ) ) ;
#67974=DIRECTION ( 'NONE',  ( 1.000000000000000000, 0.000000000000000000, 0.000000000000000000 ) ) ;
#68006=EDGE_CURVE ( 'NONE', #61112, #51828, #5271, .T. ) ;
#68028=AXIS2_PLACEMENT_3D ( 'NONE', #60004, #38607, #27271 ) ;
#68046=EDGE_CURVE ( 'NONE', #28073, #65666, #61599, .T. ) ;
#68048=AXIS2_PLACEMENT_3D ( 'NONE', #21508, #59472, #54208 ) ;
#68065=AXIS2_PLACEMENT_3D ( 'NONE', #57395, #47232, #4963 ) ;
#68088=ORIENTED_EDGE ( 'NONE', *, *, #68972, .F. ) ;
#68089=EDGE_CURVE ( 'NONE', #27009, #32736, #25666, .T. ) ;
#68094=FILL_AREA_STYLE ('',( #47010 ) ) ;
#68101=EDGE_CURVE ( 'NONE', #64166, #9969, #66814, .T. ) ;
#68102=DIRECTION ( 'NONE',  ( 1.000000000000000000, -0.000000000000000000, -0.000000000000000000 ) ) ;
#68107=CARTESIAN_POINT ( 'NONE',  ( 12.75000000000000533, 28.24999999999998224, 4.000000000000000000 ) ) ;
#68156=EDGE_LOOP ( 'NONE', ( #60315, #29076, #65078, #13554 ) ) ;
#68159=( GEOMETRIC_REPRESENTATION_CONTEXT ( 3 ) GLOBAL_UNCERTAINTY_ASSIGNED_CONTEXT ( ( #49006 ) ) GLOBAL_UNIT_ASSIGNED_CONTEXT ( ( #16538, #37668, #5576 ) ) REPRESENTATION_CONTEXT ( 'NONE', 'WORKASPACE' ) );
#68176=ORIENTED_EDGE ( 'NONE', *, *, #51876, .T. ) ;
#68226=DIRECTION ( 'NONE',  ( 0.000000000000000000, 0.000000000000000000, -1.000000000000000000 ) ) ;
#68228=CARTESIAN_POINT ( 'NONE',  ( 68.99999999999998579, 8.450062914116736267E-15, -3.000000000000000000 ) ) ;
#68244=CARTESIAN_POINT ( 'NONE',  ( 48.50000000000000000, 22.24999999999998579, 4.000000000000000000 ) ) ;
#68246=EDGE_CURVE ( 'NONE', #31871, #17336, #6618, .T. ) ;
#68262=ORIENTED_EDGE ( 'NONE', *, *, #59242, .F. ) ;
#68277=DIRECTION ( 'NONE',  ( -7.709882115452468306E-16, -1.000000000000000000, 0.000000000000000000 ) ) ;
#68289=LINE ( 'NONE', #25365, #55019 ) ;
#68293=CARTESIAN_POINT ( 'NONE',  ( 44.00000000000000000, 21.74999999999998579, 3.750000000000000000 ) ) ;
#68297=ORIENTED_EDGE ( 'NONE', *, *, #35373, .T. ) ;
#68298=VECTOR ( 'NONE', #19567, 1000.000000000000000 ) ;
#68306=ADVANCED_FACE ( 'NONE', ( #43240 ), #31575, .T. ) ;
#68319=EDGE_CURVE ( 'NONE', #14417, #68764, #47106, .T. ) ;
#68323=VERTEX_POINT ( 'NONE', #38293 ) ;
#68333=EDGE_CURVE ( 'NONE', #24476, #44314, #35822, .T. ) ;
#68338=DIRECTION ( 'NONE',  ( 0.000000000000000000, 0.000000000000000000, -1.000000000000000000 ) ) ;
#68339=FACE_OUTER_BOUND ( 'NONE', #27693, .T. ) ;
#68349=ORIENTED_EDGE ( 'NONE', *, *, #64074, .F. ) ;
#68358=ORIENTED_EDGE ( 'NONE', *, *, #55603, .F. ) ;
#68388=ORIENTED_EDGE ( 'NONE', *, *, #40463, .F. ) ;
#68419=EDGE_CURVE ( 'NONE', #64166, #24250, #66129, .T. ) ;
#68421=ORIENTED_EDGE ( 'NONE', *, *, #37719, .T. ) ;
#68423=CARTESIAN_POINT ( 'NONE',  ( 21.75000000000001066, 22.24999999999998224, -3.750000000000000000 ) ) ;
#68428=DIRECTION ( 'NONE',  ( -1.000000000000000000, 0.000000000000000000, 0.000000000000000000 ) ) ;
#68437=DIRECTION ( 'NONE',  ( -0.000000000000000000, 0.000000000000000000, -1.000000000000000000 ) ) ;
#68445=ORIENTED_EDGE ( 'NONE', *, *, #62638, .F. ) ;
#68446=AXIS2_PLACEMENT_3D ( 'NONE', #7897, #52147, #29343 ) ;
#68452=EDGE_CURVE ( 'NONE', #18083, #40281, #66013, .T. ) ;
#68514=ORIENTED_EDGE ( 'NONE', *, *, #39438, .F. ) ;
#68521=CIRCLE ( 'NONE', #20197, 0.2500000000000002220 ) ;
#68526=FACE_OUTER_BOUND ( 'NONE', #16635, .T. ) ;
#68531=CARTESIAN_POINT ( 'NONE',  ( 12.25000000000000355, 30.74999999999998579, 3.750000000000000000 ) ) ;
#68534=VERTEX_POINT ( 'NONE', #38646 ) ;
#68538=DIRECTION ( 'NONE',  ( -1.000000000000000000, 0.000000000000000000, 0.000000000000000000 ) ) ;
#68564=SURFACE_SIDE_STYLE ('',( #25621 ) ) ;
#68578=VECTOR ( 'NONE', #57063, 1000.000000000000000 ) ;
#68599=DIRECTION ( 'NONE',  ( -0.000000000000000000, -0.000000000000000000, 1.000000000000000000 ) ) ;
#68605=CARTESIAN_POINT ( 'NONE',  ( 43.75000000000000000, 18.74999999999998224, 4.000000000000000000 ) ) ;
#68610=VERTEX_POINT ( 'NONE', #37176 ) ;
#68619=CARTESIAN_POINT ( 'NONE',  ( 57.74999999999998579, 30.74999999999999289, 4.000000000000000000 ) ) ;
#68622=ORIENTED_EDGE ( 'NONE', *, *, #32750, .T. ) ;
#68625=DIRECTION ( 'NONE',  ( -1.000000000000000000, 0.000000000000000000, 0.000000000000000000 ) ) ;
#68629=EDGE_CURVE ( 'NONE', #51066, #19343, #15371, .T. ) ;
#68631=FACE_OUTER_BOUND ( 'NONE', #4981, .T. ) ;
#68636=DIRECTION ( 'NONE',  ( 0.000000000000000000, 0.000000000000000000, -1.000000000000000000 ) ) ;
#68665=CYLINDRICAL_SURFACE ( 'NONE', #58543, 0.2500000000000002220 ) ;
#68699=CIRCLE ( 'NONE', #38407, 0.2500000000000002220 ) ;
#68710=EDGE_CURVE ( 'NONE', #31245, #7454, #986, .T. ) ;
#68714=ADVANCED_FACE ( 'NONE', ( #37535 ), #58941, .T. ) ;
#68749=CARTESIAN_POINT ( 'NONE',  ( 52.99999999999999289, 27.74999999999998579, 4.000000000000000000 ) ) ;
#68753=DIRECTION ( 'NONE',  ( 0.000000000000000000, 0.000000000000000000, -1.000000000000000000 ) ) ;
#68759=EDGE_LOOP ( 'NONE', ( #39738, #55277, #29304, #56394 ) ) ;
#68764=VERTEX_POINT ( 'NONE', #25868 ) ;
#68782=VERTEX_POINT ( 'NONE', #60310 ) ;
#68787=TOROIDAL_SURFACE ( 'NONE', #11464, 0.5000000000000000000, 0.2500000000000000000 ) ;
#68789=ORIENTED_EDGE ( 'NONE', *, *, #7635, .F. ) ;
#68792=VECTOR ( 'NONE', #53291, 1000.000000000000000 ) ;
#68793=EDGE_CURVE ( 'NONE', #24621, #4102, #44869, .T. ) ;
#68807=SPHERICAL_SURFACE ( 'NONE', #2575, 0.2500000000000000000 ) ;
#68813=DIRECTION ( 'NONE',  ( 1.000000000000000000, 0.000000000000000000, -0.000000000000000000 ) ) ;
#68833=DIRECTION ( 'NONE',  ( -0.000000000000000000, -0.000000000000000000, 1.000000000000000000 ) ) ;
#68850=CIRCLE ( 'NONE', #27231, 0.2500000000000002220 ) ;
#68857=DIRECTION ( 'NONE',  ( -1.000000000000000000, 0.000000000000000000, 0.000000000000000000 ) ) ;
#68858=FACE_OUTER_BOUND ( 'NONE', #22395, .T. ) ;
#68876=EDGE_LOOP ( 'NONE', ( #59210, #21492, #46498, #51297 ) ) ;
#68885=DIRECTION ( 'NONE',  ( -0.000000000000000000, 0.000000000000000000, -1.000000000000000000 ) ) ;
#68887=CARTESIAN_POINT ( 'NONE',  ( 21.75000000000001066, 22.24999999999998224, -3.750000000000000000 ) ) ;
#68911=CIRCLE ( 'NONE', #7128, 0.5000000000000004441 ) ;
#68919=VERTEX_POINT ( 'NONE', #56780 ) ;
#68921=DIRECTION ( 'NONE',  ( -0.000000000000000000, 1.000000000000000000, -0.000000000000000000 ) ) ;
#68936=ORIENTED_EDGE ( 'NONE', *, *, #22174, .T. ) ;
#68944=DIRECTION ( 'NONE',  ( -0.000000000000000000, 0.000000000000000000, -1.000000000000000000 ) ) ;
#68946=ORIENTED_EDGE ( 'NONE', *, *, #3691, .F. ) ;
#68953=DIRECTION ( 'NONE',  ( -0.000000000000000000, 0.000000000000000000, -1.000000000000000000 ) ) ;
#68972=EDGE_CURVE ( 'NONE', #26540, #61448, #16814, .T. ) ;
#68983=DIRECTION ( 'NONE',  ( -0.000000000000000000, 0.000000000000000000, -1.000000000000000000 ) ) ;
#68984=FACE_OUTER_BOUND ( 'NONE', #37764, .T. ) ;
#68997=CARTESIAN_POINT ( 'NONE',  ( 3.749999999999999556, 33.99999999999998579, -3.750000000000000000 ) ) ;
#69001=EDGE_LOOP ( 'NONE', ( #67092, #50036, #268, #13311 ) ) ;
#69023=ADVANCED_FACE ( 'NONE', ( #56416 ), #33414, .T. ) ;
#69030=ORIENTED_EDGE ( 'NONE', *, *, #54170, .T. ) ;
#69057=EDGE_LOOP ( 'NONE', ( #38605, #16934, #12921, #46461 ) ) ;
#69062=LINE ( 'NONE', #36006, #31689 ) ;
#69071=VERTEX_POINT ( 'NONE', #31403 ) ;
#69088=CONICAL_SURFACE ( 'NONE', #8433, 3.600000000000005862, 0.7853981633974447263 ) ;
#69093=EDGE_LOOP ( 'NONE', ( #1092, #41363, #51472, #4286 ) ) ;
#69102=DIRECTION ( 'NONE',  ( 0.000000000000000000, 1.000000000000000000, 0.000000000000000000 ) ) ;
#69110=EDGE_CURVE ( 'NONE', #39296, #20493, #54842, .T. ) ;
#69119=LINE ( 'NONE', #20928, #20934 ) ;
#69121=EDGE_CURVE ( 'NONE', #47549, #65448, #63441, .T. ) ;
#69124=AXIS2_PLACEMENT_3D ( 'NONE', #65663, #49167, #6230 ) ;
#69127=CARTESIAN_POINT ( 'NONE',  ( 62.10000000000000142, 11.99999999999999822, 3.499999999999992895 ) ) ;
#69133=FACE_OUTER_BOUND ( 'NONE', #35777, .T. ) ;
#69149=CARTESIAN_POINT ( 'NONE',  ( 21.24999999999998579, -2.457524924300472510E-14, 3.750000000000000000 ) ) ;
#69157=VERTEX_POINT ( 'NONE', #48604 ) ;
#69174=DIRECTION ( 'NONE',  ( 0.000000000000000000, 0.000000000000000000, -1.000000000000000000 ) ) ;
#69180=CIRCLE ( 'NONE', #5133, 0.5000000000000004441 ) ;
#69196=ORIENTED_EDGE ( 'NONE', *, *, #69336, .F. ) ;
#69205=CARTESIAN_POINT ( 'NONE',  ( 66.74999999999998579, 36.75000000000000000, 4.000000000000000000 ) ) ;
#69220=LINE ( 'NONE', #20679, #22052 ) ;
#69222=DIRECTION ( 'NONE',  ( -1.000000000000000000, 0.000000000000000000, 0.000000000000000000 ) ) ;
#69225=CARTESIAN_POINT ( 'NONE',  ( 30.25000000000002842, 3.498359009886561184E-14, 4.000000000000000000 ) ) ;
#69227=EDGE_LOOP ( 'NONE', ( #39033, #40814, #30664, #2003 ) ) ;
#69237=CARTESIAN_POINT ( 'NONE',  ( 21.25000000000001066, 24.74999999999998224, 3.750000000000000000 ) ) ;
#69269=VERTEX_POINT ( 'NONE', #19658 ) ;
#69281=ORIENTED_EDGE ( 'NONE', *, *, #28702, .F. ) ;
#69288=DIRECTION ( 'NONE',  ( 0.000000000000000000, -1.000000000000000000, 0.000000000000000000 ) ) ;
#69294=ORIENTED_EDGE ( 'NONE', *, *, #11023, .F. ) ;
#69298=VECTOR ( 'NONE', #49074, 1000.000000000000000 ) ;
#69303=ORIENTED_EDGE ( 'NONE', *, *, #21282, .F. ) ;
#69310=CARTESIAN_POINT ( 'NONE',  ( 48.74999999999999289, 24.99999999999998579, 3.750000000000000000 ) ) ;
#69318=DIRECTION ( 'NONE',  ( -0.000000000000000000, 0.000000000000000000, -1.000000000000000000 ) ) ;
#69326=DIRECTION ( 'NONE',  ( -1.000000000000000000, -2.168404344971008868E-16, 0.000000000000000000 ) ) ;
#69332=VECTOR ( 'NONE', #43396, 1000.000000000000000 ) ;
#69336=EDGE_CURVE ( 'NONE', #49467, #5853, #9055, .T. ) ;
#69338=CARTESIAN_POINT ( 'NONE',  ( 12.75000000000000533, 28.24999999999998224, -3.750000000000000000 ) ) ;
#69346=EDGE_CURVE ( 'NONE', #24587, #41886, #21738, .T. ) ;
#69355=CIRCLE ( 'NONE', #39061, 0.2500000000000002220 ) ;
#69364=FACE_OUTER_BOUND ( 'NONE', #38381, .T. ) ;
#69381=AXIS2_PLACEMENT_3D ( 'NONE', #27029, #10888, #58379 ) ;
#69388=FACE_OUTER_BOUND ( 'NONE', #8402, .T. ) ;
#69390=SURFACE_STYLE_FILL_AREA ( #36382 ) ;
#69423=EDGE_CURVE ( 'NONE', #11461, #69157, #26979, .T. ) ;
#69428=ADVANCED_FACE ( 'NONE', ( #7624 ), #7297, .T. ) ;
#69430=CARTESIAN_POINT ( 'NONE',  ( 16.75000000000000711, 0.000000000000000000, 4.000000000000000000 ) ) ;
#69432=EDGE_CURVE ( 'NONE', #51828, #40202, #29226, .T. ) ;
#69448=COLOUR_RGB ( '', 0.40784314, 0.44705882, 0.49803922) ;
#69450=AXIS2_PLACEMENT_3D ( 'NONE', #23793, #39656, #45296 ) ;
#69466=DIRECTION ( 'NONE',  ( 0.000000000000000000, 0.000000000000000000, 1.000000000000000000 ) ) ;
#69515=ORIENTED_EDGE ( 'NONE', *, *, #14156, .F. ) ;
#69536=ADVANCED_FACE ( 'NONE', ( #45987 ), #7895, .T. ) ;
#69545=VECTOR ( 'NONE', #5032, 1000.000000000000000 ) ;
#69573=DIRECTION ( 'NONE',  ( -1.000000000000000000, 0.000000000000000000, 0.000000000000000000 ) ) ;
#69595=ORIENTED_EDGE ( 'NONE', *, *, #38732, .T. ) ;
#69600=CARTESIAN_POINT ( 'NONE',  ( 53.24999999999999289, 27.74999999999998579, -4.000000000000000000 ) ) ;
#69601=ORIENTED_EDGE ( 'NONE', *, *, #55026, .F. ) ;
#69608=ORIENTED_EDGE ( 'NONE', *, *, #36180, .F. ) ;
#69609=VECTOR ( 'NONE', #31817, 1000.000000000000000 ) ;
#69618=ORIENTED_EDGE ( 'NONE', *, *, #31868, .F. ) ;
#69623=CARTESIAN_POINT ( 'NONE',  ( 3.249999999999998668, 36.99999999999999289, -3.750000000000000000 ) ) ;
#69626=DIRECTION ( 'NONE',  ( -1.000000000000000000, 0.000000000000000000, 0.000000000000000000 ) ) ;
#69627=ORIENTED_EDGE ( 'NONE', *, *, #54408, .T. ) ;
#69635=DIRECTION ( 'NONE',  ( 0.000000000000000000, 0.000000000000000000, -1.000000000000000000 ) ) ;
#69639=ORIENTED_EDGE ( 'NONE', *, *, #54481, .T. ) ;
#69642=DIRECTION ( 'NONE',  ( -1.000000000000000000, 0.000000000000000000, 0.000000000000000000 ) ) ;
#69643=CARTESIAN_POINT ( 'NONE',  ( 43.75000000000000000, 19.24999999999998224, -3.750000000000000000 ) ) ;
#69646=VERTEX_POINT ( 'NONE', #19206 ) ;
#69648=FACE_OUTER_BOUND ( 'NONE', #25685, .T. ) ;
#69649=EDGE_CURVE ( 'NONE', #38116, #50390, #33748, .T. ) ;
#69650=CARTESIAN_POINT ( 'NONE',  ( 57.49999999999999289, 27.74999999999998934, -3.750000000000000000 ) ) ;
#69666=DIRECTION ( 'NONE',  ( 1.000000000000000000, 2.312964634635740689E-15, -0.000000000000000000 ) ) ;
#69670=AXIS2_PLACEMENT_3D ( 'NONE', #4502, #63617, #21385 ) ;
#69684=AXIS2_PLACEMENT_3D ( 'NONE', #18967, #30214, #41181 ) ;
ENDSEC;
END-ISO-10303-21;
